ISO-10303-21;
HEADER;
FILE_DESCRIPTION (('STEP AP214'),
    '1' );
FILE_NAME ('Actuator Return Helical Spring.step',
    '2026-10-09T19:32:29',
    ( '' ),
    ( '' ),
    'SwSTEP 2.0',
    'SolidWorks 2026',
    '' );
FILE_SCHEMA (( 'AUTOMOTIVE_DESIGN' ));
ENDSEC;

DATA;
#1=PRODUCT_DEFINITION_FORMATION_WITH_SPECIFIED_SOURCE ( 'ANY', '', #17748, .NOT_KNOWN. ) ;
#3=CARTESIAN_POINT ( 'NONE',  ( -1.670747221194380128, -5.103620102360550526, 3.047345349617600174 ) ) ;
#5=CARTESIAN_POINT ( 'NONE',  ( 1.315859850362970151, -5.328211948015590060, 2.737664967889629875 ) ) ;
#8=CARTESIAN_POINT ( 'NONE',  ( -0.4005155088301869948, -1.125163681423230200, 7.019123328904779413 ) ) ;
#10=CARTESIAN_POINT ( 'NONE',  ( -0.8934014991059870958, -4.614566048306490309, 6.877287176483410924 ) ) ;
#12=CARTESIAN_POINT ( 'NONE',  ( 2.044452488559148851, -4.148800282540726414, 4.887392274793745273 ) ) ;
#23=CARTESIAN_POINT ( 'NONE',  ( -1.526871680339578541, -5.259957627118655665, 3.327650196883449762 ) ) ;
#24=CARTESIAN_POINT ( 'NONE',  ( 1.236224677598260158, -1.986830348089900777, 2.351625617688071657 ) ) ;
#26=CARTESIAN_POINT ( 'NONE',  ( 1.652654650382400003, -0.7952867690272209522, 3.029252778805629820 ) ) ;
#31=CARTESIAN_POINT ( 'NONE',  ( -1.669205944673819886, -3.147403886144329643, 6.359065158982450505 ) ) ;
#32=CARTESIAN_POINT ( 'NONE',  ( -1.599895119336340876, -2.871785303044851023, 5.986560317183706736 ) ) ;
#33=CARTESIAN_POINT ( 'NONE',  ( 1.821706171509118954, -0.09788135593220394226, 5.646608543709396244 ) ) ;
#35=CARTESIAN_POINT ( 'NONE',  ( -0.06264882350515391107, -0.4512711864406790396, 7.052569299041220319 ) ) ;
#38=CARTESIAN_POINT ( 'NONE',  ( -2.058670345754650022, -0.2491525423728820077, 3.559656372813929881 ) ) ;
#39=CARTESIAN_POINT ( 'NONE',  ( -0.09706517602693919000, -2.961097579838030125, 7.051451474958980725 ) ) ;
#43=CARTESIAN_POINT ( 'NONE',  ( 2.062913653388429136, -2.382731248990799688, 5.832754583370791224 ) ) ;
#46=CARTESIAN_POINT ( 'NONE',  ( -0.6640878839024662028, -5.462076271186444565, 7.269405042592523181 ) ) ;
#48=CARTESIAN_POINT ( 'NONE',  ( 0.7109160811436110450, -1.307629111369560171, 6.943511536198400336 ) ) ;
#49=CARTESIAN_POINT ( 'NONE',  ( 1.750316316486830059, -0.3400423728813560253, 3.126818518378580158 ) ) ;
#53=CARTESIAN_POINT ( 'NONE',  ( -1.883235269974520287, -3.240557039297494057, 5.517512544583926370 ) ) ;
#58=CARTESIAN_POINT ( 'NONE',  ( 0.5137283630188955730, -0.4379237288135597317, 6.687652957477222770 ) ) ;
#60=CARTESIAN_POINT ( 'NONE',  ( -1.440522616026439495, -4.804713230972779137, 3.241384813161591438 ) ) ;
#61=CARTESIAN_POINT ( 'NONE',  ( -1.647941990407690627, -5.555508474576275724, 3.475676388127094896 ) ) ;
#65=CARTESIAN_POINT ( 'NONE',  ( -0.5198535559317755128, -0.5906145504024216120, 2.087183161631441131 ) ) ;
#68=CARTESIAN_POINT ( 'NONE',  ( 1.097561405233190124, -1.986830348089889897, 2.618148744692249785 ) ) ;
#70=CARTESIAN_POINT ( 'NONE',  ( -2.039016451601939117, -3.011515032774579215, 4.939402908764104261 ) ) ;
#73=COLOUR_RGB ( '', 0.09019608, 0.27058824, 0.51372549) ;
#75=CARTESIAN_POINT ( 'NONE',  ( -0.5609751937345790473, -0.4601694915254239682, 7.293870047334757523 ) ) ;
#76=CARTESIAN_POINT ( 'NONE',  ( -1.145304265383870090, -3.077539021279469988, 6.755972720436099088 ) ) ;
#79=CARTESIAN_POINT ( 'NONE',  ( -2.638803263991410741, -5.219915254237295521, 4.982085668537435730 ) ) ;
#85=CARTESIAN_POINT ( 'NONE',  ( 1.668426559427239608, -1.214475958216409746, 6.763847501342977075 ) ) ;
#89=CARTESIAN_POINT ( 'NONE',  ( 0.2435295127647320035, -5.004947479095229745, 2.350795284704489507 ) ) ;
#92=CARTESIAN_POINT ( 'NONE',  ( -1.026235786675429917, -1.195028546288090077, 6.817920158464570335 ) ) ;
#95=CARTESIAN_POINT ( 'NONE',  ( 0.6150581927482109412, -4.451548030288480895, 6.971662190339319665 ) ) ;
#97=CARTESIAN_POINT ( 'NONE',  ( 0.8893259633308030487, -3.846052534792983923, 2.849594321892129134 ) ) ;
#107=CARTESIAN_POINT ( 'NONE',  ( -1.489797906646480596, -5.188771186440680694, 6.112509577910826941 ) ) ;
#116=CARTESIAN_POINT ( 'NONE',  ( -0.09706517602693919000, -2.961097579838030125, 7.051451474958980725 ) ) ;
#117=CARTESIAN_POINT ( 'NONE',  ( 1.978802102381368888, -3.756740257999804378, 4.152967933079626306 ) ) ;
#118=CARTESIAN_POINT ( 'NONE',  ( 1.851073041990159984, -0.4067796610169499560, 6.153284478378259870 ) ) ;
#122=CARTESIAN_POINT ( 'NONE',  ( 0.3803919826356921829, -0.008898305084746057844, 2.682580100125298461 ) ) ;
#123=CARTESIAN_POINT ( 'NONE',  ( -1.552749016687749783, -1.563800282540730002, 6.468535037441760061 ) ) ;
#126=CARTESIAN_POINT ( 'NONE',  ( 1.236334101859160262, -3.570433951693499974, 2.697445712080690949 ) ) ;
#128=CARTESIAN_POINT ( 'NONE',  ( -2.560337424259679917, -5.537711864406785978, 4.001768473655595848 ) ) ;
#131=CARTESIAN_POINT ( 'NONE',  ( -1.432215783582709401, -0.4868644067796619179, 6.170863372171116801 ) ) ;
#136=CARTESIAN_POINT ( 'NONE',  ( 1.854389246811829706, -2.448755237495690462, 3.819010576716856065 ) ) ;
#137=CARTESIAN_POINT ( 'NONE',  ( 2.638803263991410741, -0.3800847457627119508, 4.982085668537405532 ) ) ;
#140=CARTESIAN_POINT ( 'NONE',  ( 1.965557623688110933, -0.3889830508474575455, 5.292675575926325315 ) ) ;
#144=CARTESIAN_POINT ( 'NONE',  ( 0.05465110135556765225, -5.448728813559320372, 6.752241303418941243 ) ) ;
#145=CARTESIAN_POINT ( 'NONE',  ( 2.011500846714318502, -0.04894067796610199889, 3.478373409938461336 ) ) ;
#146=CARTESIAN_POINT ( 'NONE',  ( 1.791574935211219799, -5.408686440677969998, 6.226029630577610163 ) ) ;
#147=CARTESIAN_POINT ( 'NONE',  ( -0.2097343361107079085, -0.5962015548080615845, 2.050670208512068715 ) ) ;
#150=CARTESIAN_POINT ( 'NONE',  ( 1.917298190932609891, -2.103271789531340197, 3.335187436117899917 ) ) ;
#153=CARTESIAN_POINT ( 'NONE',  ( -1.831349212334698828, -1.590929447188999646, 3.772065786216939554 ) ) ;
#158=CARTESIAN_POINT ( 'NONE',  ( -2.020286629067959971, -0.4913135593220345210, 6.420841923842841581 ) ) ;
#159=CARTESIAN_POINT ( 'NONE',  ( -2.283153923255329953, -3.403575057315510133, 4.129076318403500423 ) ) ;
#162=CARTESIAN_POINT ( 'NONE',  ( -2.458531667407850563, -5.206567796610170440, 5.699238225248945966 ) ) ;
#165=CARTESIAN_POINT ( 'NONE',  ( -2.353194804772640314, -5.224364406779659298, 4.731327187377240229 ) ) ;
#168=CARTESIAN_POINT ( 'NONE',  ( -2.349129089426440054, -4.894025507765950245, 4.842612091679129982 ) ) ;
#170=CARTESIAN_POINT ( 'NONE',  ( 0.6575972843460591299, -0.3612150962701959900, 2.110392115010549130 ) ) ;
#172=CARTESIAN_POINT ( 'NONE',  ( 2.334032080503399609, -2.289578095837639715, 5.001728246382190157 ) ) ;
#175=CARTESIAN_POINT ( 'NONE',  ( 1.724579595320000047, -3.939205687946140344, 3.098572228637889836 ) ) ;
#178=CARTESIAN_POINT ( 'NONE',  ( 1.835037444103841286, -4.241953435693877061, 5.620619042473564697 ) ) ;
#180=CARTESIAN_POINT ( 'NONE',  ( 2.011500846714319835, -0.3489406779661020086, 3.478373409938460448 ) ) ;
#191=CARTESIAN_POINT ( 'NONE',  ( 1.782460458101500889, -5.399788135593215799, 5.718585207845976015 ) ) ;
#192=CARTESIAN_POINT ( 'NONE',  ( -0.3832714063288900630, -2.685478996738538626, 7.326064873930687504 ) ) ;
#194=CARTESIAN_POINT ( 'NONE',  ( 1.662071288245189793, -0.7952852869591279239, 3.019836320359400084 ) ) ;
#196=CARTESIAN_POINT ( 'NONE',  ( 0.009452110982653675123, -5.000192044704546035, 2.050000000000001155 ) ) ;
#202=CARTESIAN_POINT ( 'NONE',  ( 2.276802572547980130, -2.495331814072260013, 4.104251954998760610 ) ) ;
#203=CARTESIAN_POINT ( 'NONE',  ( 1.750352751699790987, -3.686875393134939394, 3.627075451280439733 ) ) ;
#204=CARTESIAN_POINT ( 'NONE',  ( 0.1910247150515120007, -0.004449152542373194588, 2.655937705488500722 ) ) ;
#212=CARTESIAN_POINT ( 'NONE',  ( -2.043308330018790198, -0.2002118644067800157, 5.867646457774669422 ) ) ;
#213=CARTESIAN_POINT ( 'NONE',  ( -1.881914957835490121, -1.936412895153350133, 3.286797332666350435 ) ) ;
#221=CARTESIAN_POINT ( 'NONE',  ( -1.644832646965619372, -4.408812330071871344, 6.383232381746490880 ) ) ;
#223=CARTESIAN_POINT ( 'NONE',  ( -2.645377369053839356, -5.228813559322024851, 4.488260618344918740 ) ) ;
#227=CARTESIAN_POINT ( 'NONE',  ( 2.270487904532159984, -0.3622881355932209835, 4.080813552109670894 ) ) ;
#232=B_SPLINE_CURVE_WITH_KNOTS ( 'NONE', 3,
 ( #17325, #2928, #4655, #4553, #14218, #1537, #7186 ),
 .UNSPECIFIED., .F., .F.,
 ( 4, 1, 1, 1, 4 ),
 ( 18.06415775814129887, 18.36448856483159986, 18.49670707487869947, 18.62179267666130045, 18.84955592153880133 ),
 .UNSPECIFIED. ) ;
#233=CARTESIAN_POINT ( 'NONE',  ( 1.810994336139499783, -2.681638120378568857, 5.667058093962681120 ) ) ;
#239=ADVANCED_FACE ( 'NONE', ( #1597 ), #11504, .T. ) ;
#243=CARTESIAN_POINT ( 'NONE',  ( -0.5664586606772434862, -5.586652542372875452, 2.726727161522279452 ) ) ;
#247=CARTESIAN_POINT ( 'NONE',  ( 1.000896394980339332, -0.1290254237288140371, 6.829956240957368863 ) ) ;
#251=CARTESIAN_POINT ( 'NONE',  ( 0.03714311608463249925, -1.078587104846649991, 7.053160869216429596 ) ) ;
#254=CARTESIAN_POINT ( 'NONE',  ( -0.1086361371090530797, -2.662190708450249854, 6.750146344128172160 ) ) ;
#262=CARTESIAN_POINT ( 'NONE',  ( -2.321479326063761395, -0.5491525423728815802, 3.414080590619972710 ) ) ;
#263=CARTESIAN_POINT ( 'NONE',  ( -0.2564439965878500538, -4.544701183441629766, 7.039440566481220074 ) ) ;
#266=CARTESIAN_POINT ( 'NONE',  ( -0.6640878839024662028, -5.162076271186444743, 7.269405042592523181 ) ) ;
#273=CARTESIAN_POINT ( 'NONE',  ( -2.461935615161759294, -1.680241723982170754, 5.690952430644365734 ) ) ;
#274=CARTESIAN_POINT ( 'NONE',  ( -0.009452110982655128821, -0.5998079552954630467, 2.350000000000000089 ) ) ;
#276=CARTESIAN_POINT ( 'NONE',  ( 1.816660071039059909, -2.429307825567370127, 6.196159040268200968 ) ) ;
#277=CARTESIAN_POINT ( 'NONE',  ( 1.338894208872951186, -5.333856471232010676, 3.139702328019969180 ) ) ;
#278=CARTESIAN_POINT ( 'NONE',  ( 1.864786684738361178, -0.7952867690272195089, 2.817120744449660652 ) ) ;
#282=CARTESIAN_POINT ( 'NONE',  ( -1.953802435660519921, -4.987178660919110662, 4.069478085301024173 ) ) ;
#292=CARTESIAN_POINT ( 'NONE',  ( 0.2453710345350221533, -5.444279661016954819, 6.738252723719333481 ) ) ;
#293=CARTESIAN_POINT ( 'NONE',  ( -2.339254516529639449, -2.918361879621429011, 5.953396186326395778 ) ) ;
#299=CARTESIAN_POINT ( 'NONE',  ( -2.036228139452650243, -3.473439922180369788, 3.519948877554409883 ) ) ;
#300=CARTESIAN_POINT ( 'NONE',  ( 1.942813984510739056, -1.074746228486680000, 5.363608065214415355 ) ) ;
#301=CARTESIAN_POINT ( 'NONE',  ( 0.5664586606772286093, -0.01334745762711899916, 2.726727161522279452 ) ) ;
#306=CARTESIAN_POINT ( 'NONE',  ( 2.603140590302639890, -3.873181699441240244, 5.216500493824248963 ) ) ;
#307=CARTESIAN_POINT ( 'NONE',  ( -0.7982439214406890082, -0.1690677966101698793, 6.591424794228156081 ) ) ;
#308=CARTESIAN_POINT ( 'NONE',  ( 1.074829861819710075, -2.285737219477669946, 2.606322265575589991 ) ) ;
#311=CARTESIAN_POINT ( 'NONE',  ( -1.444955263746759533, -3.267686203945749490, 2.842353646881510709 ) ) ;
#313=CARTESIAN_POINT ( 'NONE',  ( 2.651721837666119796, -5.073093220338980025, 4.594045830208265180 ) ) ;
#318=CARTESIAN_POINT ( 'NONE',  ( -2.350067830300900162, -0.5224576271186440746, 4.825253242917699303 ) ) ;
#323=CARTESIAN_POINT ( 'NONE',  ( -0.1781895581254780980, -2.146007489747939090, 2.654724878163539969 ) ) ;
#325=CARTESIAN_POINT ( 'NONE',  ( -1.713314936023349944, -0.5610169491525430763, 3.089913064446579760 ) ) ;
#332=CARTESIAN_POINT ( 'NONE',  ( 0.009303514085962454744, -0.3025471796894717014, 2.316528937223512497 ) ) ;
#333=CARTESIAN_POINT ( 'NONE',  ( -1.088937603231280304, -5.573305084745765470, 2.959627624143549074 ) ) ;
#336=B_SPLINE_CURVE_WITH_KNOTS ( 'NONE', 3,
 ( #3611, #846, #9261, #16396, #652, #10551, #6486, #16212, #12146, #3518, #17765, #8602, #2858, #12943, #14328, #1649 ),
 .UNSPECIFIED., .F., .F.,
 ( 4, 1, 1, 1, 1, 1, 1, 1, 1, 1, 1, 1, 1, 4 ),
 ( 0.4999998211434338868, 0.5106244842458940170, 0.5531978902117569152, 0.5957712970451829460, 0.6383447191101619955, 0.6809180289765489613, 0.7234918990886729517, 0.7660634153087889642, 0.8086437809560700352, 0.8511815656862139479, 0.8935997744640420404, 0.9363910903531720287, 0.9718312009676199903, 1.000000000000000000 ),
 .UNSPECIFIED. ) ;
#337=CARTESIAN_POINT ( 'NONE',  ( -1.236224677598320332, -3.613169651910099756, 2.351625617688101411 ) ) ;
#339=CARTESIAN_POINT ( 'NONE',  ( -1.219286470748949913, -1.218316834576380181, 6.712979431025680732 ) ) ;
#342=CARTESIAN_POINT ( 'NONE',  ( 2.029711248330070994, -2.219713230972778728, 4.391497016172514201 ) ) ;
#347=CARTESIAN_POINT ( 'NONE',  ( 2.524473153133520054, -0.6128213390808875394, 3.881373716577345867 ) ) ;
#348=CARTESIAN_POINT ( 'NONE',  ( -0.8934014991059870958, -4.614566048306490309, 6.877287176483410924 ) ) ;
#351=CARTESIAN_POINT ( 'NONE',  ( 2.351526912647309953, -5.073093220338979137, 4.606040641882800379 ) ) ;
#358=CARTESIAN_POINT ( 'NONE',  ( 2.022685914314938938, -1.167899381639830203, 6.418096442297061444 ) ) ;
#360=CARTESIAN_POINT ( 'NONE',  ( 1.139503474074560874, -0.7471169921413568504, 2.982738323988489260 ) ) ;
#362=CARTESIAN_POINT ( 'NONE',  ( -0.3413183941262150078, -2.685478996738539958, 7.028571974690709823 ) ) ;
#364=CARTESIAN_POINT ( 'NONE',  ( -0.1785884594054470975, -1.400782264522720366, 7.347870815423047652 ) ) ;
#366=CARTESIAN_POINT ( 'NONE',  ( 0.1608173401625761778, -4.498124606865046893, 6.746714348835997299 ) ) ;
#367=CARTESIAN_POINT ( 'NONE',  ( -2.043308330018790198, -0.5002118644067800046, 5.867646457774669422 ) ) ;
#376=CARTESIAN_POINT ( 'NONE',  ( -3.503171016405825766E-15, -5.300000000000000711, 2.649999999999998579 ) ) ;
#377=CARTESIAN_POINT ( 'NONE',  ( -2.353343516942199898, -1.773394877135329839, 4.722803042560189901 ) ) ;
#378=CARTESIAN_POINT ( 'NONE',  ( 0.4722227023514015687, -3.477280798540335560, 2.088464165977070408 ) ) ;
#383=CARTESIAN_POINT ( 'NONE',  ( 1.928817277882869829, -1.144611093351550091, 6.048484184565929844 ) ) ;
#385=CARTESIAN_POINT ( 'NONE',  ( 1.401708661791409849, -4.358394877135329359, 6.590491606684049763 ) ) ;
#386=CARTESIAN_POINT ( 'NONE',  ( -2.032257487115171291, -4.571830348089889640, 4.991258216523934976 ) ) ;
#387=CARTESIAN_POINT ( 'NONE',  ( 0.009037091307169229856, -5.006769755134070188, 2.399753621991540076 ) ) ;
#390=CARTESIAN_POINT ( 'NONE',  ( 2.543624461644950152, -3.896469987729531681, 5.457025951419980814 ) ) ;
#391=CARTESIAN_POINT ( 'NONE',  ( -2.051331987628511211, -0.2269067796610169385, 4.618035453557344461 ) ) ;
#392=CARTESIAN_POINT ( 'NONE',  ( -2.111627294540180166, -1.889836318576769925, 3.660877362176710559 ) ) ;
#397=CARTESIAN_POINT ( 'NONE',  ( 1.741913176380120110, -3.640298816558360517, 3.117443785062520067 ) ) ;
#400=CARTESIAN_POINT ( 'NONE',  ( -0.1765068388402301069, -5.153177966101685215, 7.347961541693647902 ) ) ;
#403=CARTESIAN_POINT ( 'NONE',  ( -1.925796468768790071, -0.4957627118644070130, 6.052706598917719560 ) ) ;
#407=CARTESIAN_POINT ( 'NONE',  ( 0.2047443300700049207, -2.192584066324520187, 2.657212296411530783 ) ) ;
#409=CARTESIAN_POINT ( 'NONE',  ( 1.192209327851080136, -0.02224576271186471527, 2.329031440774910422 ) ) ;
#413=CARTESIAN_POINT ( 'NONE',  ( 0.007090208766915150063, -0.3376261948321719886, 2.248104425785740101 ) ) ;
#414=CARTESIAN_POINT ( 'NONE',  ( -0.3265524029357583236, -5.457627118644064801, 6.726831181542982208 ) ) ;
#418=CARTESIAN_POINT ( 'NONE',  ( -1.873832970144350130, -0.2625000000000002331, 2.826167029855650270 ) ) ;
#419=CARTESIAN_POINT ( 'NONE',  ( -2.589141052314440916, -3.287133615874059611, 5.282633936723525991 ) ) ;
#421=CARTESIAN_POINT ( 'NONE',  ( -1.167621112247339887, -2.778632149891699932, 6.743381174846780013 ) ) ;
#424=CARTESIAN_POINT ( 'NONE',  ( -0.3429245540020551819, -1.823812330071880705, 2.675820019639910452 ) ) ;
#428=CARTESIAN_POINT ( 'NONE',  ( -0.009452110982655128821, -0.5998079552954630467, 2.350000000000000089 ) ) ;
#429=CARTESIAN_POINT ( 'NONE',  ( -2.549960444629829848, -1.544352870612421880, 3.964598460822165382 ) ) ;
#434=CARTESIAN_POINT ( 'NONE',  ( 2.328217775191430139, -5.081991525423729783, 5.043379051721160522 ) ) ;
#439=ADVANCED_FACE ( 'NONE', ( #5496 ), #3228, .T. ) ;
#442=CARTESIAN_POINT ( 'NONE',  ( 2.339254516529669647, -2.681638120378568857, 5.953396186326336270 ) ) ;
#445=CARTESIAN_POINT ( 'NONE',  ( -0.3949552299395130417, -1.823812330071880039, 2.379923265530350385 ) ) ;
#446=CARTESIAN_POINT ( 'NONE',  ( 1.487835687536851470, -5.028306595106930565, 2.490167689244129789 ) ) ;
#447=CARTESIAN_POINT ( 'NONE',  ( -2.653777292528150866, -1.773394877135329839, 4.724078510415215426 ) ) ;
#449=CARTESIAN_POINT ( 'NONE',  ( -1.772995665808888788, -4.777584066324515710, 5.735078843205186239 ) ) ;
#452=ORIENTED_EDGE ( 'NONE', *, *, #9830, .T. ) ;
#454=CARTESIAN_POINT ( 'NONE',  ( -0.009452110982656868748, -5.299807955295460005, 2.350000000000000089 ) ) ;
#459=CARTESIAN_POINT ( 'NONE',  ( 2.347833536521260367, -2.541908390648839777, 4.537447324629859224 ) ) ;
#461=CARTESIAN_POINT ( 'NONE',  ( 1.811729841638690219, -5.341949152542369461, 3.197954009834290012 ) ) ;
#464=CARTESIAN_POINT ( 'NONE',  ( 2.287919158821199783, -1.051457940198389895, 5.251517552016890633 ) ) ;
#465=CARTESIAN_POINT ( 'NONE',  ( 2.353452300571019506, -4.125511994252439862, 4.697179287168359529 ) ) ;
#466=CARTESIAN_POINT ( 'NONE',  ( 1.688800633088581860, -0.8418633456037974971, 3.532586505616389871 ) ) ;
#473=CARTESIAN_POINT ( 'NONE',  ( 0.3803919826356921829, -0.3088983050847459166, 2.682580100125298461 ) ) ;
#474=CARTESIAN_POINT ( 'NONE',  ( 0.4005155088302400634, -4.474836318576759453, 7.019123328904770531 ) ) ;
#479=CARTESIAN_POINT ( 'NONE',  ( -0.2818998297622349325, -4.245794312053861042, 7.036509827384406890 ) ) ;
#480=CARTESIAN_POINT ( 'NONE',  ( 1.031876288691629506, -5.130932203389829915, 7.145012538880298081 ) ) ;
#484=CARTESIAN_POINT ( 'NONE',  ( -2.293398556041709835, -0.5358050847457630494, 4.171956209133480975 ) ) ;
#488=CARTESIAN_POINT ( 'NONE',  ( -1.937109463115380903, -3.426863345603793576, 4.019920026366796684 ) ) ;
#489=CARTESIAN_POINT ( 'NONE',  ( -1.666450993087168930, -0.4824152542372879826, 6.765380371283871597 ) ) ;
#494=CARTESIAN_POINT ( 'NONE',  ( -0.009227126607029439292, -0.5962421434521730790, 2.310024366371980165 ) ) ;
#495=CARTESIAN_POINT ( 'NONE',  ( 0.06264882350516240428, -5.448728813559320372, 7.052569299041220319 ) ) ;
#496=CARTESIAN_POINT ( 'NONE',  ( -1.811729841638699767, -0.2580508474576270195, 3.197954009834300226 ) ) ;
#498=CARTESIAN_POINT ( 'NONE',  ( 1.155768864438629695, -4.404971453711897134, 7.088998121597438029 ) ) ;
#500=CARTESIAN_POINT ( 'NONE',  ( 2.334032080503399609, -2.289578095837639715, 5.001728246382190157 ) ) ;
#503=AXIS2_PLACEMENT_3D ( 'NONE', #7453, #4395, #3187 ) ;
#505=CARTESIAN_POINT ( 'NONE',  ( 0.7368491673939637776, -3.523857375116919322, 2.783765372628159263 ) ) ;
#508=CARTESIAN_POINT ( 'NONE',  ( 0.4114611322411816374, -1.032010528270079330, 6.711368086473216366 ) ) ;
#516=CARTESIAN_POINT ( 'NONE',  ( 0.7756407636289058827, -1.008722239981790558, 7.238010066725317770 ) ) ;
#521=CARTESIAN_POINT ( 'NONE',  ( 1.477796163681079911, -5.117584745762710163, 6.531563725478140015 ) ) ;
#528=EDGE_CURVE ( 'NONE', #17501, #10555, #13235, .T. ) ;
#530=CARTESIAN_POINT ( 'NONE',  ( -0.1110902655589390137, -2.961097579838030569, 7.351560417169478612 ) ) ;
#535=CARTESIAN_POINT ( 'NONE',  ( 2.036228139452630259, -2.126560077819629857, 3.519948877554369915 ) ) ;
#539=CARTESIAN_POINT ( 'NONE',  ( -2.161802606005209793, -5.010466949207389220, 3.769755311421840283 ) ) ;
#555=CARTESIAN_POINT ( 'NONE',  ( 0.4539185741479240255, -2.215872354612800521, 2.390735265170440105 ) ) ;
#563=CARTESIAN_POINT ( 'NONE',  ( 0.4005155088302400634, -4.474836318576759453, 7.019123328904770531 ) ) ;
#564=CARTESIAN_POINT ( 'NONE',  ( 2.050994839075679366, -0.9815930753335269099, 4.608774933727144862 ) ) ;
#565=CARTESIAN_POINT ( 'NONE',  ( 0.8731223871105069367, -0.1290254237288140371, 6.558046933601105799 ) ) ;
#569=CARTESIAN_POINT ( 'NONE',  ( -0.9707742057416274273, -0.1735169491525429541, 6.508944043303927174 ) ) ;
#570=CARTESIAN_POINT ( 'NONE',  ( -2.351999299633229956, -3.333710192450639820, 4.782734406438290620 ) ) ;
#578=CARTESIAN_POINT ( 'NONE',  ( -1.610878918935079840, -5.568855932203385706, 2.590989782159090815 ) ) ;
#580=CARTESIAN_POINT ( 'NONE',  ( 2.306642602145299925, -0.3845338983050849979, 5.166805192608480368 ) ) ;
#586=CARTESIAN_POINT ( 'NONE',  ( 1.974086094277279768, -4.195376859117311064, 5.263813741415705572 ) ) ;
#587=CARTESIAN_POINT ( 'NONE',  ( 1.554165089654128584, -0.1201271186440679706, 6.851145244874527584 ) ) ;
#590=CARTESIAN_POINT ( 'NONE',  ( -2.431060148753501515, -0.5447033898305090327, 3.635668498923334102 ) ) ;
#596=CARTESIAN_POINT ( 'NONE',  ( 2.642175029090480631, -4.102223705964154199, 4.450952196049445142 ) ) ;
#599=CARTESIAN_POINT ( 'NONE',  ( 2.295719155670170153, -2.312866384125930264, 5.218091927917190453 ) ) ;
#602=CARTESIAN_POINT ( 'NONE',  ( 0.6965028529799376367, -4.129352870612409632, 6.631265289497767057 ) ) ;
#604=CARTESIAN_POINT ( 'NONE',  ( 1.673492459604400961, -2.103271789531340641, 3.510746103527379702 ) ) ;
#608=CARTESIAN_POINT ( 'NONE',  ( 0.8469861386668179337, -0.7068739681193977331, 2.826929786773349385 ) ) ;
#609=CARTESIAN_POINT ( 'NONE',  ( 1.648422021521518621, -0.9155690868286361361, 6.779860219333207816 ) ) ;
#611=CARTESIAN_POINT ( 'NONE',  ( 2.353452300571019506, -4.125511994252439862, 4.697179287168359529 ) ) ;
#614=CARTESIAN_POINT ( 'NONE',  ( -1.978267656359410154, -5.197669491525420682, 5.974740860598790171 ) ) ;
#622=CARTESIAN_POINT ( 'NONE',  ( 0.7540633504677742849, -2.239160642901089293, 2.155495695330191364 ) ) ;
#625=CARTESIAN_POINT ( 'NONE',  ( -0.6673090596498669758, -3.360839357098900138, 2.443133963569589895 ) ) ;
#626=CARTESIAN_POINT ( 'NONE',  ( 0.2435295127647320035, -5.004947479095229745, 2.350795284704489507 ) ) ;
#627=CARTESIAN_POINT ( 'NONE',  ( -2.543624461644929724, -1.703530012270459970, 5.457025951420040322 ) ) ;
#631=CARTESIAN_POINT ( 'NONE',  ( -2.353194804772640314, -5.524364406779660008, 4.731327187377240229 ) ) ;
#641=CARTESIAN_POINT ( 'NONE',  ( -0.5320716618283710675, -3.007674156414609890, 6.992519451207139802 ) ) ;
#643=CARTESIAN_POINT ( 'NONE',  ( 2.058670345754650022, -5.350847457627120107, 3.559656372813920111 ) ) ;
#645=CARTESIAN_POINT ( 'NONE',  ( -2.091095264232510242, -1.656953435693890198, 5.779845490516250628 ) ) ;
#647=CARTESIAN_POINT ( 'NONE',  ( 0.5133516189064986079, -4.152641158900696183, 6.687805814961351736 ) ) ;
#648=B_SPLINE_CURVE_WITH_KNOTS ( 'NONE', 3,
 ( #13687, #15087, #10621, #17733, #16359, #12289, #10909 ),
 .UNSPECIFIED., .F., .F.,
 ( 4, 1, 1, 1, 4 ),
 ( 0.000000000000000000, 0.3003308066897660278, 0.4325493167368040237, 0.5576349185195599301, 0.7853981633974479459 ),
 .UNSPECIFIED. ) ;
#652=CARTESIAN_POINT ( 'NONE',  ( 1.608484968265039949, -0.5211538081685300750, 3.106608516387050045 ) ) ;
#653=EDGE_CURVE ( 'NONE', #14665, #6595, #1073, .T. ) ;
#654=CARTESIAN_POINT ( 'NONE',  ( -1.695509042132779864, -0.2536016949152540834, 3.542446458728619518 ) ) ;
#655=CARTESIAN_POINT ( 'NONE',  ( 1.567709126316360058, -3.915917399657849796, 2.944712621036570166 ) ) ;
#661=CARTESIAN_POINT ( 'NONE',  ( -2.350542563031990273, -4.595118636378179744, 4.817027120179790067 ) ) ;
#663=CARTESIAN_POINT ( 'NONE',  ( 2.234315482767910144, -5.059745762711860273, 3.960850823455320580 ) ) ;
#665=CARTESIAN_POINT ( 'NONE',  ( -2.328217775191430139, -0.5180084745762719711, 5.043379051721170292 ) ) ;
#669=CARTESIAN_POINT ( 'NONE',  ( 0.3509990757148593321, -4.474836318576761229, 6.722795464567642654 ) ) ;
#670=CARTESIAN_POINT ( 'NONE',  ( -2.304156201936080617, -0.5002118644067795605, 6.016707707703351282 ) ) ;
#672=CARTESIAN_POINT ( 'NONE',  ( 1.128670402850170174, -0.4290254237288141370, 7.101865548313628373 ) ) ;
#674=CARTESIAN_POINT ( 'NONE',  ( -2.270487904532170198, -5.537711864406779760, 4.080813552109679776 ) ) ;
#679=CARTESIAN_POINT ( 'NONE',  ( 0.6890111762202997259, -3.799475958216412153, 2.137115435286760956 ) ) ;
#681=CARTESIAN_POINT ( 'NONE',  ( 2.237394498046680003, -2.336154672414219924, 5.429939413646329704 ) ) ;
#685=CARTESIAN_POINT ( 'NONE',  ( -1.985741519624380835, -3.104668185927728974, 4.178720363079513334 ) ) ;
#690=CARTESIAN_POINT ( 'NONE',  ( -0.1608173401625278554, -1.101875393134940984, 6.746714348835997299 ) ) ;
#694=CARTESIAN_POINT ( 'NONE',  ( -1.373536515609910191, -1.218316834576379737, 6.970795264502737787 ) ) ;
#699=CARTESIAN_POINT ( 'NONE',  ( 1.695509042132770761, -5.046398305084744962, 3.542446458728613301 ) ) ;
#705=CARTESIAN_POINT ( 'NONE',  ( -0.009452110982655708218, -0.5998079552954630467, 2.350000000000000089 ) ) ;
#707=CARTESIAN_POINT ( 'NONE',  ( -2.052786957354850728, -5.524364406779660897, 4.727327971967373976 ) ) ;
#708=CARTESIAN_POINT ( 'NONE',  ( 2.652303127816839190, -2.266289807549351387, 4.791661394135748431 ) ) ;
#710=CARTESIAN_POINT ( 'NONE',  ( 0.3832714063289482387, -2.914521003261450360, 7.326064873930673294 ) ) ;
#714=CARTESIAN_POINT ( 'NONE',  ( 0.8001898266890951072, -4.129352870612410520, 6.913242401714550844 ) ) ;
#717=CARTESIAN_POINT ( 'NONE',  ( 0.02098813186351079427, -2.169295778036230526, 2.046196467083000403 ) ) ;
#721=CARTESIAN_POINT ( 'NONE',  ( -2.316639661709700260, -1.819971453711900056, 4.285359956977770501 ) ) ;
#723=CARTESIAN_POINT ( 'NONE',  ( -1.000896394980330006, -5.470974576271190770, 6.829956240957379521 ) ) ;
#732=CARTESIAN_POINT ( 'NONE',  ( 1.962536940652990003, -2.704926408666860294, 5.998920491814760503 ) ) ;
#733=( BOUNDED_SURFACE ( )  B_SPLINE_SURFACE ( 3, 3, ( 
 ( #4152, #5646, #9810, #11289, #18030, #15467, #5376 ),
 ( #8513, #2776, #11014, #12683, #14163, #16663, #5817 ),
 ( #14519, #5913, #170, #10428, #1838, #1752, #17103 ),
 ( #14601, #14332, #3045, #15913, #11734, #10345, #7399 ),
 ( #13038, #13131, #11836, #14251, #13212, #1569, #8685 ),
 ( #5998, #1652, #16091, #8607, #360, #4427, #7214 ),
 ( #274, #3122, #4778, #1916, #10087, #8870, #7299 ) ),
 .UNSPECIFIED., .T., .F., .F. ) 
 B_SPLINE_SURFACE_WITH_KNOTS ( ( 4, 3, 4 ),
 ( 4, 1, 1, 1, 4 ),
 ( 0.000000000000000000, 3.141592653589790007, 6.283185307179590673 ),
 ( 0.000000000000000000, 0.3003308066897660278, 0.4325493167368040237, 0.5576349185195599301, 0.7853981633974479459 ),
 .UNSPECIFIED. ) 
 GEOMETRIC_REPRESENTATION_ITEM ( )  RATIONAL_B_SPLINE_SURFACE ( (
 ( 1.000000000000000000, 1.000000000000000000, 1.000000000000000000, 1.000000000000000000, 1.000000000000000000, 1.000000000000000000, 1.000000000000000000),
 ( 0.3333333333333329818, 0.3333333333333329818, 0.3333333333333329818, 0.3333333333333329818, 0.3333333333333329818, 0.3333333333333329818, 0.3333333333333329818),
 ( 0.3333333333333329818, 0.3333333333333329818, 0.3333333333333329818, 0.3333333333333329818, 0.3333333333333329818, 0.3333333333333329818, 0.3333333333333329818),
 ( 1.000000000000000000, 1.000000000000000000, 1.000000000000000000, 1.000000000000000000, 1.000000000000000000, 1.000000000000000000, 1.000000000000000000),
 ( 0.3333333333333329818, 0.3333333333333329818, 0.3333333333333329818, 0.3333333333333329818, 0.3333333333333329818, 0.3333333333333329818, 0.3333333333333329818),
 ( 0.3333333333333329818, 0.3333333333333329818, 0.3333333333333329818, 0.3333333333333329818, 0.3333333333333329818, 0.3333333333333329818, 0.3333333333333329818),
 ( 1.000000000000000000, 1.000000000000000000, 1.000000000000000000, 1.000000000000000000, 1.000000000000000000, 1.000000000000000000, 1.000000000000000000) ) ) 
 REPRESENTATION_ITEM ( '' )  SURFACE ( )  );
#735=CARTESIAN_POINT ( 'NONE',  ( -1.707817112497179934, -5.488771186440679628, 6.319218296629480314 ) ) ;
#737=CARTESIAN_POINT ( 'NONE',  ( 2.347833536521260367, -2.541908390648839777, 4.537447324629859224 ) ) ;
#738=CARTESIAN_POINT ( 'NONE',  ( 1.219286470748990103, -4.381683165423610582, 6.712979431025659416 ) ) ;
#739=CARTESIAN_POINT ( 'NONE',  ( 0.6217226704572607066, -1.307629111369559949, 6.656620240022977697 ) ) ;
#746=CARTESIAN_POINT ( 'NONE',  ( -2.137408332595969629, -3.450151633892079683, 3.714996798363980002 ) ) ;
#753=CARTESIAN_POINT ( 'NONE',  ( 2.043308330018790198, -5.099788135593220417, 5.867646457774659652 ) ) ;
#759=CARTESIAN_POINT ( 'NONE',  ( -0.5972539422561604638, -4.591277760018214416, 6.664227474374482263 ) ) ;
#762=CARTESIAN_POINT ( 'NONE',  ( -1.031876288691620625, -0.4690677966101705065, 7.145012538880312292 ) ) ;
#765=CARTESIAN_POINT ( 'NONE',  ( 1.248294325655350034, -0.02669491525423759934, 2.704938983774300088 ) ) ;
#772=CARTESIAN_POINT ( 'NONE',  ( -0.4005155088301870503, -1.125163681423229978, 7.019123328904779413 ) ) ;
#773=CARTESIAN_POINT ( 'NONE',  ( 1.791574935211219799, -5.408686440677969998, 6.226029630577610163 ) ) ;
#774=CARTESIAN_POINT ( 'NONE',  ( 2.652408070456659051, -0.6826862039457533005, 4.611427313555195084 ) ) ;
#777=CARTESIAN_POINT ( 'NONE',  ( 0.8429265834919229539, -3.523857375116919766, 2.502678798553439776 ) ) ;
#778=CARTESIAN_POINT ( 'NONE',  ( -1.835211330903778970, -4.707719201459645397, 6.617058440404012032 ) ) ;
#785=CARTESIAN_POINT ( 'NONE',  ( -0.7128755192781907057, -1.777235753495299608, 2.774718115017459130 ) ) ;
#789=CARTESIAN_POINT ( 'NONE',  ( -2.282375681463830297, -3.174533050792599731, 3.345793611865449435 ) ) ;
#792=CARTESIAN_POINT ( 'NONE',  ( 2.350542563031990273, -1.004881363621820123, 4.817027120179740329 ) ) ;
#794=CARTESIAN_POINT ( 'NONE',  ( 2.030998484741458832, -5.081991525423726230, 4.999543428097175557 ) ) ;
#801=CARTESIAN_POINT ( 'NONE',  ( -0.5664586606772434862, -5.286652542372874741, 2.726727161522279452 ) ) ;
#804=CARTESIAN_POINT ( 'NONE',  ( 1.071153154657499718, -2.545749267008810435, 7.128115444592616257 ) ) ;
#805=CARTESIAN_POINT ( 'NONE',  ( 0.2435295127647319202, -5.004947479095227969, 2.350795284704489507 ) ) ;
#806=CARTESIAN_POINT ( 'NONE',  ( 1.991177874369370882, -2.378890372630820149, 2.945484578117438801 ) ) ;
#810=CARTESIAN_POINT ( 'NONE',  ( -1.480680413335760059, -4.385524041783589233, 6.529298007719829933 ) ) ;
#815=CARTESIAN_POINT ( 'NONE',  ( 2.146130664537611032, -2.402178660919109365, 3.138834773724044958 ) ) ;
#820=CARTESIAN_POINT ( 'NONE',  ( 0.8570167067220200163, -0.3177966101694920664, 2.508190348879349774 ) ) ;
#821=CARTESIAN_POINT ( 'NONE',  ( -1.741913176380149864, -1.959701183441629802, 3.117443785062560035 ) ) ;
#822=CARTESIAN_POINT ( 'NONE',  ( -1.811729841638700211, -0.5580508474576270084, 3.197954009834299782 ) ) ;
#826=CARTESIAN_POINT ( 'NONE',  ( 0.4974685680287857514, -5.139830508474579673, 7.000224381598740386 ) ) ;
#833=CARTESIAN_POINT ( 'NONE',  ( 2.276802572547980130, -2.495331814072260013, 4.104251954998760610 ) ) ;
#835=CARTESIAN_POINT ( 'NONE',  ( -2.353194804772640314, -5.524364406779660008, 4.731327187377240229 ) ) ;
#838=CARTESIAN_POINT ( 'NONE',  ( 2.075124426334590044, -2.681638120378570189, 5.810227140144509583 ) ) ;
#842=CARTESIAN_POINT ( 'NONE',  ( -0.5133516189064535329, -1.447358841099289251, 6.687805814961367723 ) ) ;
#846=CARTESIAN_POINT ( 'NONE',  ( 1.668386990667991565, -0.4963805274437239623, 3.049705503900983938 ) ) ;
#849=CARTESIAN_POINT ( 'NONE',  ( -1.948278411993560111, -3.193980462720909852, 6.020210936496040333 ) ) ;
#857=CARTESIAN_POINT ( 'NONE',  ( 2.328217775191430139, -5.081991525423729783, 5.043379051721160522 ) ) ;
#860=CARTESIAN_POINT ( 'NONE',  ( -2.313035575219740014, -1.427911429170980018, 5.134294963419759661 ) ) ;
#863=CARTESIAN_POINT ( 'NONE',  ( 1.224086244040949900, -4.358394877135324030, 6.348185277745746369 ) ) ;
#864=CARTESIAN_POINT ( 'NONE',  ( 2.253200202764420013, -0.08898305084745811167, 5.379408587037500133 ) ) ;
#866=CARTESIAN_POINT ( 'NONE',  ( 2.318251751302029984, -0.3667372881355940306, 4.294764266798990704 ) ) ;
#868=CARTESIAN_POINT ( 'NONE',  ( 1.347262683220810553, -0.1245762711864410871, 6.986424775243341045 ) ) ;
#870=CARTESIAN_POINT ( 'NONE',  ( -2.306642602145299925, -5.515466101694909362, 5.166805192608490138 ) ) ;
#872=CARTESIAN_POINT ( 'NONE',  ( 1.914021115237029225, -0.8457042219637708191, 6.069404563272199127 ) ) ;
#873=CARTESIAN_POINT ( 'NONE',  ( 1.112838723655040107, -5.426483050847459744, 6.773667561836210105 ) ) ;
#874=EDGE_CURVE ( 'NONE', #7005, #8096, #1357, .T. ) ;
#875=CARTESIAN_POINT ( 'NONE',  ( -2.501774541437291610, -4.824160642901089702, 5.585572039315926496 ) ) ;
#880=CARTESIAN_POINT ( 'NONE',  ( 2.267872052190590182, -3.756740257999799937, 4.071110468860600129 ) ) ;
#882=CARTESIAN_POINT ( 'NONE',  ( 1.373536515609961484, -4.381683165423609694, 6.970795264502707589 ) ) ;
#885=CARTESIAN_POINT ( 'NONE',  ( 2.052909741356249373, -3.826605122864674247, 4.721527574705135066 ) ) ;
#888=CARTESIAN_POINT ( 'NONE',  ( 0.2220816246932099114, -1.055298816558370101, 6.740975647723836950 ) ) ;
#893=CARTESIAN_POINT ( 'NONE',  ( 1.503451935564949826, -2.499172690432241772, 6.886949009567407742 ) ) ;
#899=CARTESIAN_POINT ( 'NONE',  ( 1.940327948426050941, -5.090889830508485758, 5.370677689277660427 ) ) ;
#907=CARTESIAN_POINT ( 'NONE',  ( -0.3743405594629430344, -5.457627118644070130, 7.023440622744399953 ) ) ;
#908=CARTESIAN_POINT ( 'NONE',  ( -1.923406176634930853, -4.796950468210009255, 2.875176962145308934 ) ) ;
#913=CARTESIAN_POINT ( 'NONE',  ( 0.2023972492402060230, -3.453992510252060111, 2.355265251465770149 ) ) ;
#916=CARTESIAN_POINT ( 'NONE',  ( -2.121170185508219230, -1.936412895153350133, 3.105085978143999448 ) ) ;
#920=CARTESIAN_POINT ( 'NONE',  ( -1.003115764947269950, -1.493935417675869903, 6.828967930617589666 ) ) ;
#921=CARTESIAN_POINT ( 'NONE',  ( -0.002227590684729350255, -5.185305426092289949, 2.202374039106770098 ) ) ;
#922=CARTESIAN_POINT ( 'NONE',  ( -2.253200202764409799, -5.511016949152540256, 5.379408587037509903 ) ) ;
#930=CARTESIAN_POINT ( 'NONE',  ( 2.190084968185480374, -4.032358841099290103, 3.838447030292440054 ) ) ;
#932=CARTESIAN_POINT ( 'NONE',  ( -0.1565249325564300187, -5.453177966101690366, 7.048192310558509810 ) ) ;
#935=CARTESIAN_POINT ( 'NONE',  ( -0.09706517602693919000, -2.961097579838030125, 7.051451474958980725 ) ) ;
#937=CARTESIAN_POINT ( 'NONE',  ( 1.259207372045950457, -2.332313796054251487, 3.078488779929903441 ) ) ;
#939=CARTESIAN_POINT ( 'NONE',  ( -0.009452110982655715157, -0.5998079552954631577, 2.050000000000001155 ) ) ;
#941=CARTESIAN_POINT ( 'NONE',  ( 1.561564427405139899, -5.242163535134220176, 3.138435572594850065 ) ) ;
#950=CARTESIAN_POINT ( 'NONE',  ( 2.350067830300900162, -5.077542372881360677, 4.825253242917690422 ) ) ;
#954=CARTESIAN_POINT ( 'NONE',  ( -2.579602008086729459, -4.548542059801595094, 5.323511966907305215 ) ) ;
#956=CARTESIAN_POINT ( 'NONE',  ( -1.586727176531439909, -1.982989471729919906, 2.961885344765640138 ) ) ;
#958=CARTESIAN_POINT ( 'NONE',  ( 1.378221871957440170, -0.1201271186440679983, 6.607619368096269596 ) ) ;
#960=CARTESIAN_POINT ( 'NONE',  ( -2.508228811380011081, -0.2091101694915259990, 5.566973598334550744 ) ) ;
#963=CARTESIAN_POINT ( 'NONE',  ( -2.313035575219740014, -1.427911429170980240, 5.134294963419758773 ) ) ;
#964=CARTESIAN_POINT ( 'NONE',  ( -1.496290472746829803, -0.5672554343907050267, 2.872674968141029961 ) ) ;
#965=CARTESIAN_POINT ( 'NONE',  ( 2.051568858000881068, -0.5196681859277345605, 3.016498023208322277 ) ) ;
#967=CARTESIAN_POINT ( 'NONE',  ( -1.314185150718290895, -5.128627060139315574, 3.113044112970123400 ) ) ;
#969=CARTESIAN_POINT ( 'NONE',  ( 1.953802435660499048, -0.6128213390808875394, 4.069478085300975323 ) ) ;
#970=CARTESIAN_POINT ( 'NONE',  ( -2.652408070456659051, -4.917313796054240349, 4.611427313555255481 ) ) ;
#973=CARTESIAN_POINT ( 'NONE',  ( -1.978802102381380879, -1.843259742000191048, 4.152967933079680485 ) ) ;
#976=CARTESIAN_POINT ( 'NONE',  ( -0.3943683997330095781, -3.384127645387192018, 2.685210827922659860 ) ) ;
#980=CARTESIAN_POINT ( 'NONE',  ( -0.7982439214406890082, -0.1690677966101698793, 6.591424794228156081 ) ) ;
#981=CARTESIAN_POINT ( 'NONE',  ( 1.139503474074560874, -0.7471169921413568504, 2.982738323988489260 ) ) ;
#982=CARTESIAN_POINT ( 'NONE',  ( 2.327043743583509627, -2.382731248990799244, 5.975923629552606364 ) ) ;
#986=CARTESIAN_POINT ( 'NONE',  ( -0.5137283630188880235, -5.162076271186444743, 6.687652957477222770 ) ) ;
#993=CARTESIAN_POINT ( 'NONE',  ( 1.925796468768800063, -5.404237288135590234, 6.052706598917719560 ) ) ;
#994=CARTESIAN_POINT ( 'NONE',  ( -2.650521604678268694, -4.595118636378185073, 4.833599835830360014 ) ) ;
#996=CARTESIAN_POINT ( 'NONE',  ( -1.837442528958838750, -3.543304787045241433, 2.785079989718828752 ) ) ;
#998=CARTESIAN_POINT ( 'NONE',  ( -1.444955263746759977, -3.267686203945750378, 2.842353646881510265 ) ) ;
#1002=CARTESIAN_POINT ( 'NONE',  ( 2.567863625471588751, -2.495331814072259569, 4.029783546918046078 ) ) ;
#1007=CARTESIAN_POINT ( 'NONE',  ( 2.203023580853990193, -0.3578389830508479919, 3.872235369154280349 ) ) ;
#1009=CARTESIAN_POINT ( 'NONE',  ( -1.552749016687749783, -1.563800282540730002, 6.468535037441760061 ) ) ;
#1010=CARTESIAN_POINT ( 'NONE',  ( -1.641808337277740115, -0.4868644067796619734, 6.386111670537629514 ) ) ;
#1012=CARTESIAN_POINT ( 'NONE',  ( 2.171642826483958899, -5.404237288135596451, 6.225392547715717484 ) ) ;
#1015=CARTESIAN_POINT ( 'NONE',  ( 2.224278379903029457, -5.090889830508479541, 5.468825643806100700 ) ) ;
#1019=CARTESIAN_POINT ( 'NONE',  ( -0.04278372834682089842, -3.729611093351540063, 2.346934926511239805 ) ) ;
#1021=CARTESIAN_POINT ( 'NONE',  ( -0.07299321914061848715, -5.598516949152539723, 2.350000000000000089 ) ) ;
#1025=CARTESIAN_POINT ( 'NONE',  ( 1.444955263746720009, -2.332313796054249710, 2.842353646881480511 ) ) ;
#1026=CARTESIAN_POINT ( 'NONE',  ( -1.209303714320900225, -4.865515740159330527, 2.662663894020050659 ) ) ;
#1027=CARTESIAN_POINT ( 'NONE',  ( 1.893291846171430981, -2.658349832090279197, 5.493944474033856551 ) ) ;
#1030=CARTESIAN_POINT ( 'NONE',  ( 0.6493550500446280127, -0.3133474576271190193, 2.437955526623099889 ) ) ;
#1034=CARTESIAN_POINT ( 'NONE',  ( -1.820241257191459905, -5.080331814072259533, 3.208199930689799917 ) ) ;
#1041=CARTESIAN_POINT ( 'NONE',  ( -1.750316316486840051, -5.259957627118650336, 3.126818518378589928 ) ) ;
#1044=ORIENTED_EDGE ( 'NONE', *, *, #12721, .F. ) ;
#1045=CARTESIAN_POINT ( 'NONE',  ( 2.325590009395039903, -0.7292627805223299564, 5.061077271074021056 ) ) ;
#1047=CARTESIAN_POINT ( 'NONE',  ( 2.291237445532070094, -0.9350164987569499209, 4.162434510291790346 ) ) ;
#1048=CARTESIAN_POINT ( 'NONE',  ( -1.254903241568450900, -0.1735169491525429541, 7.038391080368498365 ) ) ;
#1051=CARTESIAN_POINT ( 'NONE',  ( 2.306642602145299925, -0.3845338983050849979, 5.166805192608480368 ) ) ;
#1052=CARTESIAN_POINT ( 'NONE',  ( -0.9150601050661559821, -0.4690677966101700069, 6.868218666554230190 ) ) ;
#1054=CARTESIAN_POINT ( 'NONE',  ( -2.416676968769249090, -0.2046610169491529518, 5.796598111919839980 ) ) ;
#1056=CARTESIAN_POINT ( 'NONE',  ( 2.281778813005790330, -0.7525510688106178403, 5.276394947932119273 ) ) ;
#1057=CARTESIAN_POINT ( 'NONE',  ( -0.4617942143426889690, -0.5906145504024210569, 2.383143958488499692 ) ) ;
#1058=CARTESIAN_POINT ( 'NONE',  ( 2.293791554891360551, -0.8224159336754829353, 6.034778631725497000 ) ) ;
#1061=CARTESIAN_POINT ( 'NONE',  ( 1.458615186838411626, -0.4963798976394455664, 3.259477383973563125 ) ) ;
#1062=CARTESIAN_POINT ( 'NONE',  ( 1.771358649600380142, -4.335106588847043696, 6.676209054601206283 ) ) ;
#1065=CARTESIAN_POINT ( 'NONE',  ( 1.998374131852729940, -0.9350164987569505870, 4.229465546630494011 ) ) ;
#1071=CARTESIAN_POINT ( 'NONE',  ( 0.1910247150515120007, -0.3044491525423730915, 2.655937705488500722 ) ) ;
#1073=CIRCLE ( 'NONE', #17894, 0.1499999999999999944 ) ;
#1074=CARTESIAN_POINT ( 'NONE',  ( -2.065789008932981119, -2.871785303044851023, 6.366022047745341084 ) ) ;
#1077=CARTESIAN_POINT ( 'NONE',  ( -0.06367493584607197832, -5.298516949152545230, 2.649999999999998579 ) ) ;
#1080=CARTESIAN_POINT ( 'NONE',  ( 2.286166334984490067, -5.386440677966100488, 5.258525443163859947 ) ) ;
#1083=CARTESIAN_POINT ( 'NONE',  ( 2.234315482767910144, -5.359745762711869865, 3.960850823455320580 ) ) ;
#1084=CARTESIAN_POINT ( 'NONE',  ( -2.174104834890490778, -4.455388906648449776, 6.221966445066275497 ) ) ;
#1094=CARTESIAN_POINT ( 'NONE',  ( -2.332582362116870200, -0.5313559322033900578, 4.387643303570819775 ) ) ;
#1095=CARTESIAN_POINT ( 'NONE',  ( 0.9170541073686970801, -1.284340823081270067, 6.867431071947180499 ) ) ;
#1096=CARTESIAN_POINT ( 'NONE',  ( -2.351526912647309953, -0.5269067796610169552, 4.606040641882809261 ) ) ;
#1098=CARTESIAN_POINT ( 'NONE',  ( -2.087380238839969593, -5.493220338983046069, 6.338810156469112833 ) ) ;
#1103=CARTESIAN_POINT ( 'NONE',  ( 0.004026115436748929806, -0.3861894795279390280, 2.487698411375030005 ) ) ;
#1109=CARTESIAN_POINT ( 'NONE',  ( 2.102728310581320148, -4.241953435693879726, 5.757014351541050345 ) ) ;
#1111=CARTESIAN_POINT ( 'NONE',  ( -0.4360591020458099987, -5.591101694915249887, 2.387347919655840034 ) ) ;
#1117=CARTESIAN_POINT ( 'NONE',  ( 1.687170344132030042, -2.751502985243429844, 6.340793075730549511 ) ) ;
#1119=CARTESIAN_POINT ( 'NONE',  ( -1.722199153441400066, -5.095857339597789526, 3.099360556065549943 ) ) ;
#1120=CARTESIAN_POINT ( 'NONE',  ( -1.520647680314179517, -1.959701183441630024, 3.320676805464663151 ) ) ;
#1123=CARTESIAN_POINT ( 'NONE',  ( -1.217041937262000051, -0.2742238837839079402, 2.666998181419179659 ) ) ;
#1133=CARTESIAN_POINT ( 'NONE',  ( 1.562863241354470523, -5.108686440677975504, 6.031217337312382298 ) ) ;
#1138=CARTESIAN_POINT ( 'NONE',  ( -2.185196738168510233, -4.758136654396205145, 3.194002352996703653 ) ) ;
#1141=CARTESIAN_POINT ( 'NONE',  ( -2.267872052190610166, -1.843259742000189938, 4.071110468860649867 ) ) ;
#1142=CARTESIAN_POINT ( 'NONE',  ( -0.7998959936908373036, -0.1646186440677970542, 7.230419212249866945 ) ) ;
#1144=CARTESIAN_POINT ( 'NONE',  ( 1.378221871957440170, -0.4201271186440679872, 6.607619368096269596 ) ) ;
#1146=CARTESIAN_POINT ( 'NONE',  ( -0.07064654565474801085, -0.1512711864406789675, 7.352897294663512717 ) ) ;
#1150=CARTESIAN_POINT ( 'NONE',  ( -0.9719602541832296216, -2.755343861603410271, 6.843370931913549171 ) ) ;
#1152=CARTESIAN_POINT ( 'NONE',  ( -2.345900685764729765, -5.528813559322030002, 4.512231114381339836 ) ) ;
#1153=CARTESIAN_POINT ( 'NONE',  ( -2.589817782457070727, -4.963890372630814340, 4.120381550730010112 ) ) ;
#1156=CARTESIAN_POINT ( 'NONE',  ( -1.294880990849879732, -4.829629811528119987, 3.097365952343163364 ) ) ;
#1157=CARTESIAN_POINT ( 'NONE',  ( -1.704669856830349994, -4.796950468210010143, 3.080704711052660194 ) ) ;
#1158=CARTESIAN_POINT ( 'NONE',  ( 0.6919952253610313075, -4.451548030288480895, 7.262080463427998289 ) ) ;
#1163=CARTESIAN_POINT ( 'NONE',  ( 1.436030008293490701, -1.191187669928120529, 6.167214932417436124 ) ) ;
#1168=CARTESIAN_POINT ( 'NONE',  ( 0.7476103186298468373, -0.3177966101694921219, 2.787995836256459636 ) ) ;
#1169=CARTESIAN_POINT ( 'NONE',  ( 2.049607015837390911, -2.429307825567371459, 6.385889905549011480 ) ) ;
#1171=CARTESIAN_POINT ( 'NONE',  ( -0.9138909625329535436, -4.911779243796845051, 2.204775695797560164 ) ) ;
#1172=CARTESIAN_POINT ( 'NONE',  ( -0.1365430262726299304, -5.153177966101685215, 6.748423079423377047 ) ) ;
#1179=CARTESIAN_POINT ( 'NONE',  ( -1.378221871957430178, -5.479872881355929870, 6.607619368096279366 ) ) ;
#1180=CARTESIAN_POINT ( 'NONE',  ( 2.461935615161780611, -3.919758276017824006, 5.690952430644305338 ) ) ;
#1181=CARTESIAN_POINT ( 'NONE',  ( 2.607432201095279733, -4.078935417675873865, 4.205620581240154365 ) ) ;
#1183=CARTESIAN_POINT ( 'NONE',  ( 1.990095963740240004, -0.7525510688106187285, 5.204400533041760646 ) ) ;
#1186=CIRCLE ( 'NONE', #12134, 0.1499999999999999667 ) ;
#1188=CARTESIAN_POINT ( 'NONE',  ( 1.549742865090599997, -0.4156779661016959948, 6.471102547561449647 ) ) ;
#1189=CARTESIAN_POINT ( 'NONE',  ( 1.991984774470479946, -3.985782264522710339, 3.446707398186009907 ) ) ;
#1192=CARTESIAN_POINT ( 'NONE',  ( -2.645377369053839356, -5.528813559322025561, 4.488260618344918740 ) ) ;
#1196=CARTESIAN_POINT ( 'NONE',  ( -2.306642602145299925, -5.215466101694908652, 5.166805192608489250 ) ) ;
#1201=CARTESIAN_POINT ( 'NONE',  ( 1.724579595320000047, -3.939205687946140344, 3.098572228637889836 ) ) ;
#1203=CARTESIAN_POINT ( 'NONE',  ( 0.5070585469427659753, -5.011796459788054214, 2.696565570857651473 ) ) ;
#1206=CARTESIAN_POINT ( 'NONE',  ( -2.036228139452650243, -3.473439922180369788, 3.519948877554409883 ) ) ;
#1208=CARTESIAN_POINT ( 'NONE',  ( -1.423520578776781509, -3.543304787045241433, 3.220645071516951230 ) ) ;
#1211=CARTESIAN_POINT ( 'NONE',  ( -0.3897427956305680175, -0.2909039927201511055, 2.676097687607990938 ) ) ;
#1221=CARTESIAN_POINT ( 'NONE',  ( 1.679950111053631900, -5.104237288135595740, 5.880020650119711867 ) ) ;
#1223=CARTESIAN_POINT ( 'NONE',  ( 0.7785957873161482024, -1.940253771513320125, 2.162894899107371316 ) ) ;
#1227=CARTESIAN_POINT ( 'NONE',  ( -0.8298945877350979439, -5.211074464177370302, 2.494426474263899962 ) ) ;
#1229=CARTESIAN_POINT ( 'NONE',  ( -2.353343516942199898, -1.773394877135329839, 4.722803042560189901 ) ) ;
#1230=CARTESIAN_POINT ( 'NONE',  ( -2.625437065641401446, -0.2180084745762719822, 5.087214675345155257 ) ) ;
#1233=CARTESIAN_POINT ( 'NONE',  ( 1.889104232906359870, -0.3444915254237289615, 3.296507079072520163 ) ) ;
#1234=CARTESIAN_POINT ( 'NONE',  ( -1.300961508564169922, -0.4779661016949160457, 6.661123742937279602 ) ) ;
#1237=CARTESIAN_POINT ( 'NONE',  ( -1.661700935788390066, -0.2625000000000000111, 3.038299064211610112 ) ) ;
#1238=CARTESIAN_POINT ( 'NONE',  ( 2.291237445532070094, -0.9350164987569499209, 4.162434510291790346 ) ) ;
#1240=EDGE_CURVE ( 'NONE', #15103, #7787, #232, .T. ) ;
#1242=CARTESIAN_POINT ( 'NONE',  ( 0.3159454637157338985, -2.615614131873679415, 7.032150113402087399 ) ) ;
#1244=CARTESIAN_POINT ( 'NONE',  ( 1.254903241568450900, -5.426483050847465073, 7.038391080368498365 ) ) ;
#1246=CARTESIAN_POINT ( 'NONE',  ( 1.928817277882869829, -1.144611093351550091, 6.048484184565929844 ) ) ;
#1247=CARTESIAN_POINT ( 'NONE',  ( -0.06276132972181580616, -4.222506023765570049, 7.052616990284530374 ) ) ;
#1252=CARTESIAN_POINT ( 'NONE',  ( 1.485933537025759366, -0.8030495317899833951, 3.286232459959989249 ) ) ;
#1256=CARTESIAN_POINT ( 'NONE',  ( 0.9222751404130974384, -0.3222457627118649470, 2.865854510788131027 ) ) ;
#1259=CARTESIAN_POINT ( 'NONE',  ( -2.022685914314908739, -4.432100618360157007, 6.418096442297106741 ) ) ;
#1260=CARTESIAN_POINT ( 'NONE',  ( -0.1881942810071039751, -5.280843314568230085, 2.350674491507239949 ) ) ;
#1261=CARTESIAN_POINT ( 'NONE',  ( -0.7476103186298618253, -5.282203389830510076, 2.787995836256459636 ) ) ;
#1263=CARTESIAN_POINT ( 'NONE',  ( 1.707817112497189704, -0.1112288135593230004, 6.319218296629480314 ) ) ;
#1264=DIRECTION ( 'NONE',  ( 0.000000000000000000, -1.000000000000000000, 0.000000000000000000 ) ) ;
#1268=CARTESIAN_POINT ( 'NONE',  ( -0.4360591020458099987, -5.591101694915249887, 2.387347919655840034 ) ) ;
#1269=CARTESIAN_POINT ( 'NONE',  ( -2.584100759211431786, -4.664983501243040287, 4.095403473953163953 ) ) ;
#1270=CARTESIAN_POINT ( 'NONE',  ( 2.549960444629811640, -4.055647129387581984, 3.964598460822105874 ) ) ;
#1278=CARTESIAN_POINT ( 'NONE',  ( 0.2469343877495150108, -0.3044491525423730915, 2.057675570509529539 ) ) ;
#1279=CARTESIAN_POINT ( 'NONE',  ( -2.159566522375440112, -3.240557039297490061, 5.635424033751089468 ) ) ;
#1282=CARTESIAN_POINT ( 'NONE',  ( 2.630358833876468960, -5.068644067796615360, 4.347767980622404771 ) ) ;
#1285=CARTESIAN_POINT ( 'NONE',  ( -3.760880495917719358E-15, -5.299999999999999822, 2.350000000000000089 ) ) ;
#1289=CARTESIAN_POINT ( 'NONE',  ( -2.283153923255329953, -3.403575057315510133, 4.129076318403500423 ) ) ;
#1291=CARTESIAN_POINT ( 'NONE',  ( 0.8611469534735395337, -5.020626044399135068, 2.833474624362548600 ) ) ;
#1294=CARTESIAN_POINT ( 'NONE',  ( -1.092567884283820012, -4.637854336594780413, 6.784476218553590066 ) ) ;
#1296=CARTESIAN_POINT ( 'NONE',  ( 1.627161714697888728, -3.962493976234419790, 3.448102801005814122 ) ) ;
#1306=CARTESIAN_POINT ( 'NONE',  ( 1.289141334274990447, -5.117584745762705722, 6.297747079672416426 ) ) ;
#1312=ADVANCED_FACE ( 'NONE', ( #17507 ), #4030, .T. ) ;
#1313=CARTESIAN_POINT ( 'NONE',  ( 2.331386066015260106, -0.9583047870452390260, 4.378465089518139841 ) ) ;
#1314=CARTESIAN_POINT ( 'NONE',  ( 0.2739924515130530702, -2.615614131873680748, 6.734657214162127481 ) ) ;
#1315=CARTESIAN_POINT ( 'NONE',  ( 1.088937603231269646, -0.02669491525423760975, 2.959627624143540192 ) ) ;
#1317=CARTESIAN_POINT ( 'NONE',  ( -2.293398556041709835, -0.5358050847457630494, 4.171956209133480975 ) ) ;
#1320=CARTESIAN_POINT ( 'NONE',  ( 1.549742865090599997, -0.1156779661016950067, 6.471102547561449647 ) ) ;
#1325=CARTESIAN_POINT ( 'NONE',  ( 2.137408332595948757, -2.149848366107911080, 3.714996798363940922 ) ) ;
#1326=CARTESIAN_POINT ( 'NONE',  ( 2.191755591049679541, -5.346398305084745672, 3.203650300307709475 ) ) ;
#1330=CARTESIAN_POINT ( 'NONE',  ( -0.4339619423229766348, -0.4601694915254239682, 6.706578715862737461 ) ) ;
#1335=EDGE_CURVE ( 'NONE', #7787, #10555, #11657, .T. ) ;
#1336=CARTESIAN_POINT ( 'NONE',  ( 1.440522616026430391, -0.7952867690272208412, 3.241384813161591438 ) ) ;
#1341=CARTESIAN_POINT ( 'NONE',  ( 2.653777292528160192, -3.826605122864674247, 4.724078510415155030 ) ) ;
#1345=CARTESIAN_POINT ( 'NONE',  ( -1.042222075699109407, -5.175423728813555613, 6.468743694056166227 ) ) ;
#1353=CARTESIAN_POINT ( 'NONE',  ( -2.192143888961709752, -1.381334852594400031, 5.556300681753639559 ) ) ;
#1356=CARTESIAN_POINT ( 'NONE',  ( 1.703239418290648732, -0.5429564742160235546, 3.553755118148703929 ) ) ;
#1357=CIRCLE ( 'NONE', #17589, 0.1499999999999999667 ) ;
#1361=CARTESIAN_POINT ( 'NONE',  ( -0.2812789908084309953, -0.4557203389830509765, 7.036533610117280624 ) ) ;
#1362=CARTESIAN_POINT ( 'NONE',  ( 1.687170344132030042, -2.751502985243429844, 6.340793075730549511 ) ) ;
#1364=CARTESIAN_POINT ( 'NONE',  ( 2.304156201936080617, -5.099788135593215976, 6.016707707703351282 ) ) ;
#1373=CARTESIAN_POINT ( 'NONE',  ( 0.5606293434988925961, -1.330917399657850497, 7.293994686233932434 ) ) ;
#1379=CARTESIAN_POINT ( 'NONE',  ( -1.465095039565370127, -3.566593075333519991, 2.858195935359880480 ) ) ;
#1381=CARTESIAN_POINT ( 'NONE',  ( 1.971820545011360171, -4.055647129387581984, 4.128313389260194199 ) ) ;
#1388=CARTESIAN_POINT ( 'NONE',  ( -1.661700935788390066, -0.5625000000000000000, 3.038299064211610112 ) ) ;
#1398=CARTESIAN_POINT ( 'NONE',  ( 2.050059171113549183, -5.077542372881359789, 4.809263467226075228 ) ) ;
#1399=CARTESIAN_POINT ( 'NONE',  ( 0.04661003995938393929, -1.870388906648449812, 2.046522810126899294 ) ) ;
#1408=CARTESIAN_POINT ( 'NONE',  ( 0.7678268402137939930, -2.867944426684879922, 6.924676972266129660 ) ) ;
#1411=CARTESIAN_POINT ( 'NONE',  ( 1.238036348455360258, -3.593722239981790523, 3.062267469172269330 ) ) ;
#1413=CARTESIAN_POINT ( 'NONE',  ( 2.012177589105479392, -0.08453389830508521718, 5.107213040360584877 ) ) ;
#1419=CARTESIAN_POINT ( 'NONE',  ( -2.155845792290839835, -0.2447033898305089883, 3.756158857535780271 ) ) ;
#1421=CARTESIAN_POINT ( 'NONE',  ( 1.265407828724300021, -2.309025507765960050, 2.715689360385540319 ) ) ;
#1425=CARTESIAN_POINT ( 'NONE',  ( 2.036228139452629371, -2.126560077819630301, 3.519948877554369915 ) ) ;
#1427=CARTESIAN_POINT ( 'NONE',  ( 2.508228811380011081, -5.390889830508485581, 5.566973598334535644 ) ) ;
#1431=CARTESIAN_POINT ( 'NONE',  ( 0.2189795514005130062, -0.3044491525423729805, 2.356806637999009801 ) ) ;
#1437=CARTESIAN_POINT ( 'NONE',  ( -1.583713126240711588, -3.170692174432623744, 6.006428174987420654 ) ) ;
#1447=CARTESIAN_POINT ( 'NONE',  ( 1.661700935788380074, -5.337500000000000355, 3.038299064211610112 ) ) ;
#1459=CARTESIAN_POINT ( 'NONE',  ( -2.190084968185500358, -1.567641158900710208, 3.838447030292489792 ) ) ;
#1461=CARTESIAN_POINT ( 'NONE',  ( -1.912899118714301183, -1.381334852594401363, 5.445465495009755408 ) ) ;
#1466=CARTESIAN_POINT ( 'NONE',  ( -2.155845792290839835, -0.5447033898305089217, 3.756158857535780271 ) ) ;
#1468=CARTESIAN_POINT ( 'NONE',  ( 0.3413183941262679655, -2.914521003261450360, 7.028571974690709823 ) ) ;
#1471=CARTESIAN_POINT ( 'NONE',  ( 2.043014502273419186, -5.041949152542365198, 3.006203457898239062 ) ) ;
#1475=CARTESIAN_POINT ( 'NONE',  ( -2.340070819011249803, -5.219915254237289304, 4.950151441910548122 ) ) ;
#1480=CARTESIAN_POINT ( 'NONE',  ( -1.752195476665039831, -1.563800282540731779, 6.693219682964347328 ) ) ;
#1482=CARTESIAN_POINT ( 'NONE',  ( 1.873832970144350130, -5.337500000000000355, 2.826167029855650270 ) ) ;
#1485=CARTESIAN_POINT ( 'NONE',  ( 1.092567884283869972, -0.9621456634052130141, 6.784476218553570526 ) ) ;
#1487=CARTESIAN_POINT ( 'NONE',  ( -1.781655196750479897, -3.520016498756949996, 3.162323035427820450 ) ) ;
#1489=CARTESIAN_POINT ( 'NONE',  ( -1.777111910197670008, -3.473439922180372452, 3.672004328189223621 ) ) ;
#1502=CARTESIAN_POINT ( 'NONE',  ( 1.580445181003960586, -5.041949152542365198, 3.389704561770334301 ) ) ;
#1503=CARTESIAN_POINT ( 'NONE',  ( 2.502804106625939440, -2.173136654396201184, 3.817341913956370458 ) ) ;
#1511=CARTESIAN_POINT ( 'NONE',  ( 2.347833536521260367, -2.541908390648839777, 4.537447324629859224 ) ) ;
#1512=CARTESIAN_POINT ( 'NONE',  ( -1.333132471082830506, -2.825208726468270370, 6.261300629978947541 ) ) ;
#1513=CARTESIAN_POINT ( 'NONE',  ( 1.622657008870240762E-16, -3.053113317719175556E-16, 2.649999999999998579 ) ) ;
#1519=CARTESIAN_POINT ( 'NONE',  ( -2.143090896833110381, -0.2046610169491530073, 5.672454929438350391 ) ) ;
#1520=CARTESIAN_POINT ( 'NONE',  ( -1.710920205120030069, -1.587088570829020107, 6.316012914303580139 ) ) ;
#1524=CARTESIAN_POINT ( 'NONE',  ( -2.352760675243210198, -3.034803321062869319, 4.757121734156080528 ) ) ;
#1527=CARTESIAN_POINT ( 'NONE',  ( -2.645377369053839356, -5.528813559322025561, 4.488260618344918740 ) ) ;
#1530=CARTESIAN_POINT ( 'NONE',  ( 1.057242234132090175, -0.3222457627118650025, 2.597442975781520058 ) ) ;
#1534=CARTESIAN_POINT ( 'NONE',  ( 0.6713553523423281266, -2.867944426684881254, 6.640150466718861999 ) ) ;
#1537=CARTESIAN_POINT ( 'NONE',  ( -0.1881942810071039751, -5.280843314568230085, 2.350674491507239949 ) ) ;
#1541=CARTESIAN_POINT ( 'NONE',  ( 0.005141112625548329915, -0.3685177182334790080, 2.221989741495070003 ) ) ;
#1542=CARTESIAN_POINT ( 'NONE',  ( -1.980638384804660257, -5.537711864406785978, 4.159858630563765480 ) ) ;
#1543=CARTESIAN_POINT ( 'NONE',  ( 1.889104232906358982, -0.04449152542372910440, 3.296507079072520607 ) ) ;
#1544=CARTESIAN_POINT ( 'NONE',  ( 1.477796163681079911, -5.417584745762709986, 6.531563725478140015 ) ) ;
#1549=CARTESIAN_POINT ( 'NONE',  ( -0.8242394280876599311, -1.171740257999809964, 6.904399023015030501 ) ) ;
#1551=CARTESIAN_POINT ( 'NONE',  ( -1.217499609005920025, -1.707370888630439065, 3.046943272389440960 ) ) ;
#1557=CARTESIAN_POINT ( 'NONE',  ( 2.087380238839969593, -0.4067796610169500116, 6.338810156469096846 ) ) ;
#1558=CARTESIAN_POINT ( 'NONE',  ( 1.214457691475989920, -3.869340823081270031, 2.684103622926340194 ) ) ;
#1561=CARTESIAN_POINT ( 'NONE',  ( -2.268288188848061715, -5.251059322033895249, 3.322421079292323665 ) ) ;
#1567=CARTESIAN_POINT ( 'NONE',  ( -2.218077401483159683, -4.824160642901089702, 5.486688202856539576 ) ) ;
#1569=CARTESIAN_POINT ( 'NONE',  ( 1.349044826018420906, -0.4774152569121725143, 3.148480103883603221 ) ) ;
#1572=CARTESIAN_POINT ( 'NONE',  ( -2.337178851518210365, -3.011515032774580103, 4.976298214796809560 ) ) ;
#1575=CARTESIAN_POINT ( 'NONE',  ( 0.1768565782245979934, -3.752899381639830168, 2.353200596935780098 ) ) ;
#1579=CARTESIAN_POINT ( 'NONE',  ( 2.018065005288410152, -4.172088570829024512, 5.077247235985069551 ) ) ;
#1592=CARTESIAN_POINT ( 'NONE',  ( -1.489797906646480596, -5.488771186440680516, 6.112509577910826941 ) ) ;
#1597=FACE_OUTER_BOUND ( 'NONE', #2516, .T. ) ;
#1601=CARTESIAN_POINT ( 'NONE',  ( -1.044181395669830259, -2.052854336594790219, 2.590869634085910089 ) ) ;
#1602=CARTESIAN_POINT ( 'NONE',  ( -0.7616804549307533145, -3.337551068810613142, 2.793499350326739350 ) ) ;
#1603=CARTESIAN_POINT ( 'NONE',  ( -1.661700935788390066, -0.2625000000000000111, 3.038299064211610112 ) ) ;
#1607=CARTESIAN_POINT ( 'NONE',  ( 1.764807890102179977, -2.378890372630820149, 3.143016121304719857 ) ) ;
#1612=CARTESIAN_POINT ( 'NONE',  ( 1.003115764947319244, -4.106064582324130185, 6.828967930617569237 ) ) ;
#1614=CARTESIAN_POINT ( 'NONE',  ( -1.428515267734880023, -5.568855932203390147, 2.829745655876930055 ) ) ;
#1616=CARTESIAN_POINT ( 'NONE',  ( 1.042222075699120287, -0.4245762711864407013, 6.468743694056166227 ) ) ;
#1622=CARTESIAN_POINT ( 'NONE',  ( -0.9976707306414490661, -3.077539021279473097, 6.494311833503151554 ) ) ;
#1628=CARTESIAN_POINT ( 'NONE',  ( -1.901882987994748975, -5.506567796610171150, 5.472995608211450147 ) ) ;
#1630=CARTESIAN_POINT ( 'NONE',  ( -1.300961508564169700, -0.1779661016949160290, 6.661123742937278713 ) ) ;
#1634=CARTESIAN_POINT ( 'NONE',  ( -1.026235786675429917, -1.195028546288090077, 6.817920158464570335 ) ) ;
#1637=CARTESIAN_POINT ( 'NONE',  ( 1.555285212483259683, -2.079983501243050981, 3.359854578615069087 ) ) ;
#1640=CARTESIAN_POINT ( 'NONE',  ( -2.191755591049691532, -0.5536016949152540167, 3.203650300307721466 ) ) ;
#1641=CARTESIAN_POINT ( 'NONE',  ( 2.100188519621589922, -4.009070552810999999, 3.637948273607370275 ) ) ;
#1644=CARTESIAN_POINT ( 'NONE',  ( -0.9664230948142090716, -5.282203389830510076, 2.228384861502259895 ) ) ;
#1647=CARTESIAN_POINT ( 'NONE',  ( -1.248294325655369796, -5.273305084745759430, 2.704938983774311190 ) ) ;
#1649=CARTESIAN_POINT ( 'NONE',  ( 1.652654650382400003, -0.7952867690272209522, 3.029252778805629820 ) ) ;
#1651=CARTESIAN_POINT ( 'NONE',  ( 2.418933091173299577, -1.098034516774970770, 5.791730916219126613 ) ) ;
#1652=CARTESIAN_POINT ( 'NONE',  ( 0.1953673232040119001, -0.6247245358507567126, 2.648920247487680513 ) ) ;
#1654=CARTESIAN_POINT ( 'NONE',  ( -0.7678268402137429227, -2.732055573315119723, 6.924676972266150088 ) ) ;
#1655=CARTESIAN_POINT ( 'NONE',  ( 1.873832970144350130, -5.037500000000000533, 2.826167029855650270 ) ) ;
#1656=CARTESIAN_POINT ( 'NONE',  ( -2.380466601827099016, -1.889836318576769036, 3.526759849567179916 ) ) ;
#1659=CARTESIAN_POINT ( 'NONE',  ( -0.9516466452860307124, -4.637854336594775084, 6.519140045500596337 ) ) ;
#1672=CARTESIAN_POINT ( 'NONE',  ( 2.051331987628511211, -5.373093220338980736, 4.618035453557344461 ) ) ;
#1675=CARTESIAN_POINT ( 'NONE',  ( -1.720450724489941852, -2.825208726468270370, 6.720683794561613134 ) ) ;
#1677=CARTESIAN_POINT ( 'NONE',  ( -0.009452110982656913851, -5.299807955295455564, 2.050000000000001155 ) ) ;
#1682=CARTESIAN_POINT ( 'NONE',  ( -2.237394498046660019, -3.263845327585780165, 5.429939413646380331 ) ) ;
#1683=CARTESIAN_POINT ( 'NONE',  ( -0.8014931112106958855, -4.315659176918716255, 6.590108630558016323 ) ) ;
#1684=CARTESIAN_POINT ( 'NONE',  ( -2.351526912647309953, -0.2269067796610169940, 4.606040641882809261 ) ) ;
#1688=CARTESIAN_POINT ( 'NONE',  ( 2.329383452786330189, -1.028169651910100013, 5.035735636132829818 ) ) ;
#1690=CARTESIAN_POINT ( 'NONE',  ( 2.556942001999820580, -3.756740257999804378, 3.989253004641562406 ) ) ;
#1691=CARTESIAN_POINT ( 'NONE',  ( 1.846259792136599076, -0.05338983050847485173, 3.802221692020924415 ) ) ;
#1692=CARTESIAN_POINT ( 'NONE',  ( -1.741913176380149864, -1.959701183441629802, 3.117443785062560035 ) ) ;
#1697=CARTESIAN_POINT ( 'NONE',  ( -0.7109160811435618621, -4.292370888630430592, 6.943511536198419876 ) ) ;
#1699=CARTESIAN_POINT ( 'NONE',  ( -2.087380238839969593, -5.193220338983044471, 6.338810156469112833 ) ) ;
#1703=CARTESIAN_POINT ( 'NONE',  ( 2.041338374031088865, -0.3800847457627119508, 4.918217215283659627 ) ) ;
#1708=CARTESIAN_POINT ( 'NONE',  ( 1.538437905834991515, -2.378890372630820149, 3.340547664492009350 ) ) ;
#1715=CARTESIAN_POINT ( 'NONE',  ( 1.647523294046493447, -5.038055510066682174, 3.052476705953498737 ) ) ;
#1721=CARTESIAN_POINT ( 'NONE',  ( 0.3743405594629509725, -0.1423728813559329565, 7.023440622744399953 ) ) ;
#1722=CARTESIAN_POINT ( 'NONE',  ( -1.685497504775380850, -0.2673043920988010802, 2.637581209070348987 ) ) ;
#1723=CARTESIAN_POINT ( 'NONE',  ( 2.471388659209138972, -4.218665147405589622, 5.667135868497455320 ) ) ;
#1728=CARTESIAN_POINT ( 'NONE',  ( 0.6918414964981909332, -1.940253771513320125, 2.450533167346750307 ) ) ;
#1731=CARTESIAN_POINT ( 'NONE',  ( -1.810994336139479133, -2.918361879621429011, 5.667058093962724641 ) ) ;
#1738=CARTESIAN_POINT ( 'NONE',  ( -2.325590009395030133, -4.870737219477670799, 5.061077271074069905 ) ) ;
#1741=CARTESIAN_POINT ( 'NONE',  ( -2.601107615185130673, -5.215466101694915757, 5.226397344856384741 ) ) ;
#1752=CARTESIAN_POINT ( 'NONE',  ( 1.741105240696918965, -0.4774152569121725143, 2.691996915772988608 ) ) ;
#1754=CARTESIAN_POINT ( 'NONE',  ( 2.283153923255319739, -2.196424942684489512, 4.129076318403449797 ) ) ;
#1755=CARTESIAN_POINT ( 'NONE',  ( 0.2735655355027601376, -5.004947479095214646, 2.050775599341920330 ) ) ;
#1756=CARTESIAN_POINT ( 'NONE',  ( -2.352190863465239978, -4.917313796054239461, 4.622903765856379188 ) ) ;
#1759=CARTESIAN_POINT ( 'NONE',  ( 1.936998685628529948, -0.8418633456037969420, 3.363294429306519895 ) ) ;
#1768=CARTESIAN_POINT ( 'NONE',  ( -1.821706171509118954, -5.502118644067805597, 5.646608543709410455 ) ) ;
#1770=CARTESIAN_POINT ( 'NONE',  ( -2.308170020371289599, -1.726818300558750074, 5.159452766389659217 ) ) ;
#1771=CARTESIAN_POINT ( 'NONE',  ( 2.523518139275831462, -2.336154672414218592, 5.521565513971776085 ) ) ;
#1777=CARTESIAN_POINT ( 'NONE',  ( -2.062913653388399826, -3.217268751009200400, 5.832754583370829415 ) ) ;
#1778=CARTESIAN_POINT ( 'NONE',  ( -1.292934267244330471, -4.385524041783587457, 6.294748514096648151 ) ) ;
#1781=CARTESIAN_POINT ( 'NONE',  ( 0.009452039534068971960, -5.000193177104105047, 2.350000000173209536 ) ) ;
#1784=CARTESIAN_POINT ( 'NONE',  ( 2.226511124464869873, -1.074746228486680000, 5.462491901673799610 ) ) ;
#1786=CARTESIAN_POINT ( 'NONE',  ( 1.176011442874370649, -3.547145663405211646, 2.320901267448020722 ) ) ;
#1787=CARTESIAN_POINT ( 'NONE',  ( 1.725722849164588624, -0.1023305084745770588, 5.812007984777676661 ) ) ;
#1788=CARTESIAN_POINT ( 'NONE',  ( -2.267872052190610166, -1.843259742000189938, 4.071110468860649867 ) ) ;
#1793=CARTESIAN_POINT ( 'NONE',  ( 0.3752419433107367919, -4.175929447188990729, 7.023346545710360544 ) ) ;
#1795=CARTESIAN_POINT ( 'NONE',  ( 1.254903241568450900, -5.126483050847465250, 7.038391080368498365 ) ) ;
#1800=CARTESIAN_POINT ( 'NONE',  ( -1.112838723655040107, -0.4735169491525429986, 6.773667561836210105 ) ) ;
#1805=CARTESIAN_POINT ( 'NONE',  ( -1.160665242129840014, -3.100827309567759205, 6.393445611273007145 ) ) ;
#1807=CARTESIAN_POINT ( 'NONE',  ( 1.407651048079441525, -0.02669491525423760975, 2.450250343405061759 ) ) ;
#1815=CARTESIAN_POINT ( 'NONE',  ( -0.9222751404131109831, -5.577754237288145234, 2.865854510788139908 ) ) ;
#1816=DIRECTION ( 'NONE',  ( -2.220446049250309876E-16, 0.000000000000000000, 1.000000000000000000 ) ) ;
#1817=CARTESIAN_POINT ( 'NONE',  ( 2.608006145151101407, -4.172088570829024512, 5.191342690854350295 ) ) ;
#1819=CARTESIAN_POINT ( 'NONE',  ( 2.005512128484129963, -3.686875393134939394, 3.468469736471340159 ) ) ;
#1821=CARTESIAN_POINT ( 'NONE',  ( -2.007801995112629356, -2.988226744486289999, 5.128524201241715375 ) ) ;
#1827=CARTESIAN_POINT ( 'NONE',  ( -2.370419177058770366, -1.358046564306109261, 5.893409660608596390 ) ) ;
#1828=CARTESIAN_POINT ( 'NONE',  ( -1.496290472746829803, -0.5672554343907050267, 2.872674968141029961 ) ) ;
#1831=CARTESIAN_POINT ( 'NONE',  ( 1.943632316591230147, -5.046398305084740521, 3.373048379518159834 ) ) ;
#1837=CARTESIAN_POINT ( 'NONE',  ( 2.635341251434490495, -2.588484967225421762, 5.013193520829454464 ) ) ;
#1838=CARTESIAN_POINT ( 'NONE',  ( 1.495970331552388455, -0.4480353997208171291, 2.495424373718078570 ) ) ;
#1841=CARTESIAN_POINT ( 'NONE',  ( 2.295719155670170153, -2.312866384125930264, 5.218091927917190453 ) ) ;
#1844=CARTESIAN_POINT ( 'NONE',  ( 2.185196738168471153, -0.8418633456037974971, 3.194002352996649474 ) ) ;
#1846=CARTESIAN_POINT ( 'NONE',  ( -2.049150047780149642, -4.894025507765944916, 4.826039376028564476 ) ) ;
#1855=CARTESIAN_POINT ( 'NONE',  ( -1.417709711196470046, -2.006277760018209566, 2.821478011237799954 ) ) ;
#1857=CARTESIAN_POINT ( 'NONE',  ( 1.303621121494459967, -1.237764246504700072, 6.659417683669679455 ) ) ;
#1858=CARTESIAN_POINT ( 'NONE',  ( 2.190084968185480374, -4.032358841099290103, 3.838447030292440054 ) ) ;
#1859=CARTESIAN_POINT ( 'NONE',  ( -1.485933537025771356, -4.796950468210009255, 3.286232459959995911 ) ) ;
#1862=ORIENTED_EDGE ( 'NONE', *, *, #6717, .F. ) ;
#1863=CARTESIAN_POINT ( 'NONE',  ( -1.869504824896970119, -0.2046610169491529518, 5.548311746956866131 ) ) ;
#1864=CARTESIAN_POINT ( 'NONE',  ( 1.866416942370620058, -3.962493976234419790, 3.266391446483460026 ) ) ;
#1869=CARTESIAN_POINT ( 'NONE',  ( -0.4985810152601127254, -4.269082600342141376, 7.000035360316470445 ) ) ;
#1871=CARTESIAN_POINT ( 'NONE',  ( 2.043014502273419186, -5.041949152542365198, 3.006203457898239062 ) ) ;
#1873=EDGE_CURVE ( 'NONE', #14847, #15103, #9897, .T. ) ;
#1874=CARTESIAN_POINT ( 'NONE',  ( -0.2812789908084309953, -0.4557203389830509765, 7.036533610117280624 ) ) ;
#1876=MANIFOLD_SOLID_BREP ( 'Stock-MAS-687-1', #15580 ) ;
#1879=CARTESIAN_POINT ( 'NONE',  ( -1.990095963740230900, -4.847448931189385135, 5.204400533041805943 ) ) ;
#1880=CARTESIAN_POINT ( 'NONE',  ( -1.932035991685910004, -0.5610169491525425212, 2.884370051397200818 ) ) ;
#1886=CARTESIAN_POINT ( 'NONE',  ( -2.203023580853999963, -5.542161016949149754, 3.872235369154300333 ) ) ;
#1891=CARTESIAN_POINT ( 'NONE',  ( 1.771358649600380142, -4.335106588847043696, 6.676209054601206283 ) ) ;
#1895=CARTESIAN_POINT ( 'NONE',  ( 0.5320716618284230259, -2.592325843585389755, 6.992519451207130032 ) ) ;
#1899=CARTESIAN_POINT ( 'NONE',  ( -0.6713553523422816083, -2.732055573315119723, 6.640150466718877098 ) ) ;
#1905=CARTESIAN_POINT ( 'NONE',  ( -1.221947981261169991, -0.5741044150835520332, 2.670403636935529956 ) ) ;
#1908=CARTESIAN_POINT ( 'NONE',  ( -1.347262683220810553, -5.175423728813555613, 6.986424775243341045 ) ) ;
#1915=CARTESIAN_POINT ( 'NONE',  ( 0.5134687485628864900, -2.215872354612800521, 2.096259702418241222 ) ) ;
#1916=CARTESIAN_POINT ( 'NONE',  ( 0.9724415447670879953, -0.7068739681193980662, 2.553509270169310064 ) ) ;
#1918=CARTESIAN_POINT ( 'NONE',  ( 2.219956784870649624, -2.173136654396199852, 3.918630970161570026 ) ) ;
#1919=CARTESIAN_POINT ( 'NONE',  ( 0.009452110982655399438, -5.000192044704546035, 2.649999999999998579 ) ) ;
#1920=( BOUNDED_SURFACE ( )  B_SPLINE_SURFACE ( 3, 3, ( 
 ( #428, #11716, #7201, #17444, #13288, #7644, #3648 ),
 ( #4948, #9298, #10892, #9203, #10601, #6246, #6531 ),
 ( #2382, #5139, #10700, #9406, #14867, #17802, #14667 ),
 ( #2276, #15072, #3557, #8029, #6617, #13669, #2081 ),
 ( #14965, #6426, #3371, #1985, #12095, #5235, #12275 ),
 ( #16252, #16343, #17714, #608, #981, #2182, #9016 ),
 ( #5046, #7930, #13472, #10790, #11904, #14767, #13578 ) ),
 .UNSPECIFIED., .T., .F., .F. ) 
 B_SPLINE_SURFACE_WITH_KNOTS ( ( 4, 3, 4 ),
 ( 4, 1, 1, 1, 4 ),
 ( 0.000000000000000000, 3.141592653589790007, 6.283185307179590673 ),
 ( 0.000000000000000000, 0.3003308066897660278, 0.4325493167368040237, 0.5576349185195599301, 0.7853981633974479459 ),
 .UNSPECIFIED. ) 
 GEOMETRIC_REPRESENTATION_ITEM ( )  RATIONAL_B_SPLINE_SURFACE ( (
 ( 1.000000000000000000, 1.000000000000000000, 1.000000000000000000, 1.000000000000000000, 1.000000000000000000, 1.000000000000000000, 1.000000000000000000),
 ( 0.3333333333333329818, 0.3333333333333329818, 0.3333333333333329818, 0.3333333333333329818, 0.3333333333333329818, 0.3333333333333329818, 0.3333333333333329818),
 ( 0.3333333333333329818, 0.3333333333333329818, 0.3333333333333329818, 0.3333333333333329818, 0.3333333333333329818, 0.3333333333333329818, 0.3333333333333329818),
 ( 1.000000000000000000, 1.000000000000000000, 1.000000000000000000, 1.000000000000000000, 1.000000000000000000, 1.000000000000000000, 1.000000000000000000),
 ( 0.3333333333333329818, 0.3333333333333329818, 0.3333333333333329818, 0.3333333333333329818, 0.3333333333333329818, 0.3333333333333329818, 0.3333333333333329818),
 ( 0.3333333333333329818, 0.3333333333333329818, 0.3333333333333329818, 0.3333333333333329818, 0.3333333333333329818, 0.3333333333333329818, 0.3333333333333329818),
 ( 1.000000000000000000, 1.000000000000000000, 1.000000000000000000, 1.000000000000000000, 1.000000000000000000, 1.000000000000000000, 1.000000000000000000) ) ) 
 REPRESENTATION_ITEM ( '' )  SURFACE ( )  );
#1921=CARTESIAN_POINT ( 'NONE',  ( 2.035218756299218779, -0.8185750573155082810, 2.996768277952650106 ) ) ;
#1923=CARTESIAN_POINT ( 'NONE',  ( 2.331386066015260106, -0.9583047870452390260, 4.378465089518139841 ) ) ;
#1924=B_SPLINE_CURVE_WITH_KNOTS ( 'NONE', 3,
 ( #10317, #11526, #494, #3284, #8843, #13176, #13010, #15978, #12829, #1541, #413, #11805, #332, #17428, #4747 ),
 .UNSPECIFIED., .F., .F.,
 ( 4, 1, 1, 1, 1, 1, 1, 1, 1, 1, 1, 1, 4 ),
 ( 0.000000000000000000, 0.04238384222888209873, 0.08486641011435110127, 0.1274541364341900129, 0.1700199979529180005, 0.2125927824333140037, 0.2551660849077280191, 0.2977383825900840053, 0.3403095086484199672, 0.3828788202031120358, 0.4254464832354830084, 0.4680130360808240075, 0.4999998212288440103 ),
 .UNSPECIFIED. ) ;
#1933=ORIENTED_EDGE ( 'NONE', *, *, #14000, .F. ) ;
#1934=CARTESIAN_POINT ( 'NONE',  ( 0.3413183941262679655, -2.914521003261450360, 7.028571974690709823 ) ) ;
#1938=CARTESIAN_POINT ( 'NONE',  ( 1.480680413335799805, -1.214475958216410190, 6.529298007719799735 ) ) ;
#1939=CARTESIAN_POINT ( 'NONE',  ( 1.567709126316360058, -3.915917399657849796, 2.944712621036570166 ) ) ;
#1940=CARTESIAN_POINT ( 'NONE',  ( 1.727468145286579659, -3.966334852594401994, 5.809394271505055052 ) ) ;
#1944=CARTESIAN_POINT ( 'NONE',  ( 0.3265524029357661506, -0.1423728813559330397, 6.726831181542982208 ) ) ;
#1945=CARTESIAN_POINT ( 'NONE',  ( -1.630481553867809907, -3.543304787045240101, 3.002862530617889547 ) ) ;
#1950=CARTESIAN_POINT ( 'NONE',  ( 2.345213174852950111, -3.803316834576379701, 4.503223853122318765 ) ) ;
#1951=CARTESIAN_POINT ( 'NONE',  ( -2.354888465609351389, -5.202118644067803999, 5.923664702843871588 ) ) ;
#1957=CARTESIAN_POINT ( 'NONE',  ( -0.7854158957162378218, -3.636457940198391636, 2.803154272645148826 ) ) ;
#1959=CARTESIAN_POINT ( 'NONE',  ( 1.973760952634081134, -0.04004237288135625850, 2.925986839873718992 ) ) ;
#1963=CARTESIAN_POINT ( 'NONE',  ( -2.508228811380011081, -0.5091101694915260989, 5.566973598334550744 ) ) ;
#1966=CARTESIAN_POINT ( 'NONE',  ( -0.07299321914061848715, -5.598516949152539723, 2.350000000000000089 ) ) ;
#1970=CARTESIAN_POINT ( 'NONE',  ( 2.369027826908510548, -4.009070552811004440, 3.503830760997844518 ) ) ;
#1972=CARTESIAN_POINT ( 'NONE',  ( 0.6343239990445400656, -3.500569086828630105, 2.433641963034069988 ) ) ;
#1977=CARTESIAN_POINT ( 'NONE',  ( -1.658519201881210714, -3.197821339080880065, 3.489952108543053377 ) ) ;
#1979=CARTESIAN_POINT ( 'NONE',  ( -0.8967027089122764361, -1.195028546288099625, 6.546842195331652903 ) ) ;
#1985=CARTESIAN_POINT ( 'NONE',  ( 0.8675710780368863784, -0.4076464065212254684, 2.836323152971460981 ) ) ;
#1988=CARTESIAN_POINT ( 'NONE',  ( -1.820241257191459905, -5.080331814072259533, 3.208199930689799917 ) ) ;
#1992=CARTESIAN_POINT ( 'NONE',  ( -1.194742379459959869, -5.175423728813560054, 6.727584234649759409 ) ) ;
#1998=CARTESIAN_POINT ( 'NONE',  ( 1.307725206348619995, -0.7471169921413569615, 2.732408283416570161 ) ) ;
#2002=CARTESIAN_POINT ( 'NONE',  ( -1.176011442874419943, -2.052854336594789331, 2.320901267448050476 ) ) ;
#2007=CARTESIAN_POINT ( 'NONE',  ( -2.287919158821179799, -4.548542059801599535, 5.251517552016939483 ) ) ;
#2008=CARTESIAN_POINT ( 'NONE',  ( 0.6536199613480476733, -5.011796459788070202, 2.109674034588110647 ) ) ;
#2011=CARTESIAN_POINT ( 'NONE',  ( -1.951437470830620136, -5.057043525783970317, 3.384463041838880137 ) ) ;
#2015=CARTESIAN_POINT ( 'NONE',  ( 1.707817112497189926, -0.4112288135593229477, 6.319218296629480314 ) ) ;
#2026=CARTESIAN_POINT ( 'NONE',  ( -0.3159454637156809409, -2.984385868126319785, 7.032150113402090064 ) ) ;
#2032=CARTESIAN_POINT ( 'NONE',  ( 0.06276132972186961034, -1.377493976234430040, 7.052616990284530374 ) ) ;
#2033=CARTESIAN_POINT ( 'NONE',  ( -1.092567884283820012, -4.637854336594780413, 6.784476218553590066 ) ) ;
#2034=CARTESIAN_POINT ( 'NONE',  ( -0.2475374578675481607, -4.245794312053864594, 6.738044908627027318 ) ) ;
#2040=CARTESIAN_POINT ( 'NONE',  ( -0.6187874668174415671, -0.1646186440677970542, 6.657494107589526422 ) ) ;
#2041=CARTESIAN_POINT ( 'NONE',  ( 0.3949552299394610277, -3.776187669928119828, 2.379923265530350385 ) ) ;
#2048=CARTESIAN_POINT ( 'NONE',  ( -3.161120280659493168E-15, -5.600000000000000533, 2.050000000000001155 ) ) ;
#2057=CARTESIAN_POINT ( 'NONE',  ( 0.3429245540020083860, -3.776187669928120272, 2.675820019639898906 ) ) ;
#2058=CARTESIAN_POINT ( 'NONE',  ( -1.467041701146829746, -0.4779661016949154906, 6.911479965439912831 ) ) ;
#2061=CARTESIAN_POINT ( 'NONE',  ( 0.9002849211310119948, -0.4334745762711874617, 7.196465912290821443 ) ) ;
#2063=CARTESIAN_POINT ( 'NONE',  ( -0.4360591020458099987, -5.591101694915249887, 2.387347919655840034 ) ) ;
#2065=CARTESIAN_POINT ( 'NONE',  ( 1.777964140657679382, -0.8689925102520593692, 6.241943319976220650 ) ) ;
#2067=CARTESIAN_POINT ( 'NONE',  ( -1.449568901432419343, -0.2625000000000002331, 3.250431098567584165 ) ) ;
#2068=CARTESIAN_POINT ( 'NONE',  ( 0.9279264017968674727, -4.428259742000194343, 7.186376135231798301 ) ) ;
#2070=CARTESIAN_POINT ( 'NONE',  ( 1.417709711196429856, -3.593722239981790079, 2.821478011237759986 ) ) ;
#2073=CARTESIAN_POINT ( 'NONE',  ( 0.3257255101953561716, -4.175929447188994281, 6.727018681373227338 ) ) ;
#2077=CARTESIAN_POINT ( 'NONE',  ( -2.044452488559148851, -1.451199717459271454, 4.887392274793804781 ) ) ;
#2081=CARTESIAN_POINT ( 'NONE',  ( 1.670747221194369914, -0.4963798976394459550, 3.047345349617600174 ) ) ;
#2082=CARTESIAN_POINT ( 'NONE',  ( -0.4500319419455615089, -1.125163681423229756, 7.315451193241928607 ) ) ;
#2088=CARTESIAN_POINT ( 'NONE',  ( 1.494593880360790550, -5.038983050847454237, 3.295456077495951153 ) ) ;
#2096=CARTESIAN_POINT ( 'NONE',  ( 1.289141334274990447, -5.417584745762705545, 6.297747079672416426 ) ) ;
#2097=CARTESIAN_POINT ( 'NONE',  ( 0.3578984759184136166, -2.615614131873680748, 7.329643012642057087 ) ) ;
#2099=CARTESIAN_POINT ( 'NONE',  ( -2.653777292528150866, -1.773394877135329839, 4.724078510415215426 ) ) ;
#2103=CARTESIAN_POINT ( 'NONE',  ( 2.345213174852950111, -3.803316834576380145, 4.503223853122319653 ) ) ;
#2106=CARTESIAN_POINT ( 'NONE',  ( 0.7540633504677742849, -2.239160642901089293, 2.155495695330191364 ) ) ;
#2111=CARTESIAN_POINT ( 'NONE',  ( -1.236334101859210000, -2.029566048306499670, 2.697445712080720259 ) ) ;
#2112=CARTESIAN_POINT ( 'NONE',  ( 1.194742379459969861, -0.4245762711864409789, 6.727584234649759409 ) ) ;
#2114=CARTESIAN_POINT ( 'NONE',  ( 2.431060148753489081, -5.355296610169490101, 3.635668498923322112 ) ) ;
#2124=CARTESIAN_POINT ( 'NONE',  ( 2.301223891756920104, -2.611773255513699876, 5.193066210047949660 ) ) ;
#2127=CARTESIAN_POINT ( 'NONE',  ( 0.06264882350516240428, -5.448728813559320372, 7.052569299041220319 ) ) ;
#2132=EDGE_CURVE ( 'NONE', #7787, #2833, #13428, .T. ) ;
#2133=CARTESIAN_POINT ( 'NONE',  ( -1.282210379528740063, -4.661142624883069630, 6.673494927815290190 ) ) ;
#2135=CARTESIAN_POINT ( 'NONE',  ( 1.854389246811829706, -2.448755237495690462, 3.819010576716856065 ) ) ;
#2141=CARTESIAN_POINT ( 'NONE',  ( -2.283153923255329953, -3.403575057315510133, 4.129076318403500423 ) ) ;
#2150=CARTESIAN_POINT ( 'NONE',  ( 1.925796468768800063, -5.104237288135590411, 6.052706598917719560 ) ) ;
#2152=CARTESIAN_POINT ( 'NONE',  ( -1.661700935788390066, -0.5625000000000000000, 3.038299064211610112 ) ) ;
#2158=CARTESIAN_POINT ( 'NONE',  ( 2.018065005288410152, -4.172088570829024512, 5.077247235985069551 ) ) ;
#2159=CARTESIAN_POINT ( 'NONE',  ( -2.043014502273419186, -0.5580508474576266753, 3.006203457898251052 ) ) ;
#2162=CARTESIAN_POINT ( 'NONE',  ( 2.614198783383141045, -0.06673728813559372253, 4.243032045539284702 ) ) ;
#2165=CARTESIAN_POINT ( 'NONE',  ( -0.1565249325564300187, -5.453177966101690366, 7.048192310558509810 ) ) ;
#2167=CARTESIAN_POINT ( 'NONE',  ( 2.065623031241558660, -0.5662447625043108834, 3.572193642975259653 ) ) ;
#2168=CARTESIAN_POINT ( 'NONE',  ( -0.4037348727536037574, -0.5906145504024216120, 2.679104755345550704 ) ) ;
#2169=CARTESIAN_POINT ( 'NONE',  ( -1.648422021521479763, -4.684430913171365063, 6.779860219333237126 ) ) ;
#2173=CARTESIAN_POINT ( 'NONE',  ( -2.276802572547989900, -3.104668185927729862, 4.104251954998810348 ) ) ;
#2176=CARTESIAN_POINT ( 'NONE',  ( 1.966895454505939833, -3.896469987729531681, 5.288408118292026394 ) ) ;
#2179=CARTESIAN_POINT ( 'NONE',  ( 2.049636678546640667, -2.243001519261071053, 4.582138519505345009 ) ) ;
#2182=CARTESIAN_POINT ( 'NONE',  ( 1.330034674284700458, -0.7763906680874423927, 3.132218110693851809 ) ) ;
#2183=CARTESIAN_POINT ( 'NONE',  ( -2.653064503426820764, -3.034803321062870651, 4.766048721853594294 ) ) ;
#2186=CARTESIAN_POINT ( 'NONE',  ( 2.151546283159470274, -0.8884399221803740421, 3.746273477677459773 ) ) ;
#2188=CARTESIAN_POINT ( 'NONE',  ( 2.051331987628511211, -5.073093220338980025, 4.618035453557344461 ) ) ;
#2195=CARTESIAN_POINT ( 'NONE',  ( -1.246151616534680651, -5.568855932203385706, 3.068501529594771071 ) ) ;
#2196=CARTESIAN_POINT ( 'NONE',  ( 1.176011442874370649, -3.547145663405211646, 2.320901267448020722 ) ) ;
#2198=CARTESIAN_POINT ( 'NONE',  ( 0.6265155281652680097, -2.891232714973161144, 7.278874170247493502 ) ) ;
#2201=CARTESIAN_POINT ( 'NONE',  ( -0.4985810152601130585, -4.269082600342140488, 7.000035360316470445 ) ) ;
#2204=CARTESIAN_POINT ( 'NONE',  ( -1.503451935564901643, -3.100827309567759205, 6.886949009567437052 ) ) ;
#2208=CARTESIAN_POINT ( 'NONE',  ( -2.005512128484160161, -1.913124606865060029, 3.468469736471389897 ) ) ;
#2209=CARTESIAN_POINT ( 'NONE',  ( -2.058670345754650022, -0.5491525423728820243, 3.559656372813929881 ) ) ;
#2211=CARTESIAN_POINT ( 'NONE',  ( -1.851073041990159984, -5.493220338983049622, 6.153284478378270528 ) ) ;
#2214=CARTESIAN_POINT ( 'NONE',  ( 1.925796468768799397, -5.104237288135589523, 6.052706598917718672 ) ) ;
#2219=CARTESIAN_POINT ( 'NONE',  ( -2.062913653388399826, -3.217268751009200400, 5.832754583370829415 ) ) ;
#2221=CARTESIAN_POINT ( 'NONE',  ( -1.851073041990159984, -5.493220338983049622, 6.153284478378270528 ) ) ;
#2222=CARTESIAN_POINT ( 'NONE',  ( 1.265407828724300021, -2.309025507765960050, 2.715689360385540319 ) ) ;
#2223=CARTESIAN_POINT ( 'NONE',  ( -1.626408692231610109, -4.707719201459649838, 6.401040991074980369 ) ) ;
#2224=CARTESIAN_POINT ( 'NONE',  ( 1.959085573314239159, -2.635061543801990869, 5.313910057793555630 ) ) ;
#2227=PRODUCT_DEFINITION ( 'UNKNOWN', '', #1, #8436 ) ;
#2228=CARTESIAN_POINT ( 'NONE',  ( -1.496290472746829803, -0.5672554343907050267, 2.872674968141029961 ) ) ;
#2233=CARTESIAN_POINT ( 'NONE',  ( -2.326448859701059746, -3.380286769027220029, 4.344498395672320434 ) ) ;
#2241=CARTESIAN_POINT ( 'NONE',  ( -1.851073041990159984, -5.193220338983049800, 6.153284478378270528 ) ) ;
#2244=CARTESIAN_POINT ( 'NONE',  ( 1.722199153441390074, -0.5041426604022090086, 3.099360556065540173 ) ) ;
#2246=CARTESIAN_POINT ( 'NONE',  ( -0.03895741673419786388, -3.729611093351542284, 2.647347042895590086 ) ) ;
#2247=CARTESIAN_POINT ( 'NONE',  ( -1.467041701146829746, -0.1779661016949160846, 6.911479965439912831 ) ) ;
#2250=CARTESIAN_POINT ( 'NONE',  ( 0.9002849211310119948, -0.1334745762711869732, 7.196465912290821443 ) ) ;
#2253=CARTESIAN_POINT ( 'NONE',  ( -2.253200202764409799, -5.511016949152540256, 5.379408587037509903 ) ) ;
#2256=CARTESIAN_POINT ( 'NONE',  ( 1.092567884283869750, -0.9621456634052130141, 6.784476218553569637 ) ) ;
#2257=CARTESIAN_POINT ( 'NONE',  ( 2.224278379903029901, -5.390889830508481140, 5.468825643806100700 ) ) ;
#2258=CARTESIAN_POINT ( 'NONE',  ( 1.233489123281660715, -0.9621456634052125700, 7.049812391606558037 ) ) ;
#2261=CARTESIAN_POINT ( 'NONE',  ( 1.772995665808909660, -0.8224159336754829353, 5.735078843205156041 ) ) ;
#2262=CARTESIAN_POINT ( 'NONE',  ( -2.293791554891330353, -4.777584066324515710, 6.034778631725542297 ) ) ;
#2265=CARTESIAN_POINT ( 'NONE',  ( -0.05638445020225820586, -4.222506023765566496, 6.752248190741917178 ) ) ;
#2269=CARTESIAN_POINT ( 'NONE',  ( 2.035869680587130137, -2.289578095837640159, 4.964832940349494628 ) ) ;
#2276=CARTESIAN_POINT ( 'NONE',  ( 0.009452110982655408111, -0.3001920447045370310, 2.350000000000000089 ) ) ;
#2277=CARTESIAN_POINT ( 'NONE',  ( 2.409576349373750315, -2.149848366107909303, 3.587770028483080242 ) ) ;
#2280=CARTESIAN_POINT ( 'NONE',  ( 2.226511124464869873, -1.074746228486680000, 5.462491901673799610 ) ) ;
#2283=CARTESIAN_POINT ( 'NONE',  ( 1.795861365445541091, -5.050847457627124726, 3.705232155007893713 ) ) ;
#2291=CARTESIAN_POINT ( 'NONE',  ( 2.143090896833110381, -5.395338983050850246, 5.672454929438339732 ) ) ;
#2293=CARTESIAN_POINT ( 'NONE',  ( -2.426866425021068974, -4.711560077819614278, 3.626019996130659617 ) ) ;
#2298=CARTESIAN_POINT ( 'NONE',  ( 2.005512128484129963, -3.686875393134939394, 3.468469736471340159 ) ) ;
#2303=CARTESIAN_POINT ( 'NONE',  ( 0.8642983280852605255, -2.867944426684881254, 7.209203477813407979 ) ) ;
#2308=CARTESIAN_POINT ( 'NONE',  ( -2.234315482767910144, -0.5402542372881360411, 3.960850823455329905 ) ) ;
#2311=CARTESIAN_POINT ( 'NONE',  ( -2.353343516942199898, -1.773394877135329839, 4.722803042560189901 ) ) ;
#2312=CARTESIAN_POINT ( 'NONE',  ( -0.7093417302541390468, -0.4646186440677970153, 6.943956659919700236 ) ) ;
#2315=CARTESIAN_POINT ( 'NONE',  ( 1.791574935211219355, -5.108686440677969287, 6.226029630577610163 ) ) ;
#2317=CARTESIAN_POINT ( 'NONE',  ( 0.009452039534070141164, -0.3001931771041043140, 2.350000000173209092 ) ) ;
#2321=CARTESIAN_POINT ( 'NONE',  ( -1.097561405233230092, -3.613169651910099756, 2.618148744692269769 ) ) ;
#2327=CARTESIAN_POINT ( 'NONE',  ( 0.1226612266411070129, -2.937809291549740021, 7.050255286338659388 ) ) ;
#2329=CARTESIAN_POINT ( 'NONE',  ( -0.8092638295168711471, -4.911779243796850380, 2.486823565593870189 ) ) ;
#2331=CARTESIAN_POINT ( 'NONE',  ( -1.727468145286550127, -1.633665147405598761, 5.809394271505101237 ) ) ;
#2332=CARTESIAN_POINT ( 'NONE',  ( -1.300961508564169922, -0.4779661016949160457, 6.661123742937279602 ) ) ;
#2334=CARTESIAN_POINT ( 'NONE',  ( -1.661700935788390066, -0.2625000000000000111, 3.038299064211610112 ) ) ;
#2338=SURFACE_SIDE_STYLE ('',( #13981 ) ) ;
#2344=CARTESIAN_POINT ( 'NONE',  ( -2.253200202764409799, -5.211016949152540434, 5.379408587037509903 ) ) ;
#2347=CARTESIAN_POINT ( 'NONE',  ( -2.311987889326990064, -1.521064582324129999, 4.260161748947139948 ) ) ;
#2351=CARTESIAN_POINT ( 'NONE',  ( -2.049150047780149642, -4.894025507765944916, 4.826039376028564476 ) ) ;
#2352=CARTESIAN_POINT ( 'NONE',  ( 1.549742865090599997, -0.1156779661016950067, 6.471102547561449647 ) ) ;
#2354=CARTESIAN_POINT ( 'NONE',  ( 1.438959988998139914E-16, -0.2999999999999999889, 2.350000000000000089 ) ) ;
#2356=CARTESIAN_POINT ( 'NONE',  ( 0.6640878839024751956, -0.1379237288135599648, 7.269405042592523181 ) ) ;
#2359=CARTESIAN_POINT ( 'NONE',  ( -2.102728310581289062, -1.358046564306110593, 5.757014351541100083 ) ) ;
#2360=CARTESIAN_POINT ( 'NONE',  ( -1.000896394980330006, -5.470974576271190770, 6.829956240957379521 ) ) ;
#2361=CARTESIAN_POINT ( 'NONE',  ( -0.4500319419455615089, -1.125163681423229756, 7.315451193241928607 ) ) ;
#2366=CARTESIAN_POINT ( 'NONE',  ( -2.151546283159490258, -4.711560077819619607, 3.746273477677509955 ) ) ;
#2368=CARTESIAN_POINT ( 'NONE',  ( 1.947945325730759292, -4.311818300558746486, 6.502393603230323116 ) ) ;
#2372=CARTESIAN_POINT ( 'NONE',  ( -2.045969882616350155, -1.796683165423619055, 4.529973290172065070 ) ) ;
#2375=CARTESIAN_POINT ( 'NONE',  ( 1.698651900122530867, -2.406019537279079579, 5.853032334688926142 ) ) ;
#2380=CARTESIAN_POINT ( 'NONE',  ( -0.6187874668174415671, -0.1646186440677970542, 6.657494107589526422 ) ) ;
#2382=CARTESIAN_POINT ( 'NONE',  ( 0.009452110982655399438, -0.3001920447045380858, 2.050000000000001155 ) ) ;
#2383=CARTESIAN_POINT ( 'NONE',  ( 0.2938780505771511620, -1.893677194936738806, 2.062434951628520086 ) ) ;
#2387=CARTESIAN_POINT ( 'NONE',  ( -0.8298945877350979439, -5.211074464177370302, 2.494426474263899962 ) ) ;
#2388=CARTESIAN_POINT ( 'NONE',  ( 0.9150601050661639757, -5.130932203389829915, 6.868218666554230190 ) ) ;
#2395=CARTESIAN_POINT ( 'NONE',  ( 1.811729841638690219, -5.341949152542369461, 3.197954009834290012 ) ) ;
#2396=CARTESIAN_POINT ( 'NONE',  ( 2.260671505268459391, -3.686875393134939394, 3.309864021662241029 ) ) ;
#2398=CARTESIAN_POINT ( 'NONE',  ( -2.623186471072040504, -3.380286769027221805, 4.297499775172091141 ) ) ;
#2402=CARTESIAN_POINT ( 'NONE',  ( -0.01716182025094739952, -3.430704221963770006, 2.346608583467349796 ) ) ;
#2405=CARTESIAN_POINT ( 'NONE',  ( 0.6265155281652680097, -2.891232714973161144, 7.278874170247493502 ) ) ;
#2408=CARTESIAN_POINT ( 'NONE',  ( 2.011500846714319835, -0.3489406779661020086, 3.478373409938460448 ) ) ;
#2409=CARTESIAN_POINT ( 'NONE',  ( 1.303621121494459967, -1.237764246504700072, 6.659417683669679455 ) ) ;
#2410=CARTESIAN_POINT ( 'NONE',  ( -2.328217775191430139, -0.5180084745762719711, 5.043379051721170292 ) ) ;
#2412=CARTESIAN_POINT ( 'NONE',  ( -0.07299321914061848715, -5.598516949152539723, 2.350000000000000089 ) ) ;
#2416=CARTESIAN_POINT ( 'NONE',  ( -0.7983658734557951275, -5.166525423728808519, 6.913847129767330735 ) ) ;
#2421=CARTESIAN_POINT ( 'NONE',  ( -2.219956784870669608, -3.426863345603790023, 3.918630970161619764 ) ) ;
#2424=CARTESIAN_POINT ( 'NONE',  ( -1.428515267734880023, -5.568855932203390147, 2.829745655876930055 ) ) ;
#2427=CARTESIAN_POINT ( 'NONE',  ( -2.199335452462570117, -1.866548030288480042, 3.862342996790939953 ) ) ;
#2428=CARTESIAN_POINT ( 'NONE',  ( -2.334748642087669523, -4.940602084342530453, 4.403867486184871005 ) ) ;
#2429=CARTESIAN_POINT ( 'NONE',  ( -2.013199450439951299, -1.726818300558751851, 5.102405038955014405 ) ) ;
#2431=CARTESIAN_POINT ( 'NONE',  ( -1.303682947472720954, -0.2673043920988010802, 3.104350467804975366 ) ) ;
#2434=CARTESIAN_POINT ( 'NONE',  ( -0.03714311608457869507, -4.521412895153340550, 7.053160869216429596 ) ) ;
#2439=CARTESIAN_POINT ( 'NONE',  ( -2.011500846714319835, -5.251059322033900578, 3.478373409938470218 ) ) ;
#2441=CARTESIAN_POINT ( 'NONE',  ( -2.516451517878150135, -4.688271789531334832, 3.857037693030694214 ) ) ;
#2443=CARTESIAN_POINT ( 'NONE',  ( 0.4985810152601650724, -1.330917399657850053, 7.000035360316460675 ) ) ;
#2445=CARTESIAN_POINT ( 'NONE',  ( 2.318251751302029984, -0.06673728813559359763, 4.294764266798990704 ) ) ;
#2447=CARTESIAN_POINT ( 'NONE',  ( -1.791574935211209807, -0.4913135593220339659, 6.226029630577610163 ) ) ;
#2449=CARTESIAN_POINT ( 'NONE',  ( -2.043014502273419186, -0.2580508474576271305, 3.006203457898251052 ) ) ;
#2451=CARTESIAN_POINT ( 'NONE',  ( 1.951437470830589271, -0.5429564742160231106, 3.384463041838830843 ) ) ;
#2453=CARTESIAN_POINT ( 'NONE',  ( -2.270487904532170198, -5.537711864406779760, 4.080813552109679776 ) ) ;
#2454=CARTESIAN_POINT ( 'NONE',  ( 1.940935473245969156, -0.5041426604022095637, 2.893832807158179143 ) ) ;
#2458=CARTESIAN_POINT ( 'NONE',  ( 0.8001898266890951072, -4.129352870612410520, 6.913242401714550844 ) ) ;
#2459=CARTESIAN_POINT ( 'NONE',  ( -2.589817782457070727, -4.963890372630814340, 4.120381550730010112 ) ) ;
#2462=CARTESIAN_POINT ( 'NONE',  ( 1.785776242921180756, -1.121322805063259542, 5.712869711683790541 ) ) ;
#2468=CARTESIAN_POINT ( 'NONE',  ( -2.567863625471609179, -3.104668185927728974, 4.029783546918099368 ) ) ;
#2472=CARTESIAN_POINT ( 'NONE',  ( 2.050059171113549183, -5.377542372881360500, 4.809263467226075228 ) ) ;
#2481=CARTESIAN_POINT ( 'NONE',  ( -1.596341326794979976, -5.564406779661021041, 2.970780074643819990 ) ) ;
#2482=CARTESIAN_POINT ( 'NONE',  ( 1.558664967382918931, -4.059488005747546424, 6.847947208954417775 ) ) ;
#2483=CARTESIAN_POINT ( 'NONE',  ( 0.4469859058769135030, -3.776187669928120272, 2.084026511420788985 ) ) ;
#2485=CARTESIAN_POINT ( 'NONE',  ( -2.291237445532080308, -4.664983501243040287, 4.162434510291849854 ) ) ;
#2490=CARTESIAN_POINT ( 'NONE',  ( 2.088297318559229954, -0.3978813559322040283, 5.785136623276629919 ) ) ;
#2491=CARTESIAN_POINT ( 'NONE',  ( -1.586727176531439909, -1.982989471729919906, 2.961885344765640138 ) ) ;
#2494=CARTESIAN_POINT ( 'NONE',  ( -2.268288188848061715, -5.551059322033894183, 3.322421079292323665 ) ) ;
#2498=CARTESIAN_POINT ( 'NONE',  ( 2.293398556041700065, -5.064194915254238261, 4.171956209133471205 ) ) ;
#2502=CARTESIAN_POINT ( 'NONE',  ( 2.313035575219750228, -4.172088570829020071, 5.134294963419709923 ) ) ;
#2504=CARTESIAN_POINT ( 'NONE',  ( -2.203023580853999963, -5.542161016949149754, 3.872235369154300333 ) ) ;
#2506=CARTESIAN_POINT ( 'NONE',  ( -2.237394498046660019, -3.263845327585780165, 5.429939413646380331 ) ) ;
#2508=CARTESIAN_POINT ( 'NONE',  ( -1.842787987253248883, -1.889836318576769036, 3.794994874786233652 ) ) ;
#2510=FACE_OUTER_BOUND ( 'NONE', #10800, .T. ) ;
#2514=CARTESIAN_POINT ( 'NONE',  ( -1.777964140657649850, -4.731007489747940831, 6.241943319976260618 ) ) ;
#2516=EDGE_LOOP ( 'NONE', ( #12505, #3361, #3055, #8702 ) ) ;
#2520=CARTESIAN_POINT ( 'NONE',  ( -0.4360591020458099987, -5.291101694915250064, 2.387347919655840034 ) ) ;
#2523=CARTESIAN_POINT ( 'NONE',  ( 2.065623031241559548, -0.5662447625043109944, 3.572193642975259653 ) ) ;
#2525=CARTESIAN_POINT ( 'NONE',  ( -2.182690844914350059, -1.680241723982170088, 5.580117243900479806 ) ) ;
#2526=CARTESIAN_POINT ( 'NONE',  ( 0.4221287159901364605, -0.1423728813559330397, 7.320050063945812369 ) ) ;
#2527=CARTESIAN_POINT ( 'NONE',  ( -2.043308330018790198, -0.5002118644067800046, 5.867646457774669422 ) ) ;
#2529=CARTESIAN_POINT ( 'NONE',  ( 1.750316316486830059, -0.04004237288135630013, 3.126818518378580158 ) ) ;
#2532=CARTESIAN_POINT ( 'NONE',  ( 0.5320716618284228039, -2.592325843585389311, 6.992519451207130032 ) ) ;
#2533=CARTESIAN_POINT ( 'NONE',  ( -2.306642602145299925, -5.515466101694909362, 5.166805192608490138 ) ) ;
#2534=CARTESIAN_POINT ( 'NONE',  ( -1.835211330903778970, -4.707719201459645397, 6.617058440404012032 ) ) ;
#2537=CARTESIAN_POINT ( 'NONE',  ( 0.1569242594330760021, -4.199217735477280833, 7.048216443236290374 ) ) ;
#2541=CARTESIAN_POINT ( 'NONE',  ( -1.043047520545169471, -1.517223705964159786, 6.468319459971155538 ) ) ;
#2546=CARTESIAN_POINT ( 'NONE',  ( -1.562863241354461641, -0.1913135593220339215, 6.031217337312382298 ) ) ;
#2549=CARTESIAN_POINT ( 'NONE',  ( -0.4469859058769716786, -1.823812330071880705, 2.084026511420800976 ) ) ;
#2552=CARTESIAN_POINT ( 'NONE',  ( -0.4446501070882830087, -4.952022267818760426, 2.379695998155090031 ) ) ;
#2553=CARTESIAN_POINT ( 'NONE',  ( -1.921786527979019166, -5.242161016949150820, 3.977907449687794195 ) ) ;
#2559=CARTESIAN_POINT ( 'NONE',  ( -0.1565249325564300187, -5.453177966101690366, 7.048192310558509810 ) ) ;
#2560=CARTESIAN_POINT ( 'NONE',  ( 1.132648842710480830, -4.106064582324130185, 7.100045893750476900 ) ) ;
#2561=CARTESIAN_POINT ( 'NONE',  ( 2.247144151254821143, -3.985782264522713447, 3.288101683376901452 ) ) ;
#2564=CARTESIAN_POINT ( 'NONE',  ( -1.065036425887979421, -1.218316834576379737, 6.455163597548632559 ) ) ;
#2573=CARTESIAN_POINT ( 'NONE',  ( 2.614198783383141045, -0.3667372881355940861, 4.243032045539284702 ) ) ;
#2574=CARTESIAN_POINT ( 'NONE',  ( 1.567709126316360058, -3.915917399657849796, 2.944712621036570166 ) ) ;
#2575=CARTESIAN_POINT ( 'NONE',  ( -0.009227126607030738600, -5.296242143452180251, 2.310024366372019688 ) ) ;
#2577=CARTESIAN_POINT ( 'NONE',  ( -2.354888465609351389, -5.502118644067805597, 5.923664702843871588 ) ) ;
#2582=CARTESIAN_POINT ( 'NONE',  ( -1.378221871957429512, -5.179872881355929159, 6.607619368096277590 ) ) ;
#2584=CARTESIAN_POINT ( 'NONE',  ( 0.009452071482872208621, -0.3001926707426449403, 2.353323636140386199 ) ) ;
#2589=CARTESIAN_POINT ( 'NONE',  ( 2.353452300571019506, -4.125511994252439862, 4.697179287168359529 ) ) ;
#2592=CARTESIAN_POINT ( 'NONE',  ( 0.009452110982655383825, -5.000192044704546035, 2.050000000000001155 ) ) ;
#2597=CARTESIAN_POINT ( 'NONE',  ( -0.7435598031058080482, -3.030962444702889780, 6.932904947974540377 ) ) ;
#2602=CARTESIAN_POINT ( 'NONE',  ( -1.992092870331710452, -3.403575057315514130, 4.203544726484199856 ) ) ;
#2603=CARTESIAN_POINT ( 'NONE',  ( -0.06264882350515391107, -0.4512711864406790396, 7.052569299041220319 ) ) ;
#2606=CARTESIAN_POINT ( 'NONE',  ( -0.1698804968610999888, -0.2965485159365569556, 2.349238660949160007 ) ) ;
#2609=CARTESIAN_POINT ( 'NONE',  ( -1.460675875430050175, -4.684430913171359734, 6.545310725710059785 ) ) ;
#2615=CARTESIAN_POINT ( 'NONE',  ( -1.042222075699109407, -5.175423728813555613, 6.468743694056166227 ) ) ;
#2620=CARTESIAN_POINT ( 'NONE',  ( -1.505092429369619955, -5.128627060139309357, 2.879659483602799774 ) ) ;
#2624=CARTESIAN_POINT ( 'NONE',  ( -2.255259958075430227, -1.703530012270459970, 5.372717034856060003 ) ) ;
#2625=CARTESIAN_POINT ( 'NONE',  ( -1.932035991685910004, -0.2610169491525428653, 2.884370051397200818 ) ) ;
#2628=CARTESIAN_POINT ( 'NONE',  ( 1.851073041990159984, -0.1067796610169499949, 6.153284478378259870 ) ) ;
#2635=CARTESIAN_POINT ( 'NONE',  ( -1.724579595320039793, -1.660794312053859745, 3.098572228637930248 ) ) ;
#2636=CARTESIAN_POINT ( 'NONE',  ( 1.873832970144350130, -5.337500000000000355, 2.826167029855650270 ) ) ;
#2639=CARTESIAN_POINT ( 'NONE',  ( 1.115198193348289957, -1.261052534792989954, 6.772457159276550342 ) ) ;
#2640=CARTESIAN_POINT ( 'NONE',  ( 2.182690844914370043, -3.919758276017820453, 5.580117243900430068 ) ) ;
#2646=CARTESIAN_POINT ( 'NONE',  ( -2.032257487115171291, -4.571830348089889640, 4.991258216523934976 ) ) ;
#2651=CARTESIAN_POINT ( 'NONE',  ( -1.494593880360799432, -0.2610169491525428653, 3.295456077495951153 ) ) ;
#2652=CARTESIAN_POINT ( 'NONE',  ( -1.213493134184840727, -3.314262780522333696, 2.339799138571439396 ) ) ;
#2653=CARTESIAN_POINT ( 'NONE',  ( -1.458615186838411626, -5.103620102360555855, 3.259477383973569786 ) ) ;
#2654=CARTESIAN_POINT ( 'NONE',  ( -1.846259792136611066, -5.246610169491530584, 3.802221692020929744 ) ) ;
#2657=CARTESIAN_POINT ( 'NONE',  ( 2.058670345754650022, -5.350847457627120107, 3.559656372813920111 ) ) ;
#2660=CARTESIAN_POINT ( 'NONE',  ( -1.057242234132100167, -5.577754237288139905, 2.597442975781530272 ) ) ;
#2661=CARTESIAN_POINT ( 'NONE',  ( 1.930452136971109622, -4.012911429170968880, 6.521117305355573102 ) ) ;
#2663=CARTESIAN_POINT ( 'NONE',  ( 0.4114611322411816374, -1.032010528270079330, 6.711368086473216366 ) ) ;
#2667=ADVANCED_FACE ( 'NONE', ( #10522 ), #7020, .T. ) ;
#2669=CARTESIAN_POINT ( 'NONE',  ( -2.332582362116870200, -0.5313559322033900578, 4.387643303570819775 ) ) ;
#2670=CARTESIAN_POINT ( 'NONE',  ( -2.351526912647309953, -0.5269067796610169552, 4.606040641882809261 ) ) ;
#2671=CARTESIAN_POINT ( 'NONE',  ( 0.7678268402137939930, -2.867944426684879922, 6.924676972266129660 ) ) ;
#2674=CARTESIAN_POINT ( 'NONE',  ( 1.873832970144350130, -5.037500000000000533, 2.826167029855650270 ) ) ;
#2678=CARTESIAN_POINT ( 'NONE',  ( -0.6493550500446438889, -5.286652542372878294, 2.437955526623101665 ) ) ;
#2684=CARTESIAN_POINT ( 'NONE',  ( 1.315859850362970151, -5.328211948015590060, 2.737664967889629875 ) ) ;
#2687=CARTESIAN_POINT ( 'NONE',  ( 1.219286470748990103, -4.381683165423610582, 6.712979431025659416 ) ) ;
#2689=CARTESIAN_POINT ( 'NONE',  ( -2.002297259025881182, -3.287133615874059611, 5.153549919110945510 ) ) ;
#2697=CARTESIAN_POINT ( 'NONE',  ( -2.296954468777729463, -4.963890372630819670, 4.187412587068699565 ) ) ;
#2706=CARTESIAN_POINT ( 'NONE',  ( 1.994315313497110997, -5.086440677966105994, 5.187224322759965922 ) ) ;
#2709=CARTESIAN_POINT ( 'NONE',  ( 2.161103922260819044, -2.103271789531340641, 3.159628768708413915 ) ) ;
#2716=CARTESIAN_POINT ( 'NONE',  ( 1.115198193348289957, -1.261052534792989954, 6.772457159276550342 ) ) ;
#2717=CARTESIAN_POINT ( 'NONE',  ( -2.007801995112629356, -2.988226744486289999, 5.128524201241715375 ) ) ;
#2718=CARTESIAN_POINT ( 'NONE',  ( -1.641808337277740115, -0.1868644067796620123, 6.386111670537629514 ) ) ;
#2721=CARTESIAN_POINT ( 'NONE',  ( -2.328217775191430139, -0.5180084745762719711, 5.043379051721170292 ) ) ;
#2724=CARTESIAN_POINT ( 'NONE',  ( -0.06264882350515391107, -0.1512711864406779960, 7.052569299041220319 ) ) ;
#2725=CARTESIAN_POINT ( 'NONE',  ( 0.9170541073686970801, -1.284340823081270067, 6.867431071947180499 ) ) ;
#2730=CARTESIAN_POINT ( 'NONE',  ( 2.295719155670170153, -2.312866384125930264, 5.218091927917189565 ) ) ;
#2732=CARTESIAN_POINT ( 'NONE',  ( 1.031876288691629506, -5.430932203389830626, 7.145012538880298081 ) ) ;
#2735=CARTESIAN_POINT ( 'NONE',  ( 1.248294325655350034, -0.3266949152542379942, 2.704938983774300088 ) ) ;
#2740=CARTESIAN_POINT ( 'NONE',  ( 1.872456193198871022, -1.098034516774970770, 5.541908336565965598 ) ) ;
#2747=CARTESIAN_POINT ( 'NONE',  ( -0.9880847989278745969, -3.337551068810613142, 2.236912075639700515 ) ) ;
#2749=CARTESIAN_POINT ( 'NONE',  ( 0.4339619423229844619, -5.139830508474575232, 6.706578715862737461 ) ) ;
#2753=CARTESIAN_POINT ( 'NONE',  ( 2.253200202764419569, -0.08898305084745812554, 5.379408587037500133 ) ) ;
#2755=CARTESIAN_POINT ( 'NONE',  ( -0.9290506585603975909, -0.5829339996946386604, 2.210445150547709403 ) ) ;
#2759=CARTESIAN_POINT ( 'NONE',  ( 2.135041058613650122, -0.7991276453871950514, 5.690123914223769397 ) ) ;
#2764=CARTESIAN_POINT ( 'NONE',  ( 2.306642602145299925, -0.3845338983050849979, 5.166805192608480368 ) ) ;
#2765=CARTESIAN_POINT ( 'NONE',  ( -0.6918414964982418924, -3.659746228486680408, 2.450533167346770291 ) ) ;
#2768=CARTESIAN_POINT ( 'NONE',  ( 2.625437065641401446, -5.081991525423726230, 5.087214675345139270 ) ) ;
#2771=CARTESIAN_POINT ( 'NONE',  ( -2.203023580854000851, -5.242161016949149044, 3.872235369154300333 ) ) ;
#2775=CARTESIAN_POINT ( 'NONE',  ( 1.032615103526660416, -1.284340823081270733, 7.144753513336372208 ) ) ;
#2776=CARTESIAN_POINT ( 'NONE',  ( 0.2554393686801398333, -0.6247245358507580448, 2.048880876762550596 ) ) ;
#2777=CARTESIAN_POINT ( 'NONE',  ( 1.484081582636959551, -5.328211948015596278, 2.487334927317659705 ) ) ;
#2780=CARTESIAN_POINT ( 'NONE',  ( -1.286937324407759986, -3.589881363621809651, 2.729584305145209999 ) ) ;
#2783=CARTESIAN_POINT ( 'NONE',  ( -1.313542260532420292, -3.124115597856051085, 6.277817661335885369 ) ) ;
#2786=CARTESIAN_POINT ( 'NONE',  ( -0.1869574461324000070, -0.5962015548080630278, 2.350675676344399889 ) ) ;
#2794=CARTESIAN_POINT ( 'NONE',  ( -0.6493550500446439999, -5.286652542372879182, 2.437955526623099889 ) ) ;
#2795=CARTESIAN_POINT ( 'NONE',  ( -2.247144151254851341, -1.614217735477279536, 3.288101683376949413 ) ) ;
#2797=CARTESIAN_POINT ( 'NONE',  ( 1.708406120534559980, -0.7760574766851200401, 2.975829173059839849 ) ) ;
#2801=CARTESIAN_POINT ( 'NONE',  ( 2.126557263589630153, -2.448755237495689574, 3.691783806836010040 ) ) ;
#2802=CARTESIAN_POINT ( 'NONE',  ( -1.538437905835030595, -3.221109627369172390, 3.340547664492051094 ) ) ;
#2804=CARTESIAN_POINT ( 'NONE',  ( -2.332582362116870200, -0.2313559322033900134, 4.387643303570819775 ) ) ;
#2806=CARTESIAN_POINT ( 'NONE',  ( -0.4974685680287780354, -0.4601694915254240237, 7.000224381598740386 ) ) ;
#2811=CARTESIAN_POINT ( 'NONE',  ( -1.791574935211209807, -0.1913135593220340047, 6.226029630577610163 ) ) ;
#2812=CARTESIAN_POINT ( 'NONE',  ( -0.8001898266890440370, -1.470647129387580021, 6.913242401714570384 ) ) ;
#2816=CARTESIAN_POINT ( 'NONE',  ( 1.630481553867769495, -2.056695212954760432, 3.002862530617849579 ) ) ;
#2817=CARTESIAN_POINT ( 'NONE',  ( -2.011500846714319835, -5.551059322033900401, 3.478373409938470218 ) ) ;
#2820=CARTESIAN_POINT ( 'NONE',  ( -1.940327948426050941, -0.5091101694915260989, 5.370677689277675526 ) ) ;
#2825=CARTESIAN_POINT ( 'NONE',  ( 0.3943683997329633373, -2.215872354612800521, 2.685210827922638543 ) ) ;
#2832=CARTESIAN_POINT ( 'NONE',  ( -0.06367493584607197832, -5.598516949152545941, 2.649999999999998579 ) ) ;
#2833=VERTEX_POINT ( 'NONE', #4649 ) ;
#2835=CARTESIAN_POINT ( 'NONE',  ( -1.661700935788390066, -0.4124999999999999778, 3.038299064211610112 ) ) ;
#2836=CARTESIAN_POINT ( 'NONE',  ( -0.4617942143426889690, -0.5906145504024210569, 2.383143958488499692 ) ) ;
#2839=CARTESIAN_POINT ( 'NONE',  ( 1.092567884283869972, -0.9621456634052130141, 6.784476218553570526 ) ) ;
#2842=CARTESIAN_POINT ( 'NONE',  ( 0.9516466452860694591, -0.9621456634052125700, 6.519140045500582126 ) ) ;
#2847=DIRECTION ( 'NONE',  ( -0.06030856937325100586, -0.9963562379592471041, 0.06030856937324956257 ) ) ;
#2848=CARTESIAN_POINT ( 'NONE',  ( -1.811729841638700211, -0.5580508474576270084, 3.197954009834299782 ) ) ;
#2849=CARTESIAN_POINT ( 'NONE',  ( -2.143090896833110381, -0.5046610169491529962, 5.672454929438350391 ) ) ;
#2850=CARTESIAN_POINT ( 'NONE',  ( -1.816660071039029933, -3.170692174432619748, 6.196159040268240936 ) ) ;
#2853=CARTESIAN_POINT ( 'NONE',  ( -2.653602652190420574, -5.524364406779660897, 4.735326402787099376 ) ) ;
#2858=CARTESIAN_POINT ( 'NONE',  ( 1.610148362874519901, -0.7839942975846440065, 3.073126113101479984 ) ) ;
#2862=CARTESIAN_POINT ( 'NONE',  ( 2.650521604678268694, -1.004881363621820567, 4.833599835830299618 ) ) ;
#2864=CARTESIAN_POINT ( 'NONE',  ( 1.730954623551391736, -5.333856471231995577, 2.683219139909288842 ) ) ;
#2866=CARTESIAN_POINT ( 'NONE',  ( 2.033393610350129777, -0.8224159336754830463, 5.884928737465320303 ) ) ;
#2869=CARTESIAN_POINT ( 'NONE',  ( -0.04278372834682089842, -3.729611093351540063, 2.346934926511239805 ) ) ;
#2872=CARTESIAN_POINT ( 'NONE',  ( 0.8493734496528324573, -2.844656138396588929, 6.569081749323157915 ) ) ;
#2886=CARTESIAN_POINT ( 'NONE',  ( -1.965557623688110933, -5.211016949152535993, 5.292675575926340414 ) ) ;
#2887=CARTESIAN_POINT ( 'NONE',  ( -0.6890111762203582346, -1.800524041783588824, 2.137115435286770282 ) ) ;
#2891=CARTESIAN_POINT ( 'NONE',  ( 1.766949157924760261, -0.6011269801779139943, 2.938462914781730273 ) ) ;
#2897=CARTESIAN_POINT ( 'NONE',  ( 0.01716182025089369942, -2.169295778036230082, 2.346608583467340026 ) ) ;
#2899=CARTESIAN_POINT ( 'NONE',  ( 0.3681613504764975620, -3.477280798540335560, 2.680257674196191431 ) ) ;
#2901=CARTESIAN_POINT ( 'NONE',  ( -0.9150601050661559821, -0.1690677966101700180, 6.868218666554230190 ) ) ;
#2902=CARTESIAN_POINT ( 'NONE',  ( -0.003440977838559869991, -5.204536585018660233, 2.491636233962249758 ) ) ;
#2907=CARTESIAN_POINT ( 'NONE',  ( 2.318251751302029984, -0.06673728813559359763, 4.294764266798990704 ) ) ;
#2908=CARTESIAN_POINT ( 'NONE',  ( -1.381042549632419902, -1.540511994252449890, 6.605640880016140137 ) ) ;
#2911=CARTESIAN_POINT ( 'NONE',  ( -1.021156010535439584, -1.753947465207010614, 2.579625955254301051 ) ) ;
#2912=CARTESIAN_POINT ( 'NONE',  ( -2.540842781840720654, -5.511016949152534927, 5.466141598148674952 ) ) ;
#2917=CARTESIAN_POINT ( 'NONE',  ( -1.003115764947269950, -1.493935417675869903, 6.828967930617589666 ) ) ;
#2919=CARTESIAN_POINT ( 'NONE',  ( -1.695509042132779864, -0.5536016949152540167, 3.542446458728619518 ) ) ;
#2924=CARTESIAN_POINT ( 'NONE',  ( 1.019987577504959608, -2.821367850108300157, 6.481720287913791623 ) ) ;
#2926=CARTESIAN_POINT ( 'NONE',  ( 0.7322514394120266390, -0.3133474576271193524, 2.149183891723918993 ) ) ;
#2928=CARTESIAN_POINT ( 'NONE',  ( -1.505092429369619955, -5.128627060139309357, 2.879659483602799774 ) ) ;
#2932=CARTESIAN_POINT ( 'NONE',  ( -1.670747221194380128, -5.103620102360550526, 3.047345349617600174 ) ) ;
#2933=CARTESIAN_POINT ( 'NONE',  ( -2.052786957354850728, -5.524364406779660897, 4.727327971967373976 ) ) ;
#2936=CARTESIAN_POINT ( 'NONE',  ( 1.057242234132089731, -0.02224576271186470139, 2.597442975781520946 ) ) ;
#2937=CARTESIAN_POINT ( 'NONE',  ( 0.4974685680287860290, -5.439830508474580384, 7.000224381598740386 ) ) ;
#2943=CARTESIAN_POINT ( 'NONE',  ( -2.342931736853879787, -1.497776294035840117, 4.477701633099189671 ) ) ;
#2946=CARTESIAN_POINT ( 'NONE',  ( 0.9588981328681075444, -1.986830348089900777, 2.884671871696430578 ) ) ;
#2950=CARTESIAN_POINT ( 'NONE',  ( 1.689971836761019919, -5.333928624509660210, 3.010028163238979815 ) ) ;
#2951=CARTESIAN_POINT ( 'NONE',  ( -1.851400890972779045, -0.4868644067796619179, 6.601359968904141340 ) ) ;
#2953=CARTESIAN_POINT ( 'NONE',  ( -0.5320716618283710675, -3.007674156414609890, 6.992519451207139802 ) ) ;
#2956=CARTESIAN_POINT ( 'NONE',  ( 1.254903241568450900, -5.126483050847465250, 7.038391080368498365 ) ) ;
#2965=CARTESIAN_POINT ( 'NONE',  ( -0.6672256841320821641, -1.447358841099289251, 7.268642361138727637 ) ) ;
#2967=CARTESIAN_POINT ( 'NONE',  ( 1.449568901432419343, -5.037500000000000533, 3.250431098567584165 ) ) ;
#2970=CARTESIAN_POINT ( 'NONE',  ( 2.351999299633229956, -2.266289807549350055, 4.782734406438239994 ) ) ;
#2972=CARTESIAN_POINT ( 'NONE',  ( 0.1824815401350060040, -4.498124606865050445, 7.046368721022729709 ) ) ;
#2974=CARTESIAN_POINT ( 'NONE',  ( 2.053018524985070314, -4.125511994252439862, 4.695903819313355321 ) ) ;
#2983=EDGE_CURVE ( 'NONE', #15103, #17501, #15015, .T. ) ;
#2985=CARTESIAN_POINT ( 'NONE',  ( 1.940327948426050941, -5.390889830508485581, 5.370677689277660427 ) ) ;
#2993=CARTESIAN_POINT ( 'NONE',  ( -0.8429265834919730249, -2.076142624883080323, 2.502678798553459760 ) ) ;
#2994=CARTESIAN_POINT ( 'NONE',  ( -1.985741519624380835, -3.104668185927728974, 4.178720363079513334 ) ) ;
#2995=CARTESIAN_POINT ( 'NONE',  ( -2.143090896833110381, -0.2046610169491530073, 5.672454929438350391 ) ) ;
#2996=CARTESIAN_POINT ( 'NONE',  ( 0.009452071482871029010, -5.000192670742644729, 2.353323636140357333 ) ) ;
#2999=CARTESIAN_POINT ( 'NONE',  ( 0.1565249325564390115, -0.1468220338983060036, 7.048192310558509810 ) ) ;
#3000=CARTESIAN_POINT ( 'NONE',  ( -1.044181395669830259, -2.052854336594790219, 2.590869634085910089 ) ) ;
#3003=CARTESIAN_POINT ( 'NONE',  ( 2.111627294540149080, -3.710163681423230386, 3.660877362176660377 ) ) ;
#3005=CARTESIAN_POINT ( 'NONE',  ( -1.248294325655370018, -5.573305084745760141, 2.704938983774309857 ) ) ;
#3007=CARTESIAN_POINT ( 'NONE',  ( 1.202278654260740876, -0.4201271186440683758, 6.364093491318035589 ) ) ;
#3011=CARTESIAN_POINT ( 'NONE',  ( 2.048006021857541548, -2.541908390648840665, 4.556566471620634218 ) ) ;
#3012=CARTESIAN_POINT ( 'NONE',  ( 1.800129581279440893, -0.3355932203389832558, 2.750028594811110061 ) ) ;
#3017=CARTESIAN_POINT ( 'NONE',  ( 2.293398556041700065, -5.364194915254239859, 4.171956209133470317 ) ) ;
#3021=CARTESIAN_POINT ( 'NONE',  ( -2.311987889326990064, -1.521064582324129999, 4.260161748947139948 ) ) ;
#3023=CARTESIAN_POINT ( 'NONE',  ( 0.2739924515130530702, -2.615614131873680748, 6.734657214162127481 ) ) ;
#3028=( GEOMETRIC_REPRESENTATION_CONTEXT ( 3 ) GLOBAL_UNCERTAINTY_ASSIGNED_CONTEXT ( ( #15484 ) ) GLOBAL_UNIT_ASSIGNED_CONTEXT ( ( #10944, #12592, #3895 ) ) REPRESENTATION_CONTEXT ( 'NONE', 'WORKASPACE' ) );
#3030=CARTESIAN_POINT ( 'NONE',  ( 0.6640878839024751956, -0.4379237288135597317, 7.269405042592523181 ) ) ;
#3032=CARTESIAN_POINT ( 'NONE',  ( -1.951437470830620136, -5.057043525783970317, 3.384463041838880137 ) ) ;
#3036=CARTESIAN_POINT ( 'NONE',  ( -2.130266475405059090, -5.255508474576275901, 3.117337770017961418 ) ) ;
#3043=CARTESIAN_POINT ( 'NONE',  ( 1.256119432346080478, -1.261052534792989288, 7.037793332329536966 ) ) ;
#3045=CARTESIAN_POINT ( 'NONE',  ( 0.5843165771433389555, -0.3612150962701970447, 2.403837883145309995 ) ) ;
#3047=CARTESIAN_POINT ( 'NONE',  ( -1.397172971746989845, -1.707370888630439953, 2.806153814454939610 ) ) ;
#3049=CARTESIAN_POINT ( 'NONE',  ( -1.630481553867809907, -3.543304787045240101, 3.002862530617889547 ) ) ;
#3051=CARTESIAN_POINT ( 'NONE',  ( -0.4114611322411360628, -4.567989471729919870, 6.711368086473216366 ) ) ;
#3055=ORIENTED_EDGE ( 'NONE', *, *, #1335, .F. ) ;
#3062=CARTESIAN_POINT ( 'NONE',  ( -2.041338374031088865, -5.519915254237295343, 4.918217215283674726 ) ) ;
#3063=CARTESIAN_POINT ( 'NONE',  ( 2.049607015837390911, -2.429307825567371459, 6.385889905549011480 ) ) ;
#3067=CARTESIAN_POINT ( 'NONE',  ( -0.1914205519645679199, -4.981295943764795453, 2.049234377954000319 ) ) ;
#3070=CARTESIAN_POINT ( 'NONE',  ( 1.962536940652990003, -2.704926408666860294, 5.998920491814760503 ) ) ;
#3071=CARTESIAN_POINT ( 'NONE',  ( 2.041954431566909367, -3.849893411152959910, 4.912894203848615859 ) ) ;
#3072=CARTESIAN_POINT ( 'NONE',  ( -0.7093417302541390468, -0.1646186440677969987, 6.943956659919700236 ) ) ;
#3077=CARTESIAN_POINT ( 'NONE',  ( -1.991177874369409961, -3.221109627369172390, 2.945484578117480989 ) ) ;
#3078=CARTESIAN_POINT ( 'NONE',  ( 1.980638384804650931, -0.06228813559322075172, 4.159858630563753934 ) ) ;
#3079=CARTESIAN_POINT ( 'NONE',  ( 2.075124426334590044, -2.681638120378570189, 5.810227140144509583 ) ) ;
#3083=CARTESIAN_POINT ( 'NONE',  ( 0.8001898266890952183, -4.129352870612411408, 6.913242401714550844 ) ) ;
#3085=CARTESIAN_POINT ( 'NONE',  ( -0.6640878839024662028, -5.162076271186444743, 7.269405042592523181 ) ) ;
#3088=CARTESIAN_POINT ( 'NONE',  ( 1.980638384804650931, -0.3622881355932213721, 4.159858630563753934 ) ) ;
#3093=CARTESIAN_POINT ( 'NONE',  ( -1.079900583135680714, -2.029566048306499670, 2.953942563037710300 ) ) ;
#3099=CARTESIAN_POINT ( 'NONE',  ( 1.791574935211219799, -5.408686440677969998, 6.226029630577610163 ) ) ;
#3100=CARTESIAN_POINT ( 'NONE',  ( -0.9150601050661557601, -0.1690677966101701013, 6.868218666554229301 ) ) ;
#3101=CARTESIAN_POINT ( 'NONE',  ( -0.1471036068827911436, -0.2965485159365571777, 2.649244128781490737 ) ) ;
#3104=CARTESIAN_POINT ( 'NONE',  ( 0.8934014991060330590, -0.9854339516935011201, 6.877287176483390496 ) ) ;
#3106=CARTESIAN_POINT ( 'NONE',  ( -1.472933559740131626, -2.848497014756559143, 6.130163826706357177 ) ) ;
#3110=CARTESIAN_POINT ( 'NONE',  ( 0.1765068388402390998, -0.4468220338983063811, 7.347961541693647902 ) ) ;
#3111=CARTESIAN_POINT ( 'NONE',  ( -1.092567884283820012, -4.637854336594780413, 6.784476218553590066 ) ) ;
#3114=CARTESIAN_POINT ( 'NONE',  ( 2.286166334984490067, -5.086440677966099777, 5.258525443163859947 ) ) ;
#3120=CARTESIAN_POINT ( 'NONE',  ( 2.174104834890520976, -1.144611093351550091, 6.221966445066246187 ) ) ;
#3122=CARTESIAN_POINT ( 'NONE',  ( 0.2254033459420760055, -0.6247245358507570456, 2.348900562125120217 ) ) ;
#3125=CARTESIAN_POINT ( 'NONE',  ( -0.9719602541832299547, -2.755343861603410271, 6.843370931913550059 ) ) ;
#3126=CARTESIAN_POINT ( 'NONE',  ( 0.5677251586959709551, -5.311531839079339790, 2.399563163165729929 ) ) ;
#3127=CARTESIAN_POINT ( 'NONE',  ( 2.629224451638851434, -0.9583047870452394701, 4.339039509243856507 ) ) ;
#3129=CARTESIAN_POINT ( 'NONE',  ( -1.886482464143629967, -5.010466949207390108, 3.890008792968694618 ) ) ;
#3131=CARTESIAN_POINT ( 'NONE',  ( -0.4974685680287780354, -0.4601694915254240237, 7.000224381598740386 ) ) ;
#3139=CARTESIAN_POINT ( 'NONE',  ( 1.795861365445541091, -5.350847457627126325, 3.705232155007893713 ) ) ;
#3140=CARTESIAN_POINT ( 'NONE',  ( 0.6015868932280445947, -2.592325843585391532, 7.284803068494412948 ) ) ;
#3150=CARTESIAN_POINT ( 'NONE',  ( -0.5320716618283710675, -3.007674156414609890, 6.992519451207139802 ) ) ;
#3151=CARTESIAN_POINT ( 'NONE',  ( -0.4365326870213908639, -4.269082600342137823, 6.706076034398992469 ) ) ;
#3152=CARTESIAN_POINT ( 'NONE',  ( 0.5137283630188955730, -0.1379237288135599648, 6.687652957477222770 ) ) ;
#3159=CARTESIAN_POINT ( 'NONE',  ( -1.256119432346030962, -4.338947465207014353, 7.037793332329566276 ) ) ;
#3160=CARTESIAN_POINT ( 'NONE',  ( 0.5664586606772286093, -0.3133474576271193524, 2.726727161522279452 ) ) ;
#3161=CARTESIAN_POINT ( 'NONE',  ( 0.7678268402137939930, -2.867944426684879922, 6.924676972266129660 ) ) ;
#3168=CARTESIAN_POINT ( 'NONE',  ( 0.4201920264139499817, -3.477280798540341333, 2.384360920086630031 ) ) ;
#3169=SHAPE_DEFINITION_REPRESENTATION ( #4014, #4513 ) ;
#3170=CARTESIAN_POINT ( 'NONE',  ( -1.407651048079459288, -5.573305084745765470, 2.450250343405070641 ) ) ;
#3176=CARTESIAN_POINT ( 'NONE',  ( 2.340070819011249803, -0.3800847457627120063, 4.950151441910540129 ) ) ;
#3182=CARTESIAN_POINT ( 'NONE',  ( -0.8259795455965642796, -3.054250732991181216, 6.579537079411896805 ) ) ;
#3183=CARTESIAN_POINT ( 'NONE',  ( 2.560337424259670591, -0.3622881355932213721, 4.001768473655590519 ) ) ;
#3187=DIRECTION ( 'NONE',  ( 0.000000000000000000, -1.000000000000000000, 0.000000000000000000 ) ) ;
#3192=CARTESIAN_POINT ( 'NONE',  ( -2.041338374031088865, -5.519915254237295343, 4.918217215283674726 ) ) ;
#3194=CARTESIAN_POINT ( 'NONE',  ( -1.925796468768789405, -0.1957627118644069963, 6.052706598917718672 ) ) ;
#3195=CARTESIAN_POINT ( 'NONE',  ( 2.247144151254821143, -3.985782264522713447, 3.288101683376901452 ) ) ;
#3199=CARTESIAN_POINT ( 'NONE',  ( -0.7678268402137429227, -2.732055573315119723, 6.924676972266150088 ) ) ;
#3202=CARTESIAN_POINT ( 'NONE',  ( -1.893291846171410331, -2.941650167909708458, 5.493944474033886749 ) ) ;
#3212=CARTESIAN_POINT ( 'NONE',  ( -1.747582379783008788, -5.184322033898315141, 6.697200745122486865 ) ) ;
#3222=CARTESIAN_POINT ( 'NONE',  ( -0.2266049403550400299, -2.146007489747939090, 2.055805624768001216 ) ) ;
#3225=CARTESIAN_POINT ( 'NONE',  ( 0.7435598031058590074, -2.569037555297100095, 6.932904947974519949 ) ) ;
#3227=CARTESIAN_POINT ( 'NONE',  ( 1.315859850362970151, -5.328211948015590060, 2.737664967889629875 ) ) ;
#3228=( BOUNDED_SURFACE ( )  B_SPLINE_SURFACE ( 3, 3, ( 
 ( #4196, #9856, #5411, #16794, #7088, #6977, #12625, #15514, #11337, #8288, #4284, #14537, #18250, #4611, #15332, #15603, #1246, #4008, #14100, #5600, #16888, #2639, #11244, #48, #8462, #11138, #5691, #4107, #10269, #6802, #12450, #2917, #8562, #15940, #13929, #6888, #14208, #12536, #18148, #9763, #15428, #1770, #7417, #377, #4795, #16199, #17475, #13517, #7681, #10446, #14813, #16383, #13418, #1855, #11939, #16027, #16107, #10535, #10649, #14620, #7584, #4887, #555, #3403, #14910, #8972, #6199, #3689, #4995, #11857, #7865, #13325, #6475, #3508, #833, #13147, #459, #10362, #4713, #2124, #6101, #9051, #9336, #732, #12135, #13236, #3327, #7774, #6280, #17755, #16294, #5086, #1934, #6367, #14708, #2026, #641, #10736, #12034, #7500, #17655, #17556, #3600, #9152, #9247, #2219, #11764, #17392, #3788, #18195, #9446, #15380, #15109, #1289, #2421, #13785, #9620, #17937, #6849, #10829, #5279, #16472, #2321, #8335, #13885, #8149, #12579, #1019, #13968, #8069, #15194, #6756, #13709, #5457, #12222, #6932, #1201, #15006, #6569, #17838, #930, #15280, #7971, #16578, #2589, #4150, #2502, #3883, #5176, #1109, #18110, #12494, #13619, #3968, #5552, #12406, #11098, #6656, #12314, #16745, #11196, #18028, #16839, #10930, #9535, #5375, #11013, #8240, #16661, #4058, #9713, #12857, #11640, #13037, #1567, #4326, #4425, #168, #7037, #14425, #9992, #15466, #14161, #5816, #15738, #7212, #5911, #3 ),
 ( #17011, #15816, #7398, #14250, #9898, #9809, #17101, #8773, #5732, #5997, #2862, #12772, #16928, #15656, #1651, #10086, #3120, #358, #17185, #85, #11466, #3043, #2775, #14056, #1373, #7138, #12681, #5644, #8683, #2965, #11287, #15556, #4237, #8510, #1480, #14330, #12946, #11552, #8606, #273, #4507, #9127, #7842, #2099, #7750, #6082, #17458, #4776, #15911, #10427, #16090, #4867, #17366, #14599, #16011, #2002, #6259, #7659, #13303, #3222, #8869, #7564, #1915, #622, #10344, #6177, #17627, #11732, #3311, #806, #13396, #8954, #10622, #3385, #9220, #11919, #16270, #14518, #1837, #13130, #7480, #10512, #442, #11835, #6447, #16176, #3573, #13211, #4691, #3481, #9030, #2198, #710, #14884, #530, #14783, #14686, #17538, #6345, #13489, #12008, #12114, #4966, #4583, #10242, #6633, #3761, #10804, #12290, #6548, #17817, #8315, #2398, #18091, #8047, #9688, #13688, #9515, #12387, #996, #9600, #17910, #5253, #10910, #16360, #5438, #16643, #15174, #15360, #2483, #11079, #8128, #13763, #6732, #5351, #10995, #3947, #15256, #2561, #8216, #13864, #1270, #1181, #6914, #6829, #12473, #3666, #6411, #9488, #15060, #17883, #17703, #2368, #1062, #3730, #882, #6704, #12175, #1158, #9663, #7815, #5329, #12361, #11053, #13461, #12452, #5221, #9290, #14952, #778, #10690, #17983, #2262, #17793, #5129, #16529, #10779, #13838, #970, #16425, #2459, #5034, #10974, #7915, #16620, #13565, #9392, #3923 ),
 ( #6607, #9576, #15235, #8189, #6805, #18069, #347, #5984, #11626, #9017, #14411, #10332, #7645, #16253, #14587, #15996, #17255, #7549, #4853, #609, #4572, #16076, #14768, #516, #10499, #10229, #15899, #6247, #2082, #8941, #13379, #17610, #694, #7470, #4949, #16158, #11821, #14506, #1827, #17445, #10602, #13118, #6164, #3299, #3372, #4763, #429, #6068, #10414, #11717, #17350, #3461, #9110, #4679, #17994, #12096, #14966, #8115, #2549, #8030, #9204, #2383, #5140, #3932, #13851, #13670, #3649, #11064, #10893, #8202, #17803, #18081, #2277, #6532, #10701, #16437, #13752, #3849, #15245, #9586, #10985, #12186, #982, #12276, #1169, #6815, #14868, #893, #13473, #5427, #15157, #15073, #17715, #9299, #12463, #7931, #16344, #16542, #6718, #5341, #6618, #13579, #17896, #1074, #3558, #12373, #16632, #5047, #3743, #9407, #2183, #5236, #9503, #2468, #10791, #7826, #789, #6427, #3077, #4459, #10116, #9675, #2652, #2747, #9777, #15768, #5512, #14364, #15347, #14027, #17300, #12985, #1786, #11155, #13941, #7341, #11257, #13072, #4536, #14465, #6902, #1690, #16807, #15439, #1341, #7430, #306, #390, #11584, #16901, #5945, #6995, #4120, #8392, #12642, #12552, #18161, #6029, #18267, #8814, #5614, #11675, #8720, #17215, #10189, #15853, #3159, #4628, #16708, #4020, #1259, #8303, #13814, #8088, #12777, #954, #15559, #9364, #15130, #6591, #15216, #2441, #3817, #12340, #1138, #16407, #12686, #11380 ),
 ( #13729, #2244, #12245, #10952, #2523, #6682, #11293, #5111, #7997, #7042, #14166, #1045, #7891, #17961, #16504, #2866, #7141, #5307, #15034, #4330, #3903, #1485, #10858, #17014, #13644, #17866, #3712, #9467, #8, #8170, #8516, #92, #4240, #5205, #16601, #9558, #5736, #14934, #13542, #5649, #6500, #860, #16930, #9902, #10763, #2347, #12161, #17777, #4430, #17269, #13133, #11737, #8776, #3047, #14429, #14521, #13214, #7485, #445, #11470, #4511, #10162, #11557, #8687, #15915, #14334, #8958, #17461, #9996, #6086, #8873, #535, #15661, #1918, #1754, #5819, #17105, #2970, #172, #1841, #10089, #7301, #12950, #6000, #276, #3315, #15820, #5916, #4589, #6183, #3225, #8611, #7402, #15741, #17188, #362, #17372, #1654, #3125, #13040, #11643, #10248, #4695, #10348, #16014, #11839, #14603, #7568, #14254, #1572, #7218, #12861, #10807, #16093, #3389, #13309, #7663, #5065, #9034, #6348, #998, #16365, #16453, #16179, #625, #10716, #9225, #2402, #913, #3765, #6262, #3669, #3485, #14788, #12012, #9426, #9316, #15090, #2298, #14888, #14987, #17632, #9130, #2103, #4970, #11924, #17541, #8049, #4870, #5157, #10517, #13690, #7754, #3577, #17737, #13399, #7951, #714, #10626, #16274, #10431, #6635, #13598, #2201, #12293, #7845, #4780, #13495, #810, #6451, #6551, #12117, #12203, #17820, #14690, #2007, #15452, #14137, #6832, #4221, #2485, #14040, #12389, #3864, #6916, #12476, #9690, #15176 ),
 ( #18094, #9881, #8130, #1356, #18008, #9518, #12564, #5441, #15362, #13765, #11081, #5528, #1183, #16646, #11171, #3950, #16912, #7116, #17913, #7012, #16821, #2842, #5256, #15541, #2663, #6734, #5355, #10912, #10997, #4133, #9602, #15259, #2564, #13954, #8218, #11271, #16723, #13866, #18176, #1461, #9791, #16556, #8318, #4036, #12661, #18284, #5627, #8491, #153, #15798, #11446, #14315, #7465, #1551, #17080, #8935, #15890, #4409, #424, #5893, #17342, #14404, #6060, #5716, #11362, #2946, #15638, #13019, #16995, #1637, #14583, #5979, #11709, #5799, #8586, #342, #17170, #10328, #8853, #4674, #14232, #11620, #10068, #15721, #7281, #15989, #17248, #3292, #10223, #4488, #4567, #12928, #3023, #8665, #254, #7198, #12839, #1899, #11536, #13113, #10142, #12756, #3106, #8754, #7381, #1731, #3202, #14499, #1821, #70, #4309, #9974, #6418, #685, #5132, #11900, #7919, #1977, #7728, #17519, #7818, #13372, #14761, #4940, #6241, #6520, #15064, #13187, #10693, #12087, #10783, #505, #17795, #17601, #3367, #9010, #6156, #16068, #17706, #14661, #4846, #10492, #3550, #16151, #885, #6323, #3452, #2176, #3734, #5037, #11814, #10592, #7638, #9100, #16245, #16336, #13284, #602, #9197, #2073, #11986, #2265, #14861, #13464, #9396, #3640, #14955, #13570, #12178, #16428, #17439, #4757, #10407, #13661, #10880, #5225, #2646, #6610, #3927, #16895, #13934, #14020, #13746, #16533, #8296, #6809, #18259, #16800 ),
 ( #1336, #1252, #12632, #18155, #12456, #6895, #9580, #1065, #6709, #15239, #3841, #9493, #5606, #15151, #2740, #2462, #6984, #8109, #1163, #15339, #5333, #12545, #12366, #10978, #17987, #8020, #8385, #5501, #13842, #11251, #16626, #4203, #2541, #8193, #18072, #11146, #5420, #11058, #16704, #4114, #4013, #9771, #9862, #9667, #2372, #15434, #973, #12268, #17887, #4471, #10047, #7265, #12735, #15701, #3093, #17062, #14214, #8736, #15521, #323, #14380, #407, #2825, #7448, #12908, #11343, #16978, #8471, #5699, #1708, #4290, #12823, #136, #11521, #5784, #8835, #3011, #11426, #10128, #11693, #7360, #14109, #233, #9949, #4389, #5874, #5961, #15613, #2924, #17149, #1534, #8653, #10204, #8568, #7183, #17321, #11601, #14299, #3182, #1622, #1805, #15784, #14484, #1437, #7096, #13001, #53, #17231, #4550, #15871, #4651, #13090, #6047, #3352, #488, #16225, #14743, #7894, #6393, #3625, #6135, #10569, #8995, #1957, #11884, #9275, #3533, #2246, #7799, #2057, #9180, #17504, #14644, #7617, #4823, #11799, #17420, #13546, #4740, #10675, #10390, #14936, #16054, #9081, #4913, #13265, #2158, #586, #6225, #10474, #15973, #16320, #14843, #3429, #863, #16131, #6503, #7711, #13355, #669, #13447, #6307, #11965, #17580, #759, #12063, #17683, #12163, #5020, #17779, #13171, #10309, #3276, #14565, #8917, #1879, #7527, #2351, #5310, #11037, #6686, #3821, #16685, #9471, #4088, #12609, #15132, #3993 ),
 ( #5483, #15412, #9560, #5208, #5113, #12434, #9747, #1047, #1313, #16507, #8090, #12247, #17964, #15314, #5397, #16773, #11125, #12520, #13731, #15219, #13817, #2716, #8361, #10766, #2443, #15038, #6960, #9647, #16605, #13646, #10860, #13994, #12342, #17869, #18052, #8275, #6874, #3905, #10956, #2525, #2624, #16409, #13916, #1229, #6593, #8172, #1141, #3714, #6786, #18133, #9366, #8000, #956, #11320, #15683, #1601, #2993, #8633, #16871, #4179, #2897, #9923, #14278, #5676, #10024, #7072, #8714, #15492, #5938, #17128, #18228, #9838, #2801, #8446, #202, #5582, #1511, #5846, #7425, #5762, #7164, #14080, #17036, #3070, #10111, #11226, #7244, #11576, #11404, #14358, #1408, #12714, #4453, #17208, #116, #4531, #3150, #10183, #16956, #15848, #11497, #12885, #31, #4264, #15763, #1777, #8806, #1682, #12802, #7331, #12977, #15585, #14458, #4361, #8546, #14193, #299, #6284, #4800, #9156, #17480, #10653, #14819, #6373, #8893, #13334, #6109, #4717, #14624, #12040, #11944, #5002, #10542, #10451, #17561, #1939, #11772, #17399, #7591, #14542, #1858, #16300, #7505, #13424, #465, #17662, #10367, #11863, #7688, #16032, #4892, #3332, #8977, #13241, #385, #738, #16204, #6207, #3606, #563, #9256, #16112, #3409, #9058, #3513, #14714, #2033, #2133, #14914, #2223, #13065, #6025, #11670, #17293, #15949, #4621, #10280, #3249, #15200, #2428, #17941, #5091, #8073, #13794, #9453, #6574, #1119, #12228 ) ),
 .UNSPECIFIED., .T., .F., .F. ) 
 B_SPLINE_SURFACE_WITH_KNOTS ( ( 4, 3, 4 ),
 ( 4, 1, 1, 1, 1, 1, 1, 1, 1, 1, 1, 1, 1, 1, 1, 1, 1, 1, 1, 1, 1, 1, 1, 1, 1, 1, 1, 1, 1, 1, 1, 1, 1, 1, 1, 1, 1, 1, 1, 1, 1, 1, 1, 1, 1, 1, 1, 1, 1, 1, 1, 1, 1, 1, 1, 1, 1, 1, 1, 1, 1, 1, 1, 1, 1, 1, 1, 1, 1, 1, 1, 1, 1, 1, 1, 1, 1, 1, 1, 1, 1, 1, 1, 1, 1, 1, 1, 1, 1, 1, 1, 1, 1, 1, 1, 1, 1, 1, 1, 1, 1, 1, 1, 1, 1, 1, 1, 1, 1, 1, 1, 1, 1, 1, 1, 1, 1, 1, 1, 1, 1, 1, 1, 1, 1, 1, 1, 1, 1, 1, 1, 1, 1, 1, 1, 1, 1, 1, 1, 1, 1, 1, 1, 1, 1, 1, 1, 1, 1, 1, 1, 1, 1, 1, 1, 1, 1, 1, 1, 1, 1, 1, 1, 1, 1, 1, 1, 1, 1, 1, 1, 1, 1, 1, 1, 1, 1, 1, 1, 1, 1, 1, 1, 1, 1, 4 ),
 ( 0.000000000000000000, 3.141592653589790007, 6.283185307179590673 ),
 ( 0.7853981633974479459, 0.8787968639095770085, 0.9721955644217059600, 1.065594264933839908, 1.158992965445959866, 1.252391665958090039, 1.345790366470219990, 1.439189066982349940, 1.532587767494480113, 1.625986468006610064, 1.719385168518740015, 1.812783869030869965, 1.906182569543000138, 1.999581270055129867, 2.092979970567249826, 2.186378671079379998, 2.279777371591510171, 2.373176072103639900, 2.466574772615769628, 2.559973473127900245, 2.653372173640029974, 2.746770874152160147, 2.840169574664289875, 2.933568275176409834, 3.026966975688540007, 3.120365676200670180, 3.213764376712799908, 3.307163077224930081, 3.400561777737059810, 3.493960478249190427, 3.587359178761320155, 3.680757879273439670, 3.774156579785570287, 3.867555280297700016, 3.960953980809830188, 4.054352681321960361, 4.147751381834090090, 4.241150082346219818, 4.334548782858350435, 4.427947483370480164, 4.521346183882600123, 4.614744884394729851, 4.708143584906859580, 4.801542285418989309, 4.894940985931119926, 4.988339686443250542, 5.081738386955380271, 5.175137087467510000, 5.268535787979639728, 5.361934488491760575, 5.455333189003890304, 5.548731889516020033, 5.642130590028149761, 5.735529290540279490, 5.828927991052410107, 5.922326691564539836, 6.015725392076670452, 6.109124092588789523, 6.202522793100920140, 6.295921493613049869, 6.389320194125180485, 6.482718894637310214, 6.576117595149439943, 6.669516295661569671, 6.762914996173699400, 6.856313696685830017, 6.949712397197949976, 7.043111097710079704, 7.136509798222209433, 7.229908498734340050, 7.323307199246470667, 7.416705899758600395, 7.510104600270730124, 7.603503300782859853, 7.696902001294989581, 7.790300701807110428, 7.883699402319240157, 7.977098102831369886, 8.070496803343500503, 8.163895503855631119, 8.257294204367759960, 8.350692904879890577, 8.444091605392019417, 8.537490305904139376, 8.630889006416269993, 8.724287706928398833, 8.817686407440529450, 8.911085107952660067, 9.004483808464788908, 9.097882508976921301, 9.191281209489050141, 9.284679910001178982, 9.378078610513298941, 9.471477311025429557, 9.564876011537560174, 9.658274712049690791, 9.751673412561819632, 9.845072113073950248, 9.938470813586080865, 10.03186951409819905, 10.12526821461029947, 10.21866691512249936, 10.31206561563459978, 10.40546431614669842, 10.49886301665890009, 10.59226171717100051, 10.68566041768310093, 10.77905911819519957, 10.87245781870739947, 10.96585651921949989, 11.05925521973160031, 11.15265392024380020, 11.24605262075590062, 11.33945132126800104, 11.43285002178009968, 11.52624872229229958, 11.61964742280439999, 11.71304612331650041, 11.80644482382869853, 11.89984352434079895, 11.99324222485290115, 12.08664092536500156, 12.18003962587719968, 12.27343832638930010, 12.36683702690140052, 12.46023572741360042, 12.55363442792569906, 12.64703312843779948, 12.74043182894989990, 12.83383052946209979, 12.92722922997419843, 13.02062793048630063, 13.11402663099850052, 13.20742533151059916, 13.30082403202269958, 13.39422273253480000, 13.48762143304700167, 13.58102013355910032, 13.67441883407120073, 13.76781753458340063, 13.86121623509549927, 13.95461493560759969, 14.04801363611970011, 14.14141233663190000, 14.23481103714399865, 14.32820973765609907, 14.42160843816829896, 14.51500713868040116, 14.60840583919249980, 14.70180453970460022, 14.79520324021680011, 14.88860194072889875, 14.98200064124100095, 15.07539934175320084, 15.16879804226530126, 15.26219674277739990, 15.35559544328959980, 15.44899414380170022, 15.54239284431380064, 15.63579154482589928, 15.72919024533809917, 15.82258894585019959, 15.91598764636230001, 16.00938634687449991, 16.10278504738660033, 16.19618374789869719, 16.28958244841080116, 16.38298114892299751, 16.47637984943510148, 16.56977854994720190, 16.66317725045940179, 16.75657595097149866, 16.84997465148359908, 16.94337335199570305, 17.03677205250789939, 17.13017075301999981, 17.22356945353210023, 17.31696815404430012, 17.41036685455640054, 17.50376555506850096, 17.59716425558059782, 17.69056295609280127, 17.78396165660489814, 17.87736035711699856, 17.97075905762920200, 18.06415775814129887 ),
 .UNSPECIFIED. ) 
 GEOMETRIC_REPRESENTATION_ITEM ( )  RATIONAL_B_SPLINE_SURFACE ( (
 ( 1.000000000000000000, 1.000000000000000000, 1.000000000000000000, 1.000000000000000000, 1.000000000000000000, 1.000000000000000000, 1.000000000000000000, 1.000000000000000000, 1.000000000000000000, 1.000000000000000000, 1.000000000000000000, 1.000000000000000000, 1.000000000000000000, 1.000000000000000000, 1.000000000000000000, 1.000000000000000000, 1.000000000000000000, 1.000000000000000000, 1.000000000000000000, 1.000000000000000000, 1.000000000000000000, 1.000000000000000000, 1.000000000000000000, 1.000000000000000000, 1.000000000000000000, 1.000000000000000000, 1.000000000000000000, 1.000000000000000000, 1.000000000000000000, 1.000000000000000000, 1.000000000000000000, 1.000000000000000000, 1.000000000000000000, 1.000000000000000000, 1.000000000000000000, 1.000000000000000000, 1.000000000000000000, 1.000000000000000000, 1.000000000000000000, 1.000000000000000000, 1.000000000000000000, 1.000000000000000000, 1.000000000000000000, 1.000000000000000000, 1.000000000000000000, 1.000000000000000000, 1.000000000000000000, 1.000000000000000000, 1.000000000000000000, 1.000000000000000000, 1.000000000000000000, 1.000000000000000000, 1.000000000000000000, 1.000000000000000000, 1.000000000000000000, 1.000000000000000000, 1.000000000000000000, 1.000000000000000000, 1.000000000000000000, 1.000000000000000000, 1.000000000000000000, 1.000000000000000000, 1.000000000000000000, 1.000000000000000000, 1.000000000000000000, 1.000000000000000000, 1.000000000000000000, 1.000000000000000000, 1.000000000000000000, 1.000000000000000000, 1.000000000000000000, 1.000000000000000000, 1.000000000000000000, 1.000000000000000000, 1.000000000000000000, 1.000000000000000000, 1.000000000000000000, 1.000000000000000000, 1.000000000000000000, 1.000000000000000000, 1.000000000000000000, 1.000000000000000000, 1.000000000000000000, 1.000000000000000000, 1.000000000000000000, 1.000000000000000000, 1.000000000000000000, 1.000000000000000000, 1.000000000000000000, 1.000000000000000000, 1.000000000000000000, 1.000000000000000000, 1.000000000000000000, 1.000000000000000000, 1.000000000000000000, 1.000000000000000000, 1.000000000000000000, 1.000000000000000000, 1.000000000000000000, 1.000000000000000000, 1.000000000000000000, 1.000000000000000000, 1.000000000000000000, 1.000000000000000000, 1.000000000000000000, 1.000000000000000000, 1.000000000000000000, 1.000000000000000000, 1.000000000000000000, 1.000000000000000000, 1.000000000000000000, 1.000000000000000000, 1.000000000000000000, 1.000000000000000000, 1.000000000000000000, 1.000000000000000000, 1.000000000000000000, 1.000000000000000000, 1.000000000000000000, 1.000000000000000000, 1.000000000000000000, 1.000000000000000000, 1.000000000000000000, 1.000000000000000000, 1.000000000000000000, 1.000000000000000000, 1.000000000000000000, 1.000000000000000000, 1.000000000000000000, 1.000000000000000000, 1.000000000000000000, 1.000000000000000000, 1.000000000000000000, 1.000000000000000000, 1.000000000000000000, 1.000000000000000000, 1.000000000000000000, 1.000000000000000000, 1.000000000000000000, 1.000000000000000000, 1.000000000000000000, 1.000000000000000000, 1.000000000000000000, 1.000000000000000000, 1.000000000000000000, 1.000000000000000000, 1.000000000000000000, 1.000000000000000000, 1.000000000000000000, 1.000000000000000000, 1.000000000000000000, 1.000000000000000000, 1.000000000000000000, 1.000000000000000000, 1.000000000000000000, 1.000000000000000000, 1.000000000000000000, 1.000000000000000000, 1.000000000000000000, 1.000000000000000000, 1.000000000000000000, 1.000000000000000000, 1.000000000000000000, 1.000000000000000000, 1.000000000000000000, 1.000000000000000000, 1.000000000000000000, 1.000000000000000000, 1.000000000000000000, 1.000000000000000000, 1.000000000000000000, 1.000000000000000000, 1.000000000000000000, 1.000000000000000000, 1.000000000000000000, 1.000000000000000000, 1.000000000000000000, 1.000000000000000000, 1.000000000000000000, 1.000000000000000000, 1.000000000000000000, 1.000000000000000000, 1.000000000000000000, 1.000000000000000000, 1.000000000000000000, 1.000000000000000000, 1.000000000000000000, 1.000000000000000000),
 ( 0.3333333333333329818, 0.3333333333333329818, 0.3333333333333329818, 0.3333333333333329818, 0.3333333333333329818, 0.3333333333333329818, 0.3333333333333329818, 0.3333333333333329818, 0.3333333333333329818, 0.3333333333333329818, 0.3333333333333329818, 0.3333333333333329818, 0.3333333333333329818, 0.3333333333333329818, 0.3333333333333329818, 0.3333333333333329818, 0.3333333333333329818, 0.3333333333333329818, 0.3333333333333329818, 0.3333333333333329818, 0.3333333333333329818, 0.3333333333333329818, 0.3333333333333329818, 0.3333333333333329818, 0.3333333333333329818, 0.3333333333333329818, 0.3333333333333329818, 0.3333333333333329818, 0.3333333333333329818, 0.3333333333333329818, 0.3333333333333329818, 0.3333333333333329818, 0.3333333333333329818, 0.3333333333333329818, 0.3333333333333329818, 0.3333333333333329818, 0.3333333333333329818, 0.3333333333333329818, 0.3333333333333329818, 0.3333333333333329818, 0.3333333333333329818, 0.3333333333333329818, 0.3333333333333329818, 0.3333333333333329818, 0.3333333333333329818, 0.3333333333333329818, 0.3333333333333329818, 0.3333333333333329818, 0.3333333333333329818, 0.3333333333333329818, 0.3333333333333329818, 0.3333333333333329818, 0.3333333333333329818, 0.3333333333333329818, 0.3333333333333329818, 0.3333333333333329818, 0.3333333333333329818, 0.3333333333333329818, 0.3333333333333329818, 0.3333333333333329818, 0.3333333333333329818, 0.3333333333333329818, 0.3333333333333329818, 0.3333333333333329818, 0.3333333333333329818, 0.3333333333333329818, 0.3333333333333329818, 0.3333333333333329818, 0.3333333333333329818, 0.3333333333333329818, 0.3333333333333329818, 0.3333333333333329818, 0.3333333333333329818, 0.3333333333333329818, 0.3333333333333329818, 0.3333333333333329818, 0.3333333333333329818, 0.3333333333333329818, 0.3333333333333329818, 0.3333333333333329818, 0.3333333333333329818, 0.3333333333333329818, 0.3333333333333329818, 0.3333333333333329818, 0.3333333333333329818, 0.3333333333333329818, 0.3333333333333329818, 0.3333333333333329818, 0.3333333333333329818, 0.3333333333333329818, 0.3333333333333329818, 0.3333333333333329818, 0.3333333333333329818, 0.3333333333333329818, 0.3333333333333329818, 0.3333333333333329818, 0.3333333333333329818, 0.3333333333333329818, 0.3333333333333329818, 0.3333333333333329818, 0.3333333333333329818, 0.3333333333333329818, 0.3333333333333329818, 0.3333333333333329818, 0.3333333333333329818, 0.3333333333333329818, 0.3333333333333329818, 0.3333333333333329818, 0.3333333333333329818, 0.3333333333333329818, 0.3333333333333329818, 0.3333333333333329818, 0.3333333333333329818, 0.3333333333333329818, 0.3333333333333329818, 0.3333333333333329818, 0.3333333333333329818, 0.3333333333333329818, 0.3333333333333329818, 0.3333333333333329818, 0.3333333333333329818, 0.3333333333333329818, 0.3333333333333329818, 0.3333333333333329818, 0.3333333333333329818, 0.3333333333333329818, 0.3333333333333329818, 0.3333333333333329818, 0.3333333333333329818, 0.3333333333333329818, 0.3333333333333329818, 0.3333333333333329818, 0.3333333333333329818, 0.3333333333333329818, 0.3333333333333329818, 0.3333333333333329818, 0.3333333333333329818, 0.3333333333333329818, 0.3333333333333329818, 0.3333333333333329818, 0.3333333333333329818, 0.3333333333333329818, 0.3333333333333329818, 0.3333333333333329818, 0.3333333333333329818, 0.3333333333333329818, 0.3333333333333329818, 0.3333333333333329818, 0.3333333333333329818, 0.3333333333333329818, 0.3333333333333329818, 0.3333333333333329818, 0.3333333333333329818, 0.3333333333333329818, 0.3333333333333329818, 0.3333333333333329818, 0.3333333333333329818, 0.3333333333333329818, 0.3333333333333329818, 0.3333333333333329818, 0.3333333333333329818, 0.3333333333333329818, 0.3333333333333329818, 0.3333333333333329818, 0.3333333333333329818, 0.3333333333333329818, 0.3333333333333329818, 0.3333333333333329818, 0.3333333333333329818, 0.3333333333333329818, 0.3333333333333329818, 0.3333333333333329818, 0.3333333333333329818, 0.3333333333333329818, 0.3333333333333329818, 0.3333333333333329818, 0.3333333333333329818, 0.3333333333333329818, 0.3333333333333329818, 0.3333333333333329818, 0.3333333333333329818, 0.3333333333333329818, 0.3333333333333329818, 0.3333333333333329818, 0.3333333333333329818, 0.3333333333333329818, 0.3333333333333329818, 0.3333333333333329818),
 ( 0.3333333333333329818, 0.3333333333333329818, 0.3333333333333329818, 0.3333333333333329818, 0.3333333333333329818, 0.3333333333333329818, 0.3333333333333329818, 0.3333333333333329818, 0.3333333333333329818, 0.3333333333333329818, 0.3333333333333329818, 0.3333333333333329818, 0.3333333333333329818, 0.3333333333333329818, 0.3333333333333329818, 0.3333333333333329818, 0.3333333333333329818, 0.3333333333333329818, 0.3333333333333329818, 0.3333333333333329818, 0.3333333333333329818, 0.3333333333333329818, 0.3333333333333329818, 0.3333333333333329818, 0.3333333333333329818, 0.3333333333333329818, 0.3333333333333329818, 0.3333333333333329818, 0.3333333333333329818, 0.3333333333333329818, 0.3333333333333329818, 0.3333333333333329818, 0.3333333333333329818, 0.3333333333333329818, 0.3333333333333329818, 0.3333333333333329818, 0.3333333333333329818, 0.3333333333333329818, 0.3333333333333329818, 0.3333333333333329818, 0.3333333333333329818, 0.3333333333333329818, 0.3333333333333329818, 0.3333333333333329818, 0.3333333333333329818, 0.3333333333333329818, 0.3333333333333329818, 0.3333333333333329818, 0.3333333333333329818, 0.3333333333333329818, 0.3333333333333329818, 0.3333333333333329818, 0.3333333333333329818, 0.3333333333333329818, 0.3333333333333329818, 0.3333333333333329818, 0.3333333333333329818, 0.3333333333333329818, 0.3333333333333329818, 0.3333333333333329818, 0.3333333333333329818, 0.3333333333333329818, 0.3333333333333329818, 0.3333333333333329818, 0.3333333333333329818, 0.3333333333333329818, 0.3333333333333329818, 0.3333333333333329818, 0.3333333333333329818, 0.3333333333333329818, 0.3333333333333329818, 0.3333333333333329818, 0.3333333333333329818, 0.3333333333333329818, 0.3333333333333329818, 0.3333333333333329818, 0.3333333333333329818, 0.3333333333333329818, 0.3333333333333329818, 0.3333333333333329818, 0.3333333333333329818, 0.3333333333333329818, 0.3333333333333329818, 0.3333333333333329818, 0.3333333333333329818, 0.3333333333333329818, 0.3333333333333329818, 0.3333333333333329818, 0.3333333333333329818, 0.3333333333333329818, 0.3333333333333329818, 0.3333333333333329818, 0.3333333333333329818, 0.3333333333333329818, 0.3333333333333329818, 0.3333333333333329818, 0.3333333333333329818, 0.3333333333333329818, 0.3333333333333329818, 0.3333333333333329818, 0.3333333333333329818, 0.3333333333333329818, 0.3333333333333329818, 0.3333333333333329818, 0.3333333333333329818, 0.3333333333333329818, 0.3333333333333329818, 0.3333333333333329818, 0.3333333333333329818, 0.3333333333333329818, 0.3333333333333329818, 0.3333333333333329818, 0.3333333333333329818, 0.3333333333333329818, 0.3333333333333329818, 0.3333333333333329818, 0.3333333333333329818, 0.3333333333333329818, 0.3333333333333329818, 0.3333333333333329818, 0.3333333333333329818, 0.3333333333333329818, 0.3333333333333329818, 0.3333333333333329818, 0.3333333333333329818, 0.3333333333333329818, 0.3333333333333329818, 0.3333333333333329818, 0.3333333333333329818, 0.3333333333333329818, 0.3333333333333329818, 0.3333333333333329818, 0.3333333333333329818, 0.3333333333333329818, 0.3333333333333329818, 0.3333333333333329818, 0.3333333333333329818, 0.3333333333333329818, 0.3333333333333329818, 0.3333333333333329818, 0.3333333333333329818, 0.3333333333333329818, 0.3333333333333329818, 0.3333333333333329818, 0.3333333333333329818, 0.3333333333333329818, 0.3333333333333329818, 0.3333333333333329818, 0.3333333333333329818, 0.3333333333333329818, 0.3333333333333329818, 0.3333333333333329818, 0.3333333333333329818, 0.3333333333333329818, 0.3333333333333329818, 0.3333333333333329818, 0.3333333333333329818, 0.3333333333333329818, 0.3333333333333329818, 0.3333333333333329818, 0.3333333333333329818, 0.3333333333333329818, 0.3333333333333329818, 0.3333333333333329818, 0.3333333333333329818, 0.3333333333333329818, 0.3333333333333329818, 0.3333333333333329818, 0.3333333333333329818, 0.3333333333333329818, 0.3333333333333329818, 0.3333333333333329818, 0.3333333333333329818, 0.3333333333333329818, 0.3333333333333329818, 0.3333333333333329818, 0.3333333333333329818, 0.3333333333333329818, 0.3333333333333329818, 0.3333333333333329818, 0.3333333333333329818, 0.3333333333333329818, 0.3333333333333329818, 0.3333333333333329818, 0.3333333333333329818, 0.3333333333333329818, 0.3333333333333329818, 0.3333333333333329818),
 ( 1.000000000000000000, 1.000000000000000000, 1.000000000000000000, 1.000000000000000000, 1.000000000000000000, 1.000000000000000000, 1.000000000000000000, 1.000000000000000000, 1.000000000000000000, 1.000000000000000000, 1.000000000000000000, 1.000000000000000000, 1.000000000000000000, 1.000000000000000000, 1.000000000000000000, 1.000000000000000000, 1.000000000000000000, 1.000000000000000000, 1.000000000000000000, 1.000000000000000000, 1.000000000000000000, 1.000000000000000000, 1.000000000000000000, 1.000000000000000000, 1.000000000000000000, 1.000000000000000000, 1.000000000000000000, 1.000000000000000000, 1.000000000000000000, 1.000000000000000000, 1.000000000000000000, 1.000000000000000000, 1.000000000000000000, 1.000000000000000000, 1.000000000000000000, 1.000000000000000000, 1.000000000000000000, 1.000000000000000000, 1.000000000000000000, 1.000000000000000000, 1.000000000000000000, 1.000000000000000000, 1.000000000000000000, 1.000000000000000000, 1.000000000000000000, 1.000000000000000000, 1.000000000000000000, 1.000000000000000000, 1.000000000000000000, 1.000000000000000000, 1.000000000000000000, 1.000000000000000000, 1.000000000000000000, 1.000000000000000000, 1.000000000000000000, 1.000000000000000000, 1.000000000000000000, 1.000000000000000000, 1.000000000000000000, 1.000000000000000000, 1.000000000000000000, 1.000000000000000000, 1.000000000000000000, 1.000000000000000000, 1.000000000000000000, 1.000000000000000000, 1.000000000000000000, 1.000000000000000000, 1.000000000000000000, 1.000000000000000000, 1.000000000000000000, 1.000000000000000000, 1.000000000000000000, 1.000000000000000000, 1.000000000000000000, 1.000000000000000000, 1.000000000000000000, 1.000000000000000000, 1.000000000000000000, 1.000000000000000000, 1.000000000000000000, 1.000000000000000000, 1.000000000000000000, 1.000000000000000000, 1.000000000000000000, 1.000000000000000000, 1.000000000000000000, 1.000000000000000000, 1.000000000000000000, 1.000000000000000000, 1.000000000000000000, 1.000000000000000000, 1.000000000000000000, 1.000000000000000000, 1.000000000000000000, 1.000000000000000000, 1.000000000000000000, 1.000000000000000000, 1.000000000000000000, 1.000000000000000000, 1.000000000000000000, 1.000000000000000000, 1.000000000000000000, 1.000000000000000000, 1.000000000000000000, 1.000000000000000000, 1.000000000000000000, 1.000000000000000000, 1.000000000000000000, 1.000000000000000000, 1.000000000000000000, 1.000000000000000000, 1.000000000000000000, 1.000000000000000000, 1.000000000000000000, 1.000000000000000000, 1.000000000000000000, 1.000000000000000000, 1.000000000000000000, 1.000000000000000000, 1.000000000000000000, 1.000000000000000000, 1.000000000000000000, 1.000000000000000000, 1.000000000000000000, 1.000000000000000000, 1.000000000000000000, 1.000000000000000000, 1.000000000000000000, 1.000000000000000000, 1.000000000000000000, 1.000000000000000000, 1.000000000000000000, 1.000000000000000000, 1.000000000000000000, 1.000000000000000000, 1.000000000000000000, 1.000000000000000000, 1.000000000000000000, 1.000000000000000000, 1.000000000000000000, 1.000000000000000000, 1.000000000000000000, 1.000000000000000000, 1.000000000000000000, 1.000000000000000000, 1.000000000000000000, 1.000000000000000000, 1.000000000000000000, 1.000000000000000000, 1.000000000000000000, 1.000000000000000000, 1.000000000000000000, 1.000000000000000000, 1.000000000000000000, 1.000000000000000000, 1.000000000000000000, 1.000000000000000000, 1.000000000000000000, 1.000000000000000000, 1.000000000000000000, 1.000000000000000000, 1.000000000000000000, 1.000000000000000000, 1.000000000000000000, 1.000000000000000000, 1.000000000000000000, 1.000000000000000000, 1.000000000000000000, 1.000000000000000000, 1.000000000000000000, 1.000000000000000000, 1.000000000000000000, 1.000000000000000000, 1.000000000000000000, 1.000000000000000000, 1.000000000000000000, 1.000000000000000000, 1.000000000000000000, 1.000000000000000000, 1.000000000000000000, 1.000000000000000000, 1.000000000000000000, 1.000000000000000000, 1.000000000000000000, 1.000000000000000000, 1.000000000000000000, 1.000000000000000000),
 ( 0.3333333333333329818, 0.3333333333333329818, 0.3333333333333329818, 0.3333333333333329818, 0.3333333333333329818, 0.3333333333333329818, 0.3333333333333329818, 0.3333333333333329818, 0.3333333333333329818, 0.3333333333333329818, 0.3333333333333329818, 0.3333333333333329818, 0.3333333333333329818, 0.3333333333333329818, 0.3333333333333329818, 0.3333333333333329818, 0.3333333333333329818, 0.3333333333333329818, 0.3333333333333329818, 0.3333333333333329818, 0.3333333333333329818, 0.3333333333333329818, 0.3333333333333329818, 0.3333333333333329818, 0.3333333333333329818, 0.3333333333333329818, 0.3333333333333329818, 0.3333333333333329818, 0.3333333333333329818, 0.3333333333333329818, 0.3333333333333329818, 0.3333333333333329818, 0.3333333333333329818, 0.3333333333333329818, 0.3333333333333329818, 0.3333333333333329818, 0.3333333333333329818, 0.3333333333333329818, 0.3333333333333329818, 0.3333333333333329818, 0.3333333333333329818, 0.3333333333333329818, 0.3333333333333329818, 0.3333333333333329818, 0.3333333333333329818, 0.3333333333333329818, 0.3333333333333329818, 0.3333333333333329818, 0.3333333333333329818, 0.3333333333333329818, 0.3333333333333329818, 0.3333333333333329818, 0.3333333333333329818, 0.3333333333333329818, 0.3333333333333329818, 0.3333333333333329818, 0.3333333333333329818, 0.3333333333333329818, 0.3333333333333329818, 0.3333333333333329818, 0.3333333333333329818, 0.3333333333333329818, 0.3333333333333329818, 0.3333333333333329818, 0.3333333333333329818, 0.3333333333333329818, 0.3333333333333329818, 0.3333333333333329818, 0.3333333333333329818, 0.3333333333333329818, 0.3333333333333329818, 0.3333333333333329818, 0.3333333333333329818, 0.3333333333333329818, 0.3333333333333329818, 0.3333333333333329818, 0.3333333333333329818, 0.3333333333333329818, 0.3333333333333329818, 0.3333333333333329818, 0.3333333333333329818, 0.3333333333333329818, 0.3333333333333329818, 0.3333333333333329818, 0.3333333333333329818, 0.3333333333333329818, 0.3333333333333329818, 0.3333333333333329818, 0.3333333333333329818, 0.3333333333333329818, 0.3333333333333329818, 0.3333333333333329818, 0.3333333333333329818, 0.3333333333333329818, 0.3333333333333329818, 0.3333333333333329818, 0.3333333333333329818, 0.3333333333333329818, 0.3333333333333329818, 0.3333333333333329818, 0.3333333333333329818, 0.3333333333333329818, 0.3333333333333329818, 0.3333333333333329818, 0.3333333333333329818, 0.3333333333333329818, 0.3333333333333329818, 0.3333333333333329818, 0.3333333333333329818, 0.3333333333333329818, 0.3333333333333329818, 0.3333333333333329818, 0.3333333333333329818, 0.3333333333333329818, 0.3333333333333329818, 0.3333333333333329818, 0.3333333333333329818, 0.3333333333333329818, 0.3333333333333329818, 0.3333333333333329818, 0.3333333333333329818, 0.3333333333333329818, 0.3333333333333329818, 0.3333333333333329818, 0.3333333333333329818, 0.3333333333333329818, 0.3333333333333329818, 0.3333333333333329818, 0.3333333333333329818, 0.3333333333333329818, 0.3333333333333329818, 0.3333333333333329818, 0.3333333333333329818, 0.3333333333333329818, 0.3333333333333329818, 0.3333333333333329818, 0.3333333333333329818, 0.3333333333333329818, 0.3333333333333329818, 0.3333333333333329818, 0.3333333333333329818, 0.3333333333333329818, 0.3333333333333329818, 0.3333333333333329818, 0.3333333333333329818, 0.3333333333333329818, 0.3333333333333329818, 0.3333333333333329818, 0.3333333333333329818, 0.3333333333333329818, 0.3333333333333329818, 0.3333333333333329818, 0.3333333333333329818, 0.3333333333333329818, 0.3333333333333329818, 0.3333333333333329818, 0.3333333333333329818, 0.3333333333333329818, 0.3333333333333329818, 0.3333333333333329818, 0.3333333333333329818, 0.3333333333333329818, 0.3333333333333329818, 0.3333333333333329818, 0.3333333333333329818, 0.3333333333333329818, 0.3333333333333329818, 0.3333333333333329818, 0.3333333333333329818, 0.3333333333333329818, 0.3333333333333329818, 0.3333333333333329818, 0.3333333333333329818, 0.3333333333333329818, 0.3333333333333329818, 0.3333333333333329818, 0.3333333333333329818, 0.3333333333333329818, 0.3333333333333329818, 0.3333333333333329818, 0.3333333333333329818, 0.3333333333333329818, 0.3333333333333329818, 0.3333333333333329818, 0.3333333333333329818, 0.3333333333333329818, 0.3333333333333329818, 0.3333333333333329818),
 ( 0.3333333333333329818, 0.3333333333333329818, 0.3333333333333329818, 0.3333333333333329818, 0.3333333333333329818, 0.3333333333333329818, 0.3333333333333329818, 0.3333333333333329818, 0.3333333333333329818, 0.3333333333333329818, 0.3333333333333329818, 0.3333333333333329818, 0.3333333333333329818, 0.3333333333333329818, 0.3333333333333329818, 0.3333333333333329818, 0.3333333333333329818, 0.3333333333333329818, 0.3333333333333329818, 0.3333333333333329818, 0.3333333333333329818, 0.3333333333333329818, 0.3333333333333329818, 0.3333333333333329818, 0.3333333333333329818, 0.3333333333333329818, 0.3333333333333329818, 0.3333333333333329818, 0.3333333333333329818, 0.3333333333333329818, 0.3333333333333329818, 0.3333333333333329818, 0.3333333333333329818, 0.3333333333333329818, 0.3333333333333329818, 0.3333333333333329818, 0.3333333333333329818, 0.3333333333333329818, 0.3333333333333329818, 0.3333333333333329818, 0.3333333333333329818, 0.3333333333333329818, 0.3333333333333329818, 0.3333333333333329818, 0.3333333333333329818, 0.3333333333333329818, 0.3333333333333329818, 0.3333333333333329818, 0.3333333333333329818, 0.3333333333333329818, 0.3333333333333329818, 0.3333333333333329818, 0.3333333333333329818, 0.3333333333333329818, 0.3333333333333329818, 0.3333333333333329818, 0.3333333333333329818, 0.3333333333333329818, 0.3333333333333329818, 0.3333333333333329818, 0.3333333333333329818, 0.3333333333333329818, 0.3333333333333329818, 0.3333333333333329818, 0.3333333333333329818, 0.3333333333333329818, 0.3333333333333329818, 0.3333333333333329818, 0.3333333333333329818, 0.3333333333333329818, 0.3333333333333329818, 0.3333333333333329818, 0.3333333333333329818, 0.3333333333333329818, 0.3333333333333329818, 0.3333333333333329818, 0.3333333333333329818, 0.3333333333333329818, 0.3333333333333329818, 0.3333333333333329818, 0.3333333333333329818, 0.3333333333333329818, 0.3333333333333329818, 0.3333333333333329818, 0.3333333333333329818, 0.3333333333333329818, 0.3333333333333329818, 0.3333333333333329818, 0.3333333333333329818, 0.3333333333333329818, 0.3333333333333329818, 0.3333333333333329818, 0.3333333333333329818, 0.3333333333333329818, 0.3333333333333329818, 0.3333333333333329818, 0.3333333333333329818, 0.3333333333333329818, 0.3333333333333329818, 0.3333333333333329818, 0.3333333333333329818, 0.3333333333333329818, 0.3333333333333329818, 0.3333333333333329818, 0.3333333333333329818, 0.3333333333333329818, 0.3333333333333329818, 0.3333333333333329818, 0.3333333333333329818, 0.3333333333333329818, 0.3333333333333329818, 0.3333333333333329818, 0.3333333333333329818, 0.3333333333333329818, 0.3333333333333329818, 0.3333333333333329818, 0.3333333333333329818, 0.3333333333333329818, 0.3333333333333329818, 0.3333333333333329818, 0.3333333333333329818, 0.3333333333333329818, 0.3333333333333329818, 0.3333333333333329818, 0.3333333333333329818, 0.3333333333333329818, 0.3333333333333329818, 0.3333333333333329818, 0.3333333333333329818, 0.3333333333333329818, 0.3333333333333329818, 0.3333333333333329818, 0.3333333333333329818, 0.3333333333333329818, 0.3333333333333329818, 0.3333333333333329818, 0.3333333333333329818, 0.3333333333333329818, 0.3333333333333329818, 0.3333333333333329818, 0.3333333333333329818, 0.3333333333333329818, 0.3333333333333329818, 0.3333333333333329818, 0.3333333333333329818, 0.3333333333333329818, 0.3333333333333329818, 0.3333333333333329818, 0.3333333333333329818, 0.3333333333333329818, 0.3333333333333329818, 0.3333333333333329818, 0.3333333333333329818, 0.3333333333333329818, 0.3333333333333329818, 0.3333333333333329818, 0.3333333333333329818, 0.3333333333333329818, 0.3333333333333329818, 0.3333333333333329818, 0.3333333333333329818, 0.3333333333333329818, 0.3333333333333329818, 0.3333333333333329818, 0.3333333333333329818, 0.3333333333333329818, 0.3333333333333329818, 0.3333333333333329818, 0.3333333333333329818, 0.3333333333333329818, 0.3333333333333329818, 0.3333333333333329818, 0.3333333333333329818, 0.3333333333333329818, 0.3333333333333329818, 0.3333333333333329818, 0.3333333333333329818, 0.3333333333333329818, 0.3333333333333329818, 0.3333333333333329818, 0.3333333333333329818, 0.3333333333333329818, 0.3333333333333329818, 0.3333333333333329818, 0.3333333333333329818, 0.3333333333333329818, 0.3333333333333329818, 0.3333333333333329818),
 ( 1.000000000000000000, 1.000000000000000000, 1.000000000000000000, 1.000000000000000000, 1.000000000000000000, 1.000000000000000000, 1.000000000000000000, 1.000000000000000000, 1.000000000000000000, 1.000000000000000000, 1.000000000000000000, 1.000000000000000000, 1.000000000000000000, 1.000000000000000000, 1.000000000000000000, 1.000000000000000000, 1.000000000000000000, 1.000000000000000000, 1.000000000000000000, 1.000000000000000000, 1.000000000000000000, 1.000000000000000000, 1.000000000000000000, 1.000000000000000000, 1.000000000000000000, 1.000000000000000000, 1.000000000000000000, 1.000000000000000000, 1.000000000000000000, 1.000000000000000000, 1.000000000000000000, 1.000000000000000000, 1.000000000000000000, 1.000000000000000000, 1.000000000000000000, 1.000000000000000000, 1.000000000000000000, 1.000000000000000000, 1.000000000000000000, 1.000000000000000000, 1.000000000000000000, 1.000000000000000000, 1.000000000000000000, 1.000000000000000000, 1.000000000000000000, 1.000000000000000000, 1.000000000000000000, 1.000000000000000000, 1.000000000000000000, 1.000000000000000000, 1.000000000000000000, 1.000000000000000000, 1.000000000000000000, 1.000000000000000000, 1.000000000000000000, 1.000000000000000000, 1.000000000000000000, 1.000000000000000000, 1.000000000000000000, 1.000000000000000000, 1.000000000000000000, 1.000000000000000000, 1.000000000000000000, 1.000000000000000000, 1.000000000000000000, 1.000000000000000000, 1.000000000000000000, 1.000000000000000000, 1.000000000000000000, 1.000000000000000000, 1.000000000000000000, 1.000000000000000000, 1.000000000000000000, 1.000000000000000000, 1.000000000000000000, 1.000000000000000000, 1.000000000000000000, 1.000000000000000000, 1.000000000000000000, 1.000000000000000000, 1.000000000000000000, 1.000000000000000000, 1.000000000000000000, 1.000000000000000000, 1.000000000000000000, 1.000000000000000000, 1.000000000000000000, 1.000000000000000000, 1.000000000000000000, 1.000000000000000000, 1.000000000000000000, 1.000000000000000000, 1.000000000000000000, 1.000000000000000000, 1.000000000000000000, 1.000000000000000000, 1.000000000000000000, 1.000000000000000000, 1.000000000000000000, 1.000000000000000000, 1.000000000000000000, 1.000000000000000000, 1.000000000000000000, 1.000000000000000000, 1.000000000000000000, 1.000000000000000000, 1.000000000000000000, 1.000000000000000000, 1.000000000000000000, 1.000000000000000000, 1.000000000000000000, 1.000000000000000000, 1.000000000000000000, 1.000000000000000000, 1.000000000000000000, 1.000000000000000000, 1.000000000000000000, 1.000000000000000000, 1.000000000000000000, 1.000000000000000000, 1.000000000000000000, 1.000000000000000000, 1.000000000000000000, 1.000000000000000000, 1.000000000000000000, 1.000000000000000000, 1.000000000000000000, 1.000000000000000000, 1.000000000000000000, 1.000000000000000000, 1.000000000000000000, 1.000000000000000000, 1.000000000000000000, 1.000000000000000000, 1.000000000000000000, 1.000000000000000000, 1.000000000000000000, 1.000000000000000000, 1.000000000000000000, 1.000000000000000000, 1.000000000000000000, 1.000000000000000000, 1.000000000000000000, 1.000000000000000000, 1.000000000000000000, 1.000000000000000000, 1.000000000000000000, 1.000000000000000000, 1.000000000000000000, 1.000000000000000000, 1.000000000000000000, 1.000000000000000000, 1.000000000000000000, 1.000000000000000000, 1.000000000000000000, 1.000000000000000000, 1.000000000000000000, 1.000000000000000000, 1.000000000000000000, 1.000000000000000000, 1.000000000000000000, 1.000000000000000000, 1.000000000000000000, 1.000000000000000000, 1.000000000000000000, 1.000000000000000000, 1.000000000000000000, 1.000000000000000000, 1.000000000000000000, 1.000000000000000000, 1.000000000000000000, 1.000000000000000000, 1.000000000000000000, 1.000000000000000000, 1.000000000000000000, 1.000000000000000000, 1.000000000000000000, 1.000000000000000000, 1.000000000000000000, 1.000000000000000000, 1.000000000000000000, 1.000000000000000000, 1.000000000000000000, 1.000000000000000000, 1.000000000000000000, 1.000000000000000000, 1.000000000000000000, 1.000000000000000000) ) ) 
 REPRESENTATION_ITEM ( '' )  SURFACE ( )  );
#3229=CARTESIAN_POINT ( 'NONE',  ( -2.239137794397029868, -4.987178660919110662, 3.975425900939220103 ) ) ;
#3232=CARTESIAN_POINT ( 'NONE',  ( 1.912899118714319169, -4.218665147405596727, 5.445465495009710111 ) ) ;
#3242=CARTESIAN_POINT ( 'NONE',  ( 1.880631435828169939, -5.355296610169490101, 3.876649216148224220 ) ) ;
#3244=CARTESIAN_POINT ( 'NONE',  ( 1.713314936023349944, -5.338983050847460277, 3.089913064446569546 ) ) ;
#3246=FACE_OUTER_BOUND ( 'NONE', #9018, .T. ) ;
#3249=CARTESIAN_POINT ( 'NONE',  ( -2.349129089426440054, -4.894025507765950245, 4.842612091679129982 ) ) ;
#3250=CARTESIAN_POINT ( 'NONE',  ( -1.876226141297921091, -4.711560077819614278, 3.866526959224360294 ) ) ;
#3252=CARTESIAN_POINT ( 'NONE',  ( -0.009340024727882490982, -5.298031483068750269, 2.378874508206550331 ) ) ;
#3257=CARTESIAN_POINT ( 'NONE',  ( 0.8731223871105069367, -0.1290254237288140371, 6.558046933601105799 ) ) ;
#3258=CARTESIAN_POINT ( 'NONE',  ( -1.097561405233230092, -3.613169651910099756, 2.618148744692269769 ) ) ;
#3265=CARTESIAN_POINT ( 'NONE',  ( -1.928817277882839409, -4.455388906648448888, 6.048484184565968924 ) ) ;
#3267=CARTESIAN_POINT ( 'NONE',  ( 1.932035991685901122, -5.038983050847454237, 2.884370051397200818 ) ) ;
#3268=B_SPLINE_CURVE_WITH_KNOTS ( 'NONE', 3,
 ( #16327, #15140, #8099, #2451, #2167, #13738, #16417, #7906, #3442, #14751, #13557, #6695, #1056, #14945, #17695, #5123, #872, #2065, #12353, #3632, #7720, #2256, #13364, #9283, #3724, #6403, #13455, #15053, #772, #3832, #6316, #11978, #17590, #4925, #10582, #6510, #12074, #12169, #2359, #8007, #13652, #963, #6601, #12258, #17876, #5214, #16521, #18245, #11333, #5687, #7083, #2635, #9759, #8377, #4280, #2911, #5321, #15326, #9570, #15597, #6797, #8182, #15510, #8457, #4191, #12445, #16969, #14204, #2816, #16695, #9937, #1425, #1325, #15228, #11045, #8284, #12530, #14094, #12726, #2730, #15423, #9852, #43, #5596, #13925, #14010, #16612, #7175, #6972, #18063, #3913, #2532, #1242, #9656, #5405, #11240, #13831, #16884, #1150, #4002, #11134, #17977, #6885, #18143, #8558, #10967, #5491, #16789, #4104, #12621, #1524, #11683, #5951, #10382, #17140, #13162, #7256, #12991, #4464, #13078, #311, #12814, #11418, #15860, #14635, #16044, #4542, #7349, #7437, #3168, #10036, #17411, #11590, #126, #10121, #8824, #397, #10195, #8907, #3003, #5863, #11510, #11787, #1950, #5776, #17052, #12899, #15693, #14475, #4374, #17220, #17309, #15775, #8644, #14291, #4637, #1612, #3083, #8726, #1793, #14370, #6125, #479, #1869, #1697, #6037, #10296, #4731, #3343, #221, #15964, #3265, #8988, #14555, #7518, #16403, #10560, #661, #17572, #9463, #14929, #10756, #6300, #13638, #15028, #9268, #17496, #11958 ),
 .UNSPECIFIED., .F., .F.,
 ( 4, 1, 1, 1, 1, 1, 1, 1, 1, 1, 1, 1, 1, 1, 1, 1, 1, 1, 1, 1, 1, 1, 1, 1, 1, 1, 1, 1, 1, 1, 1, 1, 1, 1, 1, 1, 1, 1, 1, 1, 1, 1, 1, 1, 1, 1, 1, 1, 1, 1, 1, 1, 1, 1, 1, 1, 1, 1, 1, 1, 1, 1, 1, 1, 1, 1, 1, 1, 1, 1, 1, 1, 1, 1, 1, 1, 1, 1, 1, 1, 1, 1, 1, 1, 1, 1, 1, 1, 1, 1, 1, 1, 1, 1, 1, 1, 1, 1, 1, 1, 1, 1, 1, 1, 1, 1, 1, 1, 1, 1, 1, 1, 1, 1, 1, 1, 1, 1, 1, 1, 1, 1, 1, 1, 1, 1, 1, 1, 1, 1, 1, 1, 1, 1, 1, 1, 1, 1, 1, 1, 1, 1, 1, 1, 1, 1, 1, 1, 1, 1, 1, 1, 1, 1, 1, 1, 1, 1, 1, 1, 1, 1, 1, 1, 1, 1, 1, 1, 1, 1, 1, 1, 1, 1, 1, 1, 1, 1, 1, 1, 1, 1, 1, 1, 1, 4 ),
 ( 0.7853981633974479459, 0.8787968639095770085, 0.9721955644217059600, 1.065594264933839908, 1.158992965445959866, 1.252391665958090039, 1.345790366470219990, 1.439189066982349940, 1.532587767494480113, 1.625986468006610064, 1.719385168518740015, 1.812783869030869965, 1.906182569543000138, 1.999581270055129867, 2.092979970567249826, 2.186378671079379998, 2.279777371591510171, 2.373176072103639900, 2.466574772615769628, 2.559973473127900245, 2.653372173640029974, 2.746770874152160147, 2.840169574664289875, 2.933568275176409834, 3.026966975688540007, 3.120365676200670180, 3.213764376712799908, 3.307163077224930081, 3.400561777737059810, 3.493960478249190427, 3.587359178761320155, 3.680757879273439670, 3.774156579785570287, 3.867555280297700016, 3.960953980809830188, 4.054352681321960361, 4.147751381834090090, 4.241150082346219818, 4.334548782858350435, 4.427947483370480164, 4.521346183882600123, 4.614744884394729851, 4.708143584906859580, 4.801542285418989309, 4.894940985931119926, 4.988339686443250542, 5.081738386955380271, 5.175137087467510000, 5.268535787979639728, 5.361934488491760575, 5.455333189003890304, 5.548731889516020033, 5.642130590028149761, 5.735529290540279490, 5.828927991052410107, 5.922326691564539836, 6.015725392076670452, 6.109124092588789523, 6.202522793100920140, 6.295921493613049869, 6.389320194125180485, 6.482718894637310214, 6.576117595149439943, 6.669516295661569671, 6.762914996173699400, 6.856313696685830017, 6.949712397197949976, 7.043111097710079704, 7.136509798222209433, 7.229908498734340050, 7.323307199246470667, 7.416705899758600395, 7.510104600270730124, 7.603503300782859853, 7.696902001294989581, 7.790300701807110428, 7.883699402319240157, 7.977098102831369886, 8.070496803343500503, 8.163895503855631119, 8.257294204367759960, 8.350692904879890577, 8.444091605392019417, 8.537490305904137600, 8.630889006416269993, 8.724287706928398833, 8.817686407440529450, 8.911085107952660067, 9.004483808464788908, 9.097882508976921301, 9.191281209489050141, 9.284679910001178982, 9.378078610513298941, 9.471477311025429557, 9.564876011537560174, 9.658274712049690791, 9.751673412561819632, 9.845072113073950248, 9.938470813586080865, 10.03186951409819905, 10.12526821461029947, 10.21866691512249936, 10.31206561563459978, 10.40546431614669842, 10.49886301665890009, 10.59226171717100051, 10.68566041768310093, 10.77905911819519957, 10.87245781870739947, 10.96585651921949989, 11.05925521973160031, 11.15265392024380020, 11.24605262075590062, 11.33945132126800104, 11.43285002178009968, 11.52624872229229958, 11.61964742280439999, 11.71304612331650041, 11.80644482382869853, 11.89984352434079895, 11.99324222485290115, 12.08664092536500156, 12.18003962587719968, 12.27343832638930010, 12.36683702690140052, 12.46023572741360042, 12.55363442792569906, 12.64703312843779948, 12.74043182894989990, 12.83383052946209979, 12.92722922997419843, 13.02062793048630063, 13.11402663099850052, 13.20742533151059916, 13.30082403202269958, 13.39422273253480000, 13.48762143304700167, 13.58102013355910032, 13.67441883407120073, 13.76781753458340063, 13.86121623509549927, 13.95461493560759969, 14.04801363611970011, 14.14141233663190000, 14.23481103714399865, 14.32820973765609907, 14.42160843816829896, 14.51500713868040116, 14.60840583919249980, 14.70180453970460022, 14.79520324021680011, 14.88860194072889875, 14.98200064124100095, 15.07539934175320084, 15.16879804226530126, 15.26219674277739990, 15.35559544328959980, 15.44899414380170022, 15.54239284431380064, 15.63579154482589928, 15.72919024533809740, 15.82258894585020137, 15.91598764636230001, 16.00938634687449991, 16.10278504738660033, 16.19618374789870074, 16.28958244841080116, 16.38298114892299751, 16.47637984943510148, 16.56977854994720545, 16.66317725045940179, 16.75657595097149866, 16.84997465148359908, 16.94337335199570305, 17.03677205250789939, 17.13017075301999981, 17.22356945353210023, 17.31696815404430012, 17.41036685455640054, 17.50376555506850096, 17.59716425558059782, 17.69056295609280127, 17.78396165660489814, 17.87736035711699856, 17.97075905762920200, 18.06415775814129887 ),
 .UNSPECIFIED. ) ;
#3271=CARTESIAN_POINT ( 'NONE',  ( -2.224278379903029901, -0.5091101694915259879, 5.468825643806110470 ) ) ;
#3276=CARTESIAN_POINT ( 'NONE',  ( -1.772995665808888788, -4.777584066324515710, 5.735078843205186239 ) ) ;
#3278=CARTESIAN_POINT ( 'NONE',  ( -2.519547246525518425, -0.5402542372881364852, 3.866491354109200529 ) ) ;
#3284=CARTESIAN_POINT ( 'NONE',  ( -0.008236272907982289393, -0.5805379513491200072, 2.272810616177410203 ) ) ;
#3285=CARTESIAN_POINT ( 'NONE',  ( -1.851073041990159984, -5.493220338983049622, 6.153284478378270528 ) ) ;
#3286=CARTESIAN_POINT ( 'NONE',  ( -1.477796163681079689, -0.1824152542372890207, 6.531563725478148896 ) ) ;
#3287=CARTESIAN_POINT ( 'NONE',  ( -2.632194480419669080, -3.310421904162345719, 5.038623552414950524 ) ) ;
#3289=CARTESIAN_POINT ( 'NONE',  ( -1.832842064134660109, -2.871785303044850135, 6.176291182464519913 ) ) ;
#3292=CARTESIAN_POINT ( 'NONE',  ( 1.160665242129880426, -2.499172690432241772, 6.393445611272976947 ) ) ;
#3299=CARTESIAN_POINT ( 'NONE',  ( -2.653886076156968699, -1.474488005747551567, 4.698454755023434792 ) ) ;
#3301=CARTESIAN_POINT ( 'NONE',  ( -1.722199153441400066, -5.095857339597789526, 3.099360556065549943 ) ) ;
#3304=CARTESIAN_POINT ( 'NONE',  ( 1.713314936023349944, -5.038983050847460454, 3.089913064446569546 ) ) ;
#3305=EDGE_LOOP ( 'NONE', ( #9084, #14268, #17891, #11631 ) ) ;
#3311=CARTESIAN_POINT ( 'NONE',  ( 1.818868030982612183, -2.355602084342530933, 2.767428454397789839 ) ) ;
#3315=CARTESIAN_POINT ( 'NONE',  ( 1.669205944673859854, -2.452596113855660231, 6.359065158982410537 ) ) ;
#3316=CARTESIAN_POINT ( 'NONE',  ( 1.112057765673850174, -5.020626044399135068, 2.286633591154370482 ) ) ;
#3317=CARTESIAN_POINT ( 'NONE',  ( -2.479511223993290603, -1.866548030288480042, 3.753882785753710483 ) ) ;
#3319=CARTESIAN_POINT ( 'NONE',  ( -0.7778405029480311983, -4.614566048306495638, 6.599964735094220991 ) ) ;
#3327=CARTESIAN_POINT ( 'NONE',  ( 1.526791597786429922, -2.774791273531720392, 6.490992212270249695 ) ) ;
#3329=CARTESIAN_POINT ( 'NONE',  ( 2.286166334984490067, -5.386440677966100488, 5.258525443163859947 ) ) ;
#3330=DIRECTION ( 'NONE',  ( -1.762990951819940286E-17, -1.000000000000000000, -2.891205793294679017E-15 ) ) ;
#3331=CARTESIAN_POINT ( 'NONE',  ( -0.3752419433106839453, -1.424070552810999812, 7.023346545710370314 ) ) ;
#3332=CARTESIAN_POINT ( 'NONE',  ( 1.869848057046569867, -4.288530012270459935, 6.129130480762009725 ) ) ;
#3333=CARTESIAN_POINT ( 'NONE',  ( -1.945780800405131350, -4.688271789531334832, 4.045142061754299689 ) ) ;
#3337=CARTESIAN_POINT ( 'NONE',  ( -1.940327948426050941, -0.2091101694915259990, 5.370677689277675526 ) ) ;
#3338=CARTESIAN_POINT ( 'NONE',  ( 2.342931736853870017, -4.102223705964150646, 4.477701633099130163 ) ) ;
#3343=CARTESIAN_POINT ( 'NONE',  ( -1.480680413335759837, -4.385524041783591009, 6.529298007719828156 ) ) ;
#3344=CARTESIAN_POINT ( 'NONE',  ( 0.3171869470818560743, -5.144279661016955885, 7.334814496515233095 ) ) ;
#3348=ADVANCED_FACE ( 'NONE', ( #3246 ), #16594, .T. ) ;
#3352=CARTESIAN_POINT ( 'NONE',  ( -1.992092870331710452, -3.403575057315514130, 4.203544726484199856 ) ) ;
#3354=CARTESIAN_POINT ( 'NONE',  ( -2.020286629067959971, -0.4913135593220345210, 6.420841923842841581 ) ) ;
#3359=CARTESIAN_POINT ( 'NONE',  ( -0.2812789908084309398, -0.1557203389830509321, 7.036533610117277959 ) ) ;
#3360=CARTESIAN_POINT ( 'NONE',  ( -1.837442528958838750, -3.543304787045241433, 2.785079989718828752 ) ) ;
#3361=ORIENTED_EDGE ( 'NONE', *, *, #528, .T. ) ;
#3363=CARTESIAN_POINT ( 'NONE',  ( 0.09706517602699299418, -2.638902420161969520, 7.051451474958980725 ) ) ;
#3364=EDGE_CURVE ( 'NONE', #4345, #14300, #14053, .T. ) ;
#3367=CARTESIAN_POINT ( 'NONE',  ( 1.238036348455360258, -3.593722239981790523, 3.062267469172269330 ) ) ;
#3369=CARTESIAN_POINT ( 'NONE',  ( 0.9516466452860694591, -0.9621456634052125700, 6.519140045500582126 ) ) ;
#3371=CARTESIAN_POINT ( 'NONE',  ( 0.5110358699406184479, -0.3612150962701983770, 2.697283651280069527 ) ) ;
#3372=CARTESIAN_POINT ( 'NONE',  ( -2.642175029090489513, -1.497776294035840561, 4.450952196049505538 ) ) ;
#3375=CARTESIAN_POINT ( 'NONE',  ( -0.03714311608457869507, -4.521412895153340550, 7.053160869216429596 ) ) ;
#3378=CARTESIAN_POINT ( 'NONE',  ( -2.340070819011249803, -5.219915254237290192, 4.950151441910549899 ) ) ;
#3385=CARTESIAN_POINT ( 'NONE',  ( 2.494165244384159763, -2.472043525783979678, 3.793218093085234166 ) ) ;
#3389=CARTESIAN_POINT ( 'NONE',  ( -2.211317922628890376, -3.127956474216019966, 3.894507149290469705 ) ) ;
#3390=CARTESIAN_POINT ( 'NONE',  ( -0.009452110982655099330, -5.299807955295455564, 2.649999999999998579 ) ) ;
#3391=CARTESIAN_POINT ( 'NONE',  ( 1.256119432346080478, -1.261052534792989288, 7.037793332329536966 ) ) ;
#3394=CARTESIAN_POINT ( 'NONE',  ( 0.1565249325564390115, -0.4468220338983060480, 7.048192310558509810 ) ) ;
#3396=CARTESIAN_POINT ( 'NONE',  ( 2.586172839791708533, -5.364194915254235418, 4.104546363490930716 ) ) ;
#3403=CARTESIAN_POINT ( 'NONE',  ( 0.6673090596498160165, -2.239160642901090181, 2.443133963569570355 ) ) ;
#3408=CARTESIAN_POINT ( 'NONE',  ( 2.046174187462399985, -1.121322805063259986, 5.862719605943959245 ) ) ;
#3409=CARTESIAN_POINT ( 'NONE',  ( -0.2564439965878500538, -4.544701183441629766, 7.039440566481220074 ) ) ;
#3410=CARTESIAN_POINT ( 'NONE',  ( -0.9742769543504515850, -4.338947465207014353, 6.507120986223577042 ) ) ;
#3416=CARTESIAN_POINT ( 'NONE',  ( 1.921786527979010062, -0.05783898305084796132, 3.977907449687776431 ) ) ;
#3417=CARTESIAN_POINT ( 'NONE',  ( -0.8986180677147959095, -3.636457940198390304, 2.524860635301629852 ) ) ;
#3423=CARTESIAN_POINT ( 'NONE',  ( -1.973760952634090238, -5.259957627118655665, 2.925986839873730982 ) ) ;
#3429=CARTESIAN_POINT ( 'NONE',  ( 1.372465729645801602, -4.335106588847043696, 6.226839763556046847 ) ) ;
#3432=CARTESIAN_POINT ( 'NONE',  ( 1.347262683220810553, -0.1245762711864410871, 6.986424775243341045 ) ) ;
#3435=CARTESIAN_POINT ( 'NONE',  ( 2.386628511786341722, -0.05338983050847501133, 3.539457309197775459 ) ) ;
#3439=CARTESIAN_POINT ( 'NONE',  ( 0.4974685680287860290, -5.439830508474580384, 7.000224381598740386 ) ) ;
#3442=CARTESIAN_POINT ( 'NONE',  ( 2.334748642087659753, -0.6593979156574648615, 4.403867486184822155 ) ) ;
#3444=CARTESIAN_POINT ( 'NONE',  ( -1.372722144827311475, -0.2742238837839081067, 2.407683403867349803 ) ) ;
#3445=CARTESIAN_POINT ( 'NONE',  ( -1.008962495263940662, -4.614566048306495638, 7.154609617872592864 ) ) ;
#3446=ORIENTED_EDGE ( 'NONE', *, *, #13244, .T. ) ;
#3447=CARTESIAN_POINT ( 'NONE',  ( -2.075124426334559846, -2.918361879621429900, 5.810227140144559321 ) ) ;
#3452=CARTESIAN_POINT ( 'NONE',  ( 2.013199450439951299, -3.873181699441240244, 5.102405038954985095 ) ) ;
#3454=CARTESIAN_POINT ( 'NONE',  ( 1.865240315818150973, -2.149848366107909303, 3.842223568244794496 ) ) ;
#3461=CARTESIAN_POINT ( 'NONE',  ( -1.945845091386011250, -1.660794312053860633, 2.895339208235828909 ) ) ;
#3467=CARTESIAN_POINT ( 'NONE',  ( -0.1565249325564300187, -5.153177966101689655, 7.048192310558509810 ) ) ;
#3479=CARTESIAN_POINT ( 'NONE',  ( 1.503451935564949826, -2.499172690432241772, 6.886949009567407742 ) ) ;
#3481=CARTESIAN_POINT ( 'NONE',  ( 1.094547058713730037, -2.844656138396588929, 7.117660114503893354 ) ) ;
#3485=CARTESIAN_POINT ( 'NONE',  ( 1.044181395669780077, -3.547145663405210314, 2.590869634085890105 ) ) ;
#3488=CARTESIAN_POINT ( 'NONE',  ( 2.647661051184980519, -2.541908390648840665, 4.518328177639069132 ) ) ;
#3491=CARTESIAN_POINT ( 'NONE',  ( -2.328217775191430139, -0.5180084745762719711, 5.043379051721170292 ) ) ;
#3494=CARTESIAN_POINT ( 'NONE',  ( -1.417709711196470046, -2.006277760018209566, 2.821478011237799954 ) ) ;
#3495=CARTESIAN_POINT ( 'NONE',  ( 2.345900685764729765, -0.3711864406779670222, 4.512231114381330066 ) ) ;
#3498=CARTESIAN_POINT ( 'NONE',  ( -0.8570167067220350043, -5.582203389830509899, 2.508190348879359988 ) ) ;
#3508=CARTESIAN_POINT ( 'NONE',  ( 2.211317922628870392, -2.472043525783979678, 3.894507149290419967 ) ) ;
#3509=CARTESIAN_POINT ( 'NONE',  ( -2.116444151961480280, -5.546610169491529518, 3.670839500609359707 ) ) ;
#3512=CARTESIAN_POINT ( 'NONE',  ( -2.345213174852959881, -1.796683165423619943, 4.503223853122380049 ) ) ;
#3513=CARTESIAN_POINT ( 'NONE',  ( -0.6864473529425049181, -4.591277760018209975, 6.951118770549909343 ) ) ;
#3514=CARTESIAN_POINT ( 'NONE',  ( -2.045969882616350155, -1.796683165423619055, 4.529973290172065070 ) ) ;
#3518=CARTESIAN_POINT ( 'NONE',  ( 1.558267747804329861, -0.7002976875533010181, 3.135138892994000059 ) ) ;
#3521=CARTESIAN_POINT ( 'NONE',  ( -0.9485663501270049647, -3.054250732991179440, 6.853826262002260528 ) ) ;
#3528=CARTESIAN_POINT ( 'NONE',  ( -0.7322514394120432923, -5.286652542372874741, 2.149183891723918993 ) ) ;
#3529=CARTESIAN_POINT ( 'NONE',  ( -2.043308330018790198, -0.5002118644067800046, 5.867646457774669422 ) ) ;
#3533=CARTESIAN_POINT ( 'NONE',  ( -0.2302241296435190154, -3.706322805063249959, 2.659926792304259990 ) ) ;
#3534=CARTESIAN_POINT ( 'NONE',  ( 0.9664230948141925293, -0.01779661016949178609, 2.228384861502251457 ) ) ;
#3536=CARTESIAN_POINT ( 'NONE',  ( 1.889104232906359870, -0.3444915254237289615, 3.296507079072520163 ) ) ;
#3538=CARTESIAN_POINT ( 'NONE',  ( 2.560337424259670591, -0.06228813559322075172, 4.001768473655590519 ) ) ;
#3543=CARTESIAN_POINT ( 'NONE',  ( -2.088297318559229954, -5.502118644067800268, 5.785136623276639689 ) ) ;
#3544=CARTESIAN_POINT ( 'NONE',  ( 0.4500319419456214609, -4.474836318576761229, 7.315451193241913508 ) ) ;
#3546=CARTESIAN_POINT ( 'NONE',  ( -1.209303714320900003, -4.865515740159329638, 2.662663894020049771 ) ) ;
#3547=CARTESIAN_POINT ( 'NONE',  ( -0.5570002967655939274, -2.708767285026830063, 6.986590552960220357 ) ) ;
#3550=CARTESIAN_POINT ( 'NONE',  ( 2.021195349941390162, -3.780028546288090041, 4.339901124684640621 ) ) ;
#3553=CARTESIAN_POINT ( 'NONE',  ( 1.992092870331701349, -2.196424942684489956, 4.203544726484164329 ) ) ;
#3555=AXIS2_PLACEMENT_3D ( 'NONE', #14493, #13277, #1816 ) ;
#3557=CARTESIAN_POINT ( 'NONE',  ( 0.5843165771433389555, -0.3612150962701970447, 2.403837883145309995 ) ) ;
#3558=CARTESIAN_POINT ( 'NONE',  ( -2.212163452524020357, -2.895073591333140239, 6.166099093621881799 ) ) ;
#3561=CARTESIAN_POINT ( 'NONE',  ( -0.5902886515192680150, -1.447358841099289917, 6.978224088050050788 ) ) ;
#3563=CARTESIAN_POINT ( 'NONE',  ( -0.3743405594629430344, -5.157627118644070308, 7.023440622744399953 ) ) ;
#3570=CARTESIAN_POINT ( 'NONE',  ( -1.392553072310521278, -5.564406779661021041, 3.191531554476531252 ) ) ;
#3571=CARTESIAN_POINT ( 'NONE',  ( -2.494165244384181079, -3.127956474216021299, 3.793218093085275910 ) ) ;
#3572=CARTESIAN_POINT ( 'NONE',  ( 1.536215498768949361, -5.033893599512578199, 2.912754292501710918 ) ) ;
#3573=CARTESIAN_POINT ( 'NONE',  ( 1.720450724489989813, -2.774791273531719060, 6.720683794561567836 ) ) ;
#3577=CARTESIAN_POINT ( 'NONE',  ( 1.552749016687789974, -4.036199717459258984, 6.468535037441730751 ) ) ;
#3582=CARTESIAN_POINT ( 'NONE',  ( 2.282375681463800543, -2.425466949207401690, 3.345793611865401473 ) ) ;
#3588=CARTESIAN_POINT ( 'NONE',  ( -2.255259958075430227, -1.703530012270459970, 5.372717034856060003 ) ) ;
#3589=CARTESIAN_POINT ( 'NONE',  ( -0.009452017499194409825, -5.299806473661739403, 2.336684903355700005 ) ) ;
#3591=CARTESIAN_POINT ( 'NONE',  ( -0.7983658734557950165, -5.466525423728810118, 6.913847129767330735 ) ) ;
#3595=CARTESIAN_POINT ( 'NONE',  ( 2.328217775191430139, -5.081991525423728895, 5.043379051721158746 ) ) ;
#3600=CARTESIAN_POINT ( 'NONE',  ( -1.669205944673819886, -3.147403886144329643, 6.359065158982450505 ) ) ;
#3602=CARTESIAN_POINT ( 'NONE',  ( 2.224278379903029901, -5.390889830508481140, 5.468825643806100700 ) ) ;
#3605=CARTESIAN_POINT ( 'NONE',  ( -1.586727176531439909, -1.982989471729919906, 2.961885344765640138 ) ) ;
#3606=CARTESIAN_POINT ( 'NONE',  ( 0.6150581927482109412, -4.451548030288480895, 6.971662190339319665 ) ) ;
#3608=CARTESIAN_POINT ( 'NONE',  ( -1.966895454505930729, -1.703530012270459970, 5.288408118292069915 ) ) ;
#3611=CARTESIAN_POINT ( 'NONE',  ( 1.670747152266691016, -0.4963810343603142217, 3.047345280935851441 ) ) ;
#3613=CARTESIAN_POINT ( 'NONE',  ( 2.311987889326980294, -4.078935417675859654, 4.260161748947079552 ) ) ;
#3620=CARTESIAN_POINT ( 'NONE',  ( -3.188875856275119715E-15, -5.300000000000000711, 2.050000000000001155 ) ) ;
#3625=CARTESIAN_POINT ( 'NONE',  ( -1.423520578776781509, -3.543304787045241433, 3.220645071516951230 ) ) ;
#3626=CARTESIAN_POINT ( 'NONE',  ( 1.800129581279440893, -0.03559322033898339871, 2.750028594811110061 ) ) ;
#3628=CARTESIAN_POINT ( 'NONE',  ( 1.438959988998139914E-16, -0.2999999999999999889, 2.350000000000000089 ) ) ;
#3629=CARTESIAN_POINT ( 'NONE',  ( 1.438959988998139914E-16, -2.775557561562889872E-16, 2.350000000000000089 ) ) ;
#3631=CARTESIAN_POINT ( 'NONE',  ( -1.194742379459959869, -5.475423728813559876, 6.727584234649759409 ) ) ;
#3632=CARTESIAN_POINT ( 'NONE',  ( 1.460675875430079484, -0.9155690868286360251, 6.545310725710027810 ) ) ;
#3633=CARTESIAN_POINT ( 'NONE',  ( 1.811729841638690219, -5.341949152542369461, 3.197954009834290012 ) ) ;
#3634=CARTESIAN_POINT ( 'NONE',  ( -2.408279507600840308, -4.800872354612795156, 5.815035204050404971 ) ) ;
#3637=CARTESIAN_POINT ( 'NONE',  ( -2.046174187462380445, -4.478677194936739880, 5.862719605944009871 ) ) ;
#3640=CARTESIAN_POINT ( 'NONE',  ( -0.8014931112106958855, -4.315659176918716255, 6.590108630558016323 ) ) ;
#3643=CARTESIAN_POINT ( 'NONE',  ( 0.9588981328681075444, -1.986830348089900777, 2.884671871696430578 ) ) ;
#3648=CARTESIAN_POINT ( 'NONE',  ( 1.652654650382400003, -0.7952867690272209522, 3.029252778805620050 ) ) ;
#3649=CARTESIAN_POINT ( 'NONE',  ( 1.449852972479971358, -2.010118636378181112, 2.477154964647140911 ) ) ;
#3654=CARTESIAN_POINT ( 'NONE',  ( -2.345900685764729765, -5.228813559322030180, 4.512231114381339836 ) ) ;
#3656=ORIENTED_EDGE ( 'NONE', *, *, #5650, .F. ) ;
#3662=CARTESIAN_POINT ( 'NONE',  ( -1.248294325655370018, -5.573305084745760141, 2.704938983774309857 ) ) ;
#3664=CARTESIAN_POINT ( 'NONE',  ( 0.1110902655589990351, -2.638902420161969520, 7.351560417169478612 ) ) ;
#3666=CARTESIAN_POINT ( 'NONE',  ( 2.608006145151101407, -4.172088570829024512, 5.191342690854350295 ) ) ;
#3669=CARTESIAN_POINT ( 'NONE',  ( 0.8429265834919229539, -3.523857375116919766, 2.502678798553439776 ) ) ;
#3672=CARTESIAN_POINT ( 'NONE',  ( 1.428323476796560465, -2.309025507765959606, 2.463260019887501429 ) ) ;
#3676=CARTESIAN_POINT ( 'NONE',  ( 1.248294325655350034, -0.3266949152542379942, 2.704938983774300088 ) ) ;
#3677=CARTESIAN_POINT ( 'NONE',  ( 0.06276132972186961034, -1.377493976234430040, 7.052616990284530374 ) ) ;
#3678=CARTESIAN_POINT ( 'NONE',  ( -0.9150601050661559821, -0.4690677966101700069, 6.868218666554230190 ) ) ;
#3683=CARTESIAN_POINT ( 'NONE',  ( 2.143090896833109493, -5.095338983050849535, 5.672454929438340621 ) ) ;
#3689=CARTESIAN_POINT ( 'NONE',  ( 1.444955263746720009, -2.332313796054249710, 2.842353646881480511 ) ) ;
#3692=CARTESIAN_POINT ( 'NONE',  ( 1.526791597786429922, -2.774791273531720392, 6.490992212270249695 ) ) ;
#3695=CARTESIAN_POINT ( 'NONE',  ( -0.1781895581254780980, -2.146007489747939090, 2.654724878163539969 ) ) ;
#3701=CARTESIAN_POINT ( 'NONE',  ( -1.914021115237000137, -4.754295778036220277, 6.069404563272239983 ) ) ;
#3708=CARTESIAN_POINT ( 'NONE',  ( -0.08231150243516484333, -5.298516949152545230, 2.050000000000001155 ) ) ;
#3712=CARTESIAN_POINT ( 'NONE',  ( 0.03714311608463249925, -1.078587104846649991, 7.053160869216429596 ) ) ;
#3714=CARTESIAN_POINT ( 'NONE',  ( -2.199335452462570117, -1.866548030288480042, 3.862342996790939953 ) ) ;
#3715=CARTESIAN_POINT ( 'NONE',  ( -2.416676968769249090, -0.2046610169491529518, 5.796598111919839980 ) ) ;
#3718=CARTESIAN_POINT ( 'NONE',  ( 1.747582379783020778, -0.1156779661016950206, 6.697200745122486865 ) ) ;
#3720=CARTESIAN_POINT ( 'NONE',  ( 1.661700935665417544, -5.037501140877957084, 3.038299064334577082 ) ) ;
#3724=CARTESIAN_POINT ( 'NONE',  ( 0.4735094604799088280, -1.032010528270080219, 7.005327412390689901 ) ) ;
#3725=CARTESIAN_POINT ( 'NONE',  ( -0.3743405594629430344, -5.457627118644070130, 7.023440622744399953 ) ) ;
#3726=CARTESIAN_POINT ( 'NONE',  ( 2.006003143956041068, -0.8689925102520592581, 6.437545705712618194 ) ) ;
#3729=CARTESIAN_POINT ( 'NONE',  ( -2.231116159141639965, -4.688271789531330391, 3.951089877392499616 ) ) ;
#3730=CARTESIAN_POINT ( 'NONE',  ( 1.579331079541870686, -4.358394877135324030, 6.832797935622368257 ) ) ;
#3734=CARTESIAN_POINT ( 'NONE',  ( 1.903446074666960364, -3.919758276017824006, 5.469282057156545029 ) ) ;
#3738=CARTESIAN_POINT ( 'NONE',  ( -2.018065005288401270, -1.427911429170979352, 5.077247235985114848 ) ) ;
#3743=CARTESIAN_POINT ( 'NONE',  ( -2.594645788401189090, -2.988226744486289999, 5.257608218854294968 ) ) ;
#3749=CARTESIAN_POINT ( 'NONE',  ( 1.289141334274990447, -5.117584745762705722, 6.297747079672416426 ) ) ;
#3754=CARTESIAN_POINT ( 'NONE',  ( -1.652654650382402668, -4.804713230972782689, 3.029252778805632484 ) ) ;
#3758=CARTESIAN_POINT ( 'NONE',  ( 1.943632316591230147, -5.346398305084740343, 3.373048379518159834 ) ) ;
#3759=CARTESIAN_POINT ( 'NONE',  ( 2.639965200365849363, -3.849893411152959910, 4.971472712918224346 ) ) ;
#3761=CARTESIAN_POINT ( 'NONE',  ( -2.435897774776361491, -3.240557039297494057, 5.753335522918235689 ) ) ;
#3765=CARTESIAN_POINT ( 'NONE',  ( 0.4201920264139500372, -3.477280798540340001, 2.384360920086630031 ) ) ;
#3770=CARTESIAN_POINT ( 'NONE',  ( 2.653064503426820764, -2.565196678937129438, 4.766048721853534786 ) ) ;
#3775=CARTESIAN_POINT ( 'NONE',  ( 1.889104232906359870, -0.3444915254237289615, 3.296507079072520163 ) ) ;
#3776=CARTESIAN_POINT ( 'NONE',  ( -0.3752419433106839453, -1.424070552810999812, 7.023346545710370314 ) ) ;
#3780=CARTESIAN_POINT ( 'NONE',  ( -0.5889081234606770021, -5.462076271186440124, 6.978529000034869867 ) ) ;
#3788=CARTESIAN_POINT ( 'NONE',  ( -2.295719155670160383, -3.287133615874060055, 5.218091927917240191 ) ) ;
#3791=CARTESIAN_POINT ( 'NONE',  ( 1.300961508564179914, -5.422033898305079092, 6.661123742937279602 ) ) ;
#3794=CARTESIAN_POINT ( 'NONE',  ( -1.417709711196470046, -2.006277760018209566, 2.821478011237799954 ) ) ;
#3798=CARTESIAN_POINT ( 'NONE',  ( 1.985741519624368845, -2.495331814072259569, 4.178720363079467148 ) ) ;
#3800=CARTESIAN_POINT ( 'NONE',  ( -0.4974685680287780354, -0.4601694915254240237, 7.000224381598740386 ) ) ;
#3803=CARTESIAN_POINT ( 'NONE',  ( -1.449568901432419343, -0.2625000000000002331, 3.250431098567584165 ) ) ;
#3814=CARTESIAN_POINT ( 'NONE',  ( -2.116444151961480280, -5.246610169491529696, 3.670839500609359707 ) ) ;
#3817=CARTESIAN_POINT ( 'NONE',  ( -2.426866425021068974, -4.711560077819614278, 3.626019996130659617 ) ) ;
#3821=CARTESIAN_POINT ( 'NONE',  ( -1.953802435660519921, -4.987178660919110662, 4.069478085301024173 ) ) ;
#3823=CARTESIAN_POINT ( 'NONE',  ( 2.203023580853990193, -0.05783898305084790581, 3.872235369154280349 ) ) ;
#3825=CARTESIAN_POINT ( 'NONE',  ( 2.340070819011249803, -0.3800847457627120063, 4.950151441910540129 ) ) ;
#3832=CARTESIAN_POINT ( 'NONE',  ( -0.6150581927481592048, -1.148451969711520082, 6.971662190339330323 ) ) ;
#3833=CARTESIAN_POINT ( 'NONE',  ( 0.2812789908084389889, -5.444279661016950378, 7.036533610117280624 ) ) ;
#3834=CARTESIAN_POINT ( 'NONE',  ( -1.947945325730720434, -1.288181699441250050, 6.502393603230366637 ) ) ;
#3835=ORIENTED_EDGE ( 'NONE', *, *, #528, .F. ) ;
#3838=CARTESIAN_POINT ( 'NONE',  ( -1.303621121494419999, -4.362235753495300905, 6.659417683669699883 ) ) ;
#3841=CARTESIAN_POINT ( 'NONE',  ( 2.050563521385710075, -1.004881363621820567, 4.800454404529174823 ) ) ;
#3847=CARTESIAN_POINT ( 'NONE',  ( 1.392553072310509510, -0.3355932203389832558, 3.191531554476519261 ) ) ;
#3849=CARTESIAN_POINT ( 'NONE',  ( 2.652303127816839190, -2.266289807549351387, 4.791661394135748431 ) ) ;
#3853=CARTESIAN_POINT ( 'NONE',  ( 1.695509042132770761, -5.346398305084745672, 3.542446458728613301 ) ) ;
#3856=CARTESIAN_POINT ( 'NONE',  ( 2.332582362116870200, -5.368644067796609853, 4.387643303570810005 ) ) ;
#3859=CARTESIAN_POINT ( 'NONE',  ( -1.194742379459959869, -5.475423728813559876, 6.727584234649759409 ) ) ;
#3860=CARTESIAN_POINT ( 'NONE',  ( -2.626509418457480649, -4.571830348089889640, 5.080213055741825023 ) ) ;
#3864=CARTESIAN_POINT ( 'NONE',  ( -2.053221424930790295, -4.734848366107910600, 3.549770689668290125 ) ) ;
#3868=CARTESIAN_POINT ( 'NONE',  ( 2.619177996481910853, -2.518620102360551893, 4.272191262657148769 ) ) ;
#3871=CARTESIAN_POINT ( 'NONE',  ( 1.978267656359410154, -0.4023305084745769644, 5.974740860598790171 ) ) ;
#3872=CARTESIAN_POINT ( 'NONE',  ( 0.4985810152601650724, -1.330917399657850053, 7.000035360316460675 ) ) ;
#3875=CARTESIAN_POINT ( 'NONE',  ( 1.932035991685901122, -5.038983050847454237, 2.884370051397200818 ) ) ;
#3883=CARTESIAN_POINT ( 'NONE',  ( 2.262450597846779932, -4.195376859117310175, 5.348122657979680561 ) ) ;
#3885=CARTESIAN_POINT ( 'NONE',  ( -2.270487904532170198, -5.537711864406779760, 4.080813552109679776 ) ) ;
#3888=CARTESIAN_POINT ( 'NONE',  ( -2.062913653388399826, -3.217268751009200400, 5.832754583370829415 ) ) ;
#3890=CARTESIAN_POINT ( 'NONE',  ( -0.6965028529798926726, -1.470647129387581575, 6.631265289497783044 ) ) ;
#3895=( NAMED_UNIT ( * ) SI_UNIT ( $, .STERADIAN. ) SOLID_ANGLE_UNIT ( ) );
#3900=CARTESIAN_POINT ( 'NONE',  ( -1.248294325655370018, -5.273305084745760318, 2.704938983774309857 ) ) ;
#3903=CARTESIAN_POINT ( 'NONE',  ( 1.282210379528780031, -0.9388573751169240200, 6.673494927815259992 ) ) ;
#3905=CARTESIAN_POINT ( 'NONE',  ( -1.981271652668300298, -1.633665147405599871, 5.970160748022450115 ) ) ;
#3906=CARTESIAN_POINT ( 'NONE',  ( 1.194742379459969861, -0.1245762711864410038, 6.727584234649759409 ) ) ;
#3908=CARTESIAN_POINT ( 'NONE',  ( 0.1565249325564390115, -0.4468220338983060480, 7.048192310558509810 ) ) ;
#3910=CARTESIAN_POINT ( 'NONE',  ( 1.057242234132090175, -0.02224576271186469792, 2.597442975781520058 ) ) ;
#3913=CARTESIAN_POINT ( 'NONE',  ( 0.7435598031058588964, -2.569037555297099651, 6.932904947974519949 ) ) ;
#3914=CARTESIAN_POINT ( 'NONE',  ( -1.194742379459959869, -5.475423728813559876, 6.727584234649759409 ) ) ;
#3916=CARTESIAN_POINT ( 'NONE',  ( -2.642463257358080853, -1.451199717459271454, 4.945970783863430142 ) ) ;
#3918=CARTESIAN_POINT ( 'NONE',  ( -0.4649462444738060030, -5.251463457376920552, 2.383584851084299849 ) ) ;
#3921=CARTESIAN_POINT ( 'NONE',  ( 2.308170020371300257, -3.873181699441239800, 5.159452766389609479 ) ) ;
#3923=CARTESIAN_POINT ( 'NONE',  ( -1.882879255550339082, -5.103620102360555855, 2.835213315261639000 ) ) ;
#3927=CARTESIAN_POINT ( 'NONE',  ( -2.050994839075679366, -4.618406924666464519, 4.608774933727191048 ) ) ;
#3932=CARTESIAN_POINT ( 'NONE',  ( 0.7785957873161482024, -1.940253771513320125, 2.162894899107371316 ) ) ;
#3935=CARTESIAN_POINT ( 'NONE',  ( 2.051331987628511211, -5.373093220338980736, 4.618035453557344461 ) ) ;
#3939=CARTESIAN_POINT ( 'NONE',  ( 1.925796468768800063, -5.404237288135590234, 6.052706598917719560 ) ) ;
#3943=CARTESIAN_POINT ( 'NONE',  ( 2.224278379903029901, -5.390889830508481140, 5.468825643806100700 ) ) ;
#3946=CARTESIAN_POINT ( 'NONE',  ( 2.349129089426440054, -0.7059744922340409623, 4.842612091679070474 ) ) ;
#3947=CARTESIAN_POINT ( 'NONE',  ( 1.945845091385960401, -3.939205687946139900, 2.895339208235789830 ) ) ;
#3950=CARTESIAN_POINT ( 'NONE',  ( 1.772995665808909660, -0.8224159336754829353, 5.735078843205156041 ) ) ;
#3955=CARTESIAN_POINT ( 'NONE',  ( 1.755774834792110051, -5.260597430386769524, 2.944225165207890349 ) ) ;
#3957=CARTESIAN_POINT ( 'NONE',  ( 0.08231150243515643339, -0.3014830508474583004, 2.050000000000001155 ) ) ;
#3958=CARTESIAN_POINT ( 'NONE',  ( -1.507201387235980183, -3.124115597856050197, 6.507509243627219497 ) ) ;
#3961=CARTESIAN_POINT ( 'NONE',  ( 1.254903241568450900, -5.426483050847465073, 7.038391080368498365 ) ) ;
#3965=CARTESIAN_POINT ( 'NONE',  ( -0.008736317425859809610, -0.5884632335339400333, 2.411138844410809501 ) ) ;
#3968=CARTESIAN_POINT ( 'NONE',  ( 1.571912189623089873, -4.335106588847041031, 6.451524409078630562 ) ) ;
#3973=CARTESIAN_POINT ( 'NONE',  ( 1.962536940652990003, -2.704926408666860294, 5.998920491814760503 ) ) ;
#3975=CARTESIAN_POINT ( 'NONE',  ( -1.798783563193318891, -3.217268751009201289, 5.689585537188996511 ) ) ;
#3978=CARTESIAN_POINT ( 'NONE',  ( -0.8147348917079840769, -0.2831443699174389650, 2.488757019513870183 ) ) ;
#3980=CARTESIAN_POINT ( 'NONE',  ( -0.4735094604798580353, -4.567989471729919870, 7.005327412390699671 ) ) ;
#3987=CARTESIAN_POINT ( 'NONE',  ( 0.4339619423229844619, -5.139830508474575232, 6.706578715862737461 ) ) ;
#3993=CARTESIAN_POINT ( 'NONE',  ( -1.458615186838411626, -5.103620102360555855, 3.259477383973569786 ) ) ;
#3994=CARTESIAN_POINT ( 'NONE',  ( -1.873832970144350130, -0.2625000000000002331, 2.826167029855650270 ) ) ;
#3996=CARTESIAN_POINT ( 'NONE',  ( 1.978267656359410154, -0.4023305084745769644, 5.974740860598790171 ) ) ;
#3997=ORIENTED_EDGE ( 'NONE', *, *, #6717, .T. ) ;
#3998=CARTESIAN_POINT ( 'NONE',  ( 1.554165089654128584, -0.1201271186440679706, 6.851145244874527584 ) ) ;
#4002=CARTESIAN_POINT ( 'NONE',  ( -1.167621112247339887, -2.778632149891699932, 6.743381174846779125 ) ) ;
#4004=CARTESIAN_POINT ( 'NONE',  ( 2.416676968769261080, -5.395338983050850246, 5.796598111919825769 ) ) ;
#4006=CARTESIAN_POINT ( 'NONE',  ( -1.155768864438580179, -1.195028546288090743, 7.088998121597467339 ) ) ;
#4008=CARTESIAN_POINT ( 'NONE',  ( 1.794646911016580137, -1.167899381639829981, 6.222494056560660347 ) ) ;
#4009=CARTESIAN_POINT ( 'NONE',  ( -2.291237445532080308, -4.664983501243040287, 4.162434510291849854 ) ) ;
#4013=CARTESIAN_POINT ( 'NONE',  ( -1.966895454505930729, -1.703530012270459970, 5.288408118292069915 ) ) ;
#4014=PRODUCT_DEFINITION_SHAPE ( 'NONE', 'NONE',  #2227 ) ;
#4019=CARTESIAN_POINT ( 'NONE',  ( -1.782460458101500889, -0.2002118644067801267, 5.718585207845990226 ) ) ;
#4020=CARTESIAN_POINT ( 'NONE',  ( -1.853635285637788899, -4.408812330071866015, 6.599249831075526984 ) ) ;
#4023=CARTESIAN_POINT ( 'NONE',  ( -1.652654650382400003, -4.804713230972780025, 3.029252778805629820 ) ) ;
#4024=CARTESIAN_POINT ( 'NONE',  ( -1.754713504580578842, -5.251059322033895249, 3.634325740584633646 ) ) ;
#4026=CARTESIAN_POINT ( 'NONE',  ( 0.07299321914061039640, -0.001483050847457899725, 2.350000000000000089 ) ) ;
#4030=( BOUNDED_SURFACE ( )  B_SPLINE_SURFACE ( 3, 3, ( 
 ( #2354, #17424, #4744, #13450, #10394, #17584, #16134, #14746, #16228, #9184, #14846, #1233, #16875, #13649, #6596, #12523, #16511, #18136, #4094, #3825, #1051, #8810, #16959, #4268, #5852, #118, #11408, #10026, #7593, #12142, #16208, #7507, #4803, #9160, #5094, #2603, #9726, #3800, #10938, #6857, #13976, #2332, #9817, #10095, #7309, #13047, #367, #12956, #13222, #11649, #3491, #6268, #5265, #2669, #11086, #2308, #11275, #5803, #10073, #2848, #325, #11603 ),
 ( #15785, #6987, #4391, #14111, #2926, #15703, #8738, #7098, #12737, #3012, #5701, #14216, #7362, #11345, #16980, #3183, #17232, #4292, #4551, #137, #10205, #15873, #8836, #5608, #9864, #15523, #7184, #12634, #12824, #11427, #16321, #13356, #13448, #13172, #10310, #7712, #6226, #17685, #16226, #762, #15974, #2058, #489, #11800, #3354, #6395, #670, #12064, #17582, #11885, #6308, #8996, #6136, #17422, #14646, #3278, #8919, #5021, #14567, #2159, #1880, #10676 ),
 ( #11968, #13091, #9082, #7800, #13266, #3534, #409, #1807, #4915, #3626, #1959, #9276, #7450, #6048, #4742, #11694, #10571, #4826, #17322, #4652, #10476, #7528, #10392, #17505, #7618, #14744, #16132, #16056, #587, #3432, #9181, #14844, #10958, #2526, #6687, #11038, #5114, #8001, #1142, #13917, #1048, #2247, #13732, #16508, #15316, #6876, #13547, #3715, #5484, #6787, #1230, #10863, #11126, #13647, #17870, #9368, #9472, #12435, #15220, #8276, #2625, #3994 ),
 ( #13819, #18134, #14937, #8173, #4090, #16686, #15133, #7897, #10767, #18054, #16410, #12248, #5209, #16606, #3823, #12521, #2445, #8091, #9561, #16778, #5398, #864, #12344, #15042, #17965, #5311, #9648, #2352, #958, #3906, #6594, #6505, #12164, #17780, #8448, #5940, #12888, #14082, #3072, #2901, #14360, #11406, #8716, #2718, #8363, #18234, #12611, #2995, #13997, #11322, #11579, #8635, #1684, #2804, #5584, #14280, #14195, #7335, #5851, #12980, #11228, #1603 ),
 ( #1513, #16873, #204, #6962, #301, #7247, #9749, #1315, #4181, #9840, #11499, #15414, #16958, #4455, #17210, #15587, #4266, #15494, #8548, #10113, #1413, #7074, #12716, #33, #7166, #5678, #9927, #12804, #5764, #9158, #565, #14821, #3152, #13067, #11776, #6992, #8302, #5426, #2380, #980, #11063, #4208, #5612, #12461, #2546, #15345, #4019, #5234, #12640, #8201, #12274, #6716, #9674, #13940, #18078, #16806, #10889, #13751, #6901, #18266, #2651, #16539 ),
 ( #8114, #8390, #1071, #11256, #12371, #1168, #1256, #5339, #12551, #3847, #16631, #9501, #17993, #14026, #18160, #13848, #16900, #5508, #9868, #4118, #9776, #140, #14385, #14304, #7269, #12912, #17236, #5788, #10210, #15527, #5882, #7454, #58, #13094, #11430, #7102, #4475, #14117, #12742, #5704, #16135, #17689, #7715, #7622, #17782, #13358, #6310, #9371, #12252, #8367, #6689, #9564, #13822, #11581, #5587, #4270, #5766, #14284, #12890, #9163, #13337, #11948 ),
 ( #14823, #10657, #7780, #15293, #1030, #12504, #10746, #6667, #7051, #5742, #8618, #14261, #180, #11477, #7312, #6006, #7490, #3495, #13138, #15924, #10436, #4877, #10523, #14610, #11750, #7573, #2015, #4980, #14802, #2112, #4600, #11844, #17466, #4701, #3394, #9038, #15832, #3131, #2312, #3678, #8057, #12301, #13699, #1010, #9234, #14897, #13607, #7962, #6646, #16373, #2410, #17745, #1096, #7853, #16653, #9525, #10635, #2209, #13504, #822, #10921, #16284 ) ),
 .UNSPECIFIED., .T., .F., .F. ) 
 B_SPLINE_SURFACE_WITH_KNOTS ( ( 4, 3, 4 ),
 ( 4, 1, 1, 1, 1, 1, 1, 1, 1, 1, 1, 1, 1, 1, 1, 1, 1, 1, 1, 1, 1, 1, 1, 1, 1, 1, 1, 1, 1, 1, 1, 1, 1, 1, 1, 1, 1, 1, 1, 1, 1, 1, 1, 1, 1, 1, 1, 1, 1, 1, 1, 1, 1, 1, 1, 1, 1, 1, 1, 4 ),
 ( 0.000000000000000000, 3.141592653589790007, 6.283185307179590673 ),
 ( 0.000000000000000000, 0.09318283294545999518, 0.1863656658909199904, 0.2795484988363799994, 0.3727313317818399807, 0.4659141647273000175, 0.5590969976727599988, 0.6522798306182200356, 0.7454626635636799614, 0.8386454965091399982, 0.9318283294545990358, 1.025011162400059961, 1.118193995345519998, 1.211376828290979812, 1.304559661236440071, 1.397742494181900108, 1.490925327127359923, 1.584108160072819960, 1.677290993018279996, 1.770473825963740033, 1.863656658909200070, 1.956839491854659885, 2.050022324800119922, 2.143205157745580181, 2.236387990691039995, 2.329570823636499810, 2.422753656581960069, 2.515936489527420328, 2.609119322472880143, 2.702302155418339957, 2.795484988363799772, 2.888667821309260031, 2.981850654254720290, 3.075033487200180105, 3.168216320145639919, 3.261399153091099734, 3.354581986036559993, 3.447764818982019808, 3.540947651927480067, 3.634130484872939881, 3.727313317818400140, 3.820496150763859955, 3.913678983709319770, 4.006861816654780029, 4.100044649600239843, 4.193227482545699658, 4.286410315491160361, 4.379593148436620176, 4.472775981382079991, 4.565958814327539805, 4.659141647272999620, 4.752324480218450553, 4.845507313163910368, 4.938690146109370183, 5.031872979054829997, 5.125055812000289812, 5.218238644945749627, 5.311421477891210330, 5.404604310836670145, 5.497787143782139729 ),
 .UNSPECIFIED. ) 
 GEOMETRIC_REPRESENTATION_ITEM ( )  RATIONAL_B_SPLINE_SURFACE ( (
 ( 1.000000000000000000, 1.000000000000000000, 1.000000000000000000, 1.000000000000000000, 1.000000000000000000, 1.000000000000000000, 1.000000000000000000, 1.000000000000000000, 1.000000000000000000, 1.000000000000000000, 1.000000000000000000, 1.000000000000000000, 1.000000000000000000, 1.000000000000000000, 1.000000000000000000, 1.000000000000000000, 1.000000000000000000, 1.000000000000000000, 1.000000000000000000, 1.000000000000000000, 1.000000000000000000, 1.000000000000000000, 1.000000000000000000, 1.000000000000000000, 1.000000000000000000, 1.000000000000000000, 1.000000000000000000, 1.000000000000000000, 1.000000000000000000, 1.000000000000000000, 1.000000000000000000, 1.000000000000000000, 1.000000000000000000, 1.000000000000000000, 1.000000000000000000, 1.000000000000000000, 1.000000000000000000, 1.000000000000000000, 1.000000000000000000, 1.000000000000000000, 1.000000000000000000, 1.000000000000000000, 1.000000000000000000, 1.000000000000000000, 1.000000000000000000, 1.000000000000000000, 1.000000000000000000, 1.000000000000000000, 1.000000000000000000, 1.000000000000000000, 1.000000000000000000, 1.000000000000000000, 1.000000000000000000, 1.000000000000000000, 1.000000000000000000, 1.000000000000000000, 1.000000000000000000, 1.000000000000000000, 1.000000000000000000, 1.000000000000000000, 1.000000000000000000, 1.000000000000000000),
 ( 0.3333333333333329818, 0.3333333333333329818, 0.3333333333333329818, 0.3333333333333329818, 0.3333333333333329818, 0.3333333333333329818, 0.3333333333333329818, 0.3333333333333329818, 0.3333333333333329818, 0.3333333333333329818, 0.3333333333333329818, 0.3333333333333329818, 0.3333333333333329818, 0.3333333333333329818, 0.3333333333333329818, 0.3333333333333329818, 0.3333333333333329818, 0.3333333333333329818, 0.3333333333333329818, 0.3333333333333329818, 0.3333333333333329818, 0.3333333333333329818, 0.3333333333333329818, 0.3333333333333329818, 0.3333333333333329818, 0.3333333333333329818, 0.3333333333333329818, 0.3333333333333329818, 0.3333333333333329818, 0.3333333333333329818, 0.3333333333333329818, 0.3333333333333329818, 0.3333333333333329818, 0.3333333333333329818, 0.3333333333333329818, 0.3333333333333329818, 0.3333333333333329818, 0.3333333333333329818, 0.3333333333333329818, 0.3333333333333329818, 0.3333333333333329818, 0.3333333333333329818, 0.3333333333333329818, 0.3333333333333329818, 0.3333333333333329818, 0.3333333333333329818, 0.3333333333333329818, 0.3333333333333329818, 0.3333333333333329818, 0.3333333333333329818, 0.3333333333333329818, 0.3333333333333329818, 0.3333333333333329818, 0.3333333333333329818, 0.3333333333333329818, 0.3333333333333329818, 0.3333333333333329818, 0.3333333333333329818, 0.3333333333333329818, 0.3333333333333329818, 0.3333333333333329818, 0.3333333333333329818),
 ( 0.3333333333333329818, 0.3333333333333329818, 0.3333333333333329818, 0.3333333333333329818, 0.3333333333333329818, 0.3333333333333329818, 0.3333333333333329818, 0.3333333333333329818, 0.3333333333333329818, 0.3333333333333329818, 0.3333333333333329818, 0.3333333333333329818, 0.3333333333333329818, 0.3333333333333329818, 0.3333333333333329818, 0.3333333333333329818, 0.3333333333333329818, 0.3333333333333329818, 0.3333333333333329818, 0.3333333333333329818, 0.3333333333333329818, 0.3333333333333329818, 0.3333333333333329818, 0.3333333333333329818, 0.3333333333333329818, 0.3333333333333329818, 0.3333333333333329818, 0.3333333333333329818, 0.3333333333333329818, 0.3333333333333329818, 0.3333333333333329818, 0.3333333333333329818, 0.3333333333333329818, 0.3333333333333329818, 0.3333333333333329818, 0.3333333333333329818, 0.3333333333333329818, 0.3333333333333329818, 0.3333333333333329818, 0.3333333333333329818, 0.3333333333333329818, 0.3333333333333329818, 0.3333333333333329818, 0.3333333333333329818, 0.3333333333333329818, 0.3333333333333329818, 0.3333333333333329818, 0.3333333333333329818, 0.3333333333333329818, 0.3333333333333329818, 0.3333333333333329818, 0.3333333333333329818, 0.3333333333333329818, 0.3333333333333329818, 0.3333333333333329818, 0.3333333333333329818, 0.3333333333333329818, 0.3333333333333329818, 0.3333333333333329818, 0.3333333333333329818, 0.3333333333333329818, 0.3333333333333329818),
 ( 1.000000000000000000, 1.000000000000000000, 1.000000000000000000, 1.000000000000000000, 1.000000000000000000, 1.000000000000000000, 1.000000000000000000, 1.000000000000000000, 1.000000000000000000, 1.000000000000000000, 1.000000000000000000, 1.000000000000000000, 1.000000000000000000, 1.000000000000000000, 1.000000000000000000, 1.000000000000000000, 1.000000000000000000, 1.000000000000000000, 1.000000000000000000, 1.000000000000000000, 1.000000000000000000, 1.000000000000000000, 1.000000000000000000, 1.000000000000000000, 1.000000000000000000, 1.000000000000000000, 1.000000000000000000, 1.000000000000000000, 1.000000000000000000, 1.000000000000000000, 1.000000000000000000, 1.000000000000000000, 1.000000000000000000, 1.000000000000000000, 1.000000000000000000, 1.000000000000000000, 1.000000000000000000, 1.000000000000000000, 1.000000000000000000, 1.000000000000000000, 1.000000000000000000, 1.000000000000000000, 1.000000000000000000, 1.000000000000000000, 1.000000000000000000, 1.000000000000000000, 1.000000000000000000, 1.000000000000000000, 1.000000000000000000, 1.000000000000000000, 1.000000000000000000, 1.000000000000000000, 1.000000000000000000, 1.000000000000000000, 1.000000000000000000, 1.000000000000000000, 1.000000000000000000, 1.000000000000000000, 1.000000000000000000, 1.000000000000000000, 1.000000000000000000, 1.000000000000000000),
 ( 0.3333333333333329818, 0.3333333333333329818, 0.3333333333333329818, 0.3333333333333329818, 0.3333333333333329818, 0.3333333333333329818, 0.3333333333333329818, 0.3333333333333329818, 0.3333333333333329818, 0.3333333333333329818, 0.3333333333333329818, 0.3333333333333329818, 0.3333333333333329818, 0.3333333333333329818, 0.3333333333333329818, 0.3333333333333329818, 0.3333333333333329818, 0.3333333333333329818, 0.3333333333333329818, 0.3333333333333329818, 0.3333333333333329818, 0.3333333333333329818, 0.3333333333333329818, 0.3333333333333329818, 0.3333333333333329818, 0.3333333333333329818, 0.3333333333333329818, 0.3333333333333329818, 0.3333333333333329818, 0.3333333333333329818, 0.3333333333333329818, 0.3333333333333329818, 0.3333333333333329818, 0.3333333333333329818, 0.3333333333333329818, 0.3333333333333329818, 0.3333333333333329818, 0.3333333333333329818, 0.3333333333333329818, 0.3333333333333329818, 0.3333333333333329818, 0.3333333333333329818, 0.3333333333333329818, 0.3333333333333329818, 0.3333333333333329818, 0.3333333333333329818, 0.3333333333333329818, 0.3333333333333329818, 0.3333333333333329818, 0.3333333333333329818, 0.3333333333333329818, 0.3333333333333329818, 0.3333333333333329818, 0.3333333333333329818, 0.3333333333333329818, 0.3333333333333329818, 0.3333333333333329818, 0.3333333333333329818, 0.3333333333333329818, 0.3333333333333329818, 0.3333333333333329818, 0.3333333333333329818),
 ( 0.3333333333333329818, 0.3333333333333329818, 0.3333333333333329818, 0.3333333333333329818, 0.3333333333333329818, 0.3333333333333329818, 0.3333333333333329818, 0.3333333333333329818, 0.3333333333333329818, 0.3333333333333329818, 0.3333333333333329818, 0.3333333333333329818, 0.3333333333333329818, 0.3333333333333329818, 0.3333333333333329818, 0.3333333333333329818, 0.3333333333333329818, 0.3333333333333329818, 0.3333333333333329818, 0.3333333333333329818, 0.3333333333333329818, 0.3333333333333329818, 0.3333333333333329818, 0.3333333333333329818, 0.3333333333333329818, 0.3333333333333329818, 0.3333333333333329818, 0.3333333333333329818, 0.3333333333333329818, 0.3333333333333329818, 0.3333333333333329818, 0.3333333333333329818, 0.3333333333333329818, 0.3333333333333329818, 0.3333333333333329818, 0.3333333333333329818, 0.3333333333333329818, 0.3333333333333329818, 0.3333333333333329818, 0.3333333333333329818, 0.3333333333333329818, 0.3333333333333329818, 0.3333333333333329818, 0.3333333333333329818, 0.3333333333333329818, 0.3333333333333329818, 0.3333333333333329818, 0.3333333333333329818, 0.3333333333333329818, 0.3333333333333329818, 0.3333333333333329818, 0.3333333333333329818, 0.3333333333333329818, 0.3333333333333329818, 0.3333333333333329818, 0.3333333333333329818, 0.3333333333333329818, 0.3333333333333329818, 0.3333333333333329818, 0.3333333333333329818, 0.3333333333333329818, 0.3333333333333329818),
 ( 1.000000000000000000, 1.000000000000000000, 1.000000000000000000, 1.000000000000000000, 1.000000000000000000, 1.000000000000000000, 1.000000000000000000, 1.000000000000000000, 1.000000000000000000, 1.000000000000000000, 1.000000000000000000, 1.000000000000000000, 1.000000000000000000, 1.000000000000000000, 1.000000000000000000, 1.000000000000000000, 1.000000000000000000, 1.000000000000000000, 1.000000000000000000, 1.000000000000000000, 1.000000000000000000, 1.000000000000000000, 1.000000000000000000, 1.000000000000000000, 1.000000000000000000, 1.000000000000000000, 1.000000000000000000, 1.000000000000000000, 1.000000000000000000, 1.000000000000000000, 1.000000000000000000, 1.000000000000000000, 1.000000000000000000, 1.000000000000000000, 1.000000000000000000, 1.000000000000000000, 1.000000000000000000, 1.000000000000000000, 1.000000000000000000, 1.000000000000000000, 1.000000000000000000, 1.000000000000000000, 1.000000000000000000, 1.000000000000000000, 1.000000000000000000, 1.000000000000000000, 1.000000000000000000, 1.000000000000000000, 1.000000000000000000, 1.000000000000000000, 1.000000000000000000, 1.000000000000000000, 1.000000000000000000, 1.000000000000000000, 1.000000000000000000, 1.000000000000000000, 1.000000000000000000, 1.000000000000000000, 1.000000000000000000, 1.000000000000000000, 1.000000000000000000, 1.000000000000000000) ) ) 
 REPRESENTATION_ITEM ( '' )  SURFACE ( )  );
#4031=CARTESIAN_POINT ( 'NONE',  ( -1.750316316486840051, -5.559957627118639500, 3.126818518378589928 ) ) ;
#4032=CARTESIAN_POINT ( 'NONE',  ( 2.065623031241559548, -0.5662447625043109944, 3.572193642975259653 ) ) ;
#4036=CARTESIAN_POINT ( 'NONE',  ( -2.053018524985070314, -1.474488005747551567, 4.695903819313384631 ) ) ;
#4044=CARTESIAN_POINT ( 'NONE',  ( 1.973760952634081134, -0.3400423728813561364, 2.925986839873718992 ) ) ;
#4046=CARTESIAN_POINT ( 'NONE',  ( 1.832842064134690085, -2.728214696955149954, 6.176291182464479945 ) ) ;
#4049=CARTESIAN_POINT ( 'NONE',  ( -1.192209327851089240, -5.577754237288145234, 2.329031440774910422 ) ) ;
#4058=CARTESIAN_POINT ( 'NONE',  ( -1.626408692231610109, -4.707719201459649838, 6.401040991074980369 ) ) ;
#4059=CARTESIAN_POINT ( 'NONE',  ( 1.147638118088980086, -5.328211948015596278, 2.987995008461610702 ) ) ;
#4063=CARTESIAN_POINT ( 'NONE',  ( 2.342931736853870017, -4.102223705964150646, 4.477701633099130163 ) ) ;
#4066=CARTESIAN_POINT ( 'NONE',  ( -1.160665242129840014, -3.100827309567759205, 6.393445611273007145 ) ) ;
#4071=CARTESIAN_POINT ( 'NONE',  ( -1.221947981261169991, -0.5741044150835520332, 2.670403636935529956 ) ) ;
#4081=CARTESIAN_POINT ( 'NONE',  ( -0.2189795514005259958, -5.295550847457629828, 2.356806637999020015 ) ) ;
#4088=CARTESIAN_POINT ( 'NONE',  ( -1.703239418290670049, -5.057043525783965876, 3.553755118148739900 ) ) ;
#4089=CARTESIAN_POINT ( 'NONE',  ( -1.712910428781911021, -2.895073591333140239, 5.831741890007735130 ) ) ;
#4090=CARTESIAN_POINT ( 'NONE',  ( 0.6493550500446280127, -0.01334745762711890028, 2.437955526623099889 ) ) ;
#4094=CARTESIAN_POINT ( 'NONE',  ( 2.353194804772640314, -0.3756355932203400139, 4.731327187377229571 ) ) ;
#4095=CARTESIAN_POINT ( 'NONE',  ( -0.2812789908084309953, -0.4557203389830509765, 7.036533610117280624 ) ) ;
#4097=CARTESIAN_POINT ( 'NONE',  ( 1.000896394980339998, -0.1290254237288140093, 6.829956240957369751 ) ) ;
#4098=CARTESIAN_POINT ( 'NONE',  ( 2.331386066015260106, -0.9583047870452390260, 4.378465089518139841 ) ) ;
#4104=CARTESIAN_POINT ( 'NONE',  ( -2.301223891756910334, -2.988226744486290887, 5.193066210047998510 ) ) ;
#4105=CARTESIAN_POINT ( 'NONE',  ( 2.519547246525509543, -5.359745762711870753, 3.866491354109194756 ) ) ;
#4107=CARTESIAN_POINT ( 'NONE',  ( -0.1569242594330230167, -1.400782264522720144, 7.048216443236290374 ) ) ;
#4108=CARTESIAN_POINT ( 'NONE',  ( 1.438959988998139914E-16, -0.2999999999999999889, 2.350000000000000089 ) ) ;
#4114=CARTESIAN_POINT ( 'NONE',  ( -1.903446074666951260, -1.680241723982170754, 5.469282057156605426 ) ) ;
#4118=CARTESIAN_POINT ( 'NONE',  ( 2.041338374031088865, -0.3800847457627119508, 4.918217215283659627 ) ) ;
#4120=CARTESIAN_POINT ( 'NONE',  ( 1.930452136971109622, -4.012911429170968880, 6.521117305355573102 ) ) ;
#4121=CARTESIAN_POINT ( 'NONE',  ( -0.4068869028847361125, -5.251463457376924104, 2.679545647941359743 ) ) ;
#4122=CARTESIAN_POINT ( 'NONE',  ( -0.3265524029357583236, -5.157627118644064979, 6.726831181542982208 ) ) ;
#4126=DIRECTION ( 'NONE',  ( 0.7071067811865470176, 4.329780281177469511E-17, -0.7071067811865480168 ) ) ;
#4128=CARTESIAN_POINT ( 'NONE',  ( -1.687197751398160861, -0.5672554343907065810, 2.639290338773708999 ) ) ;
#4131=CARTESIAN_POINT ( 'NONE',  ( 2.281778813005790330, -0.7525510688106179513, 5.276394947932120161 ) ) ;
#4133=CARTESIAN_POINT ( 'NONE',  ( -0.5381211601353440566, -1.148451969711520082, 6.681243917250651698 ) ) ;
#4138=CARTESIAN_POINT ( 'NONE',  ( 0.4917262214558945632, -0.3088983050847459166, 2.092115739186370948 ) ) ;
#4139=CARTESIAN_POINT ( 'NONE',  ( -2.351999299633229956, -3.333710192450639820, 4.782734406438290620 ) ) ;
#4142=CARTESIAN_POINT ( 'NONE',  ( -2.601107615185130673, -5.515466101694915579, 5.226397344856384741 ) ) ;
#4145=CARTESIAN_POINT ( 'NONE',  ( -0.07299321914061848715, -5.298516949152539013, 2.350000000000000089 ) ) ;
#4146=DIRECTION ( 'NONE',  ( 1.000000000000000000, 0.000000000000000000, 0.000000000000000000 ) ) ;
#4150=CARTESIAN_POINT ( 'NONE',  ( 2.343457872958619959, -4.148800282540729967, 4.916681529328559286 ) ) ;
#4152=CARTESIAN_POINT ( 'NONE',  ( -0.009452110982655128821, -0.5998079552954630467, 2.350000000000000089 ) ) ;
#4158=CARTESIAN_POINT ( 'NONE',  ( -2.033393610350109793, -4.777584066324510381, 5.884928737465370041 ) ) ;
#4160=CARTESIAN_POINT ( 'NONE',  ( 1.599895119336370852, -2.728214696955149510, 5.986560317183676538 ) ) ;
#4170=CARTESIAN_POINT ( 'NONE',  ( -0.7476103186298618253, -5.282203389830510076, 2.787995836256459636 ) ) ;
#4172=CARTESIAN_POINT ( 'NONE',  ( 0.5385843327681005821, -1.916965483225031130, 2.101338688959521139 ) ) ;
#4177=CARTESIAN_POINT ( 'NONE',  ( -0.4649462444738060030, -5.251463457376920552, 2.383584851084299849 ) ) ;
#4179=CARTESIAN_POINT ( 'NONE',  ( -0.2023972492402590084, -2.146007489747939978, 2.355265251465770149 ) ) ;
#4180=CARTESIAN_POINT ( 'NONE',  ( 0.08304008649498713368, -2.638902420161969520, 6.751342532748487280 ) ) ;
#4181=CARTESIAN_POINT ( 'NONE',  ( 1.246151616534670215, -0.03114406779661053892, 3.068501529594759081 ) ) ;
#4184=CARTESIAN_POINT ( 'NONE',  ( 2.088297318559229954, -0.3978813559322040283, 5.785136623276629919 ) ) ;
#4187=CARTESIAN_POINT ( 'NONE',  ( 2.340070819011249803, -0.08008474576271229495, 4.950151441910540129 ) ) ;
#4188=CARTESIAN_POINT ( 'NONE',  ( -0.3752419433106839453, -1.424070552810999812, 7.023346545710370314 ) ) ;
#4191=CARTESIAN_POINT ( 'NONE',  ( 0.8986180677147457274, -1.963542059801610229, 2.524860635301610312 ) ) ;
#4193=CARTESIAN_POINT ( 'NONE',  ( -1.925836318347889931, -5.488771186440680516, 6.525927015348141680 ) ) ;
#4196=CARTESIAN_POINT ( 'NONE',  ( 1.652654650382400003, -0.7952867690272209522, 3.029252778805620050 ) ) ;
#4197=CARTESIAN_POINT ( 'NONE',  ( -1.782460458101500889, -0.5002118644067795605, 5.718585207845990226 ) ) ;
#4203=CARTESIAN_POINT ( 'NONE',  ( -0.8735826871841183561, -1.493935417675870791, 6.557889967484691773 ) ) ;
#4208=CARTESIAN_POINT ( 'NONE',  ( -1.134881315981510541, -0.1779661016949160846, 6.410767520434657918 ) ) ;
#4209=CARTESIAN_POINT ( 'NONE',  ( -0.4649462444738060030, -5.251463457376920552, 2.383584851084299849 ) ) ;
#4210=CARTESIAN_POINT ( 'NONE',  ( -1.526871680339578541, -5.259957627118655665, 3.327650196883449762 ) ) ;
#4219=CARTESIAN_POINT ( 'NONE',  ( 0.4790341583531380065, -1.916965483225030242, 2.395814251711720022 ) ) ;
#4221=CARTESIAN_POINT ( 'NONE',  ( -2.331386066015260106, -4.641695212954759953, 4.378465089518190467 ) ) ;
#4226=CARTESIAN_POINT ( 'NONE',  ( -2.043308330018790198, -0.5002118644067800046, 5.867646457774669422 ) ) ;
#4227=CARTESIAN_POINT ( 'NONE',  ( -0.04278372834682089842, -3.729611093351540063, 2.346934926511239805 ) ) ;
#4230=CARTESIAN_POINT ( 'NONE',  ( -2.614198783383141045, -5.533262711864405325, 4.243032045539295360 ) ) ;
#4237=CARTESIAN_POINT ( 'NONE',  ( -1.351547610267091581, -1.517223705964159786, 6.983951126925262542 ) ) ;
#4238=CARTESIAN_POINT ( 'NONE',  ( 1.112057765673850174, -5.020626044399135068, 2.286633591154370482 ) ) ;
#4240=CARTESIAN_POINT ( 'NONE',  ( -1.219286470748949913, -1.218316834576380181, 6.712979431025680732 ) ) ;
#4242=CARTESIAN_POINT ( 'NONE',  ( 2.343457872958619959, -4.148800282540729967, 4.916681529328559286 ) ) ;
#4244=CARTESIAN_POINT ( 'NONE',  ( -2.029711248330079876, -3.380286769027221805, 4.391497016172549728 ) ) ;
#4247=CARTESIAN_POINT ( 'NONE',  ( -0.7101077586918816964, -0.2831443699174400752, 2.770804889310179764 ) ) ;
#4257=CARTESIAN_POINT ( 'NONE',  ( 1.695509042132770761, -5.046398305084744962, 3.542446458728613301 ) ) ;
#4259=CARTESIAN_POINT ( 'NONE',  ( 1.769280637098189946, -0.6409077950170640747, 2.931315639931909800 ) ) ;
#4264=CARTESIAN_POINT ( 'NONE',  ( -1.816660071039029933, -3.170692174432619748, 6.196159040268240936 ) ) ;
#4265=CARTESIAN_POINT ( 'NONE',  ( -2.052456847059610734, -3.034803321062870651, 4.748194746458554327 ) ) ;
#4266=CARTESIAN_POINT ( 'NONE',  ( 2.022304719220918479, -0.06673728813559356987, 4.346496488058688712 ) ) ;
#4268=CARTESIAN_POINT ( 'NONE',  ( 2.088297318559229954, -0.3978813559322040283, 5.785136623276629919 ) ) ;
#4270=CARTESIAN_POINT ( 'NONE',  ( -1.949083719010310078, -0.5402542372881364852, 4.055210292801460170 ) ) ;
#4274=CARTESIAN_POINT ( 'NONE',  ( 0.1910247150515120007, -0.004449152542373194588, 2.655937705488500722 ) ) ;
#4275=CARTESIAN_POINT ( 'NONE',  ( -2.308170020371289599, -1.726818300558750074, 5.159452766389659217 ) ) ;
#4280=CARTESIAN_POINT ( 'NONE',  ( -1.214457691476030332, -1.730659176918720510, 2.684103622926371280 ) ) ;
#4282=CARTESIAN_POINT ( 'NONE',  ( 2.171642826483958899, -5.404237288135596451, 6.225392547715717484 ) ) ;
#4284=CARTESIAN_POINT ( 'NONE',  ( 2.350542563031990273, -1.004881363621820123, 4.817027120179740329 ) ) ;
#4285=CARTESIAN_POINT ( 'NONE',  ( 0.5137283630188955730, -0.4379237288135597317, 6.687652957477222770 ) ) ;
#4290=CARTESIAN_POINT ( 'NONE',  ( 1.658519201881180738, -2.402178660919109365, 3.489952108543023623 ) ) ;
#4292=CARTESIAN_POINT ( 'NONE',  ( 2.645377369053839356, -0.3711864406779670222, 4.488260618344900088 ) ) ;
#4298=CARTESIAN_POINT ( 'NONE',  ( -0.7046366965007886396, -4.911779243796845051, 2.768871435390180213 ) ) ;
#4299=CARTESIAN_POINT ( 'NONE',  ( 2.286166334984490067, -5.386440677966100488, 5.258525443163859947 ) ) ;
#4301=CARTESIAN_POINT ( 'NONE',  ( 1.248294325655349590, -0.02669491525423759587, 2.704938983774301420 ) ) ;
#4302=CARTESIAN_POINT ( 'NONE',  ( 0.9150601050661639757, -5.430932203389830626, 6.868218666554230190 ) ) ;
#4306=CARTESIAN_POINT ( 'NONE',  ( 2.036228139452630259, -2.126560077819629857, 3.519948877554369915 ) ) ;
#4309=CARTESIAN_POINT ( 'NONE',  ( -2.052456847059610734, -3.034803321062870651, 4.748194746458554327 ) ) ;
#4313=EDGE_CURVE ( 'NONE', #8096, #7005, #7631, .T. ) ;
#4315=CARTESIAN_POINT ( 'NONE',  ( -1.031876288691620625, -0.4690677966101705065, 7.145012538880312292 ) ) ;
#4316=CARTESIAN_POINT ( 'NONE',  ( -0.09706517602693919000, -2.961097579838030125, 7.051451474958980725 ) ) ;
#4319=CARTESIAN_POINT ( 'NONE',  ( 0.5609751937345880402, -5.139830508474575232, 7.293870047334757523 ) ) ;
#4326=CARTESIAN_POINT ( 'NONE',  ( -2.281778813005780115, -4.847448931189379806, 5.276394947932169899 ) ) ;
#4327=FACE_OUTER_BOUND ( 'NONE', #5387, .T. ) ;
#4330=CARTESIAN_POINT ( 'NONE',  ( 1.460675875430079929, -0.9155690868286359141, 6.545310725710029587 ) ) ;
#4333=CARTESIAN_POINT ( 'NONE',  ( -0.8986180677147959095, -3.636457940198390304, 2.524860635301629852 ) ) ;
#4336=CARTESIAN_POINT ( 'NONE',  ( 0.7128755192781456307, -3.822764246504686270, 2.774718115017441367 ) ) ;
#4345=VERTEX_POINT ( 'NONE', #11860 ) ;
#4351=CARTESIAN_POINT ( 'NONE',  ( -1.980638384804660257, -5.237711864406785267, 4.159858630563765480 ) ) ;
#4361=CARTESIAN_POINT ( 'NONE',  ( -2.283153923255329953, -3.403575057315510133, 4.129076318403500423 ) ) ;
#4363=CARTESIAN_POINT ( 'NONE',  ( -1.658519201881210714, -3.197821339080880065, 3.489952108543053377 ) ) ;
#4369=CARTESIAN_POINT ( 'NONE',  ( 0.7476103186298468373, -0.01779661016949178609, 2.787995836256459636 ) ) ;
#4370=CARTESIAN_POINT ( 'NONE',  ( 1.526791597786429922, -2.774791273531720392, 6.490992212270249695 ) ) ;
#4374=CARTESIAN_POINT ( 'NONE',  ( 2.091095264232529338, -3.943046564306110113, 5.779845490516200890 ) ) ;
#4376=CARTESIAN_POINT ( 'NONE',  ( -0.07299321914061848715, -5.598516949152539723, 2.350000000000000089 ) ) ;
#4381=CARTESIAN_POINT ( 'NONE',  ( 0.3265524029357661506, -0.4423728813559331119, 6.726831181542982208 ) ) ;
#4389=CARTESIAN_POINT ( 'NONE',  ( 1.599895119336370852, -2.728214696955149510, 5.986560317183676538 ) ) ;
#4391=CARTESIAN_POINT ( 'NONE',  ( 0.2469343877495150108, -0.3044491525423730915, 2.057675570509529539 ) ) ;
#4392=ORIENTED_EDGE ( 'NONE', *, *, #11047, .F. ) ;
#4395=DIRECTION ( 'NONE',  ( 1.000000000000000000, 9.028005242978079560E-48, -6.123233995736769734E-17 ) ) ;
#4399=CARTESIAN_POINT ( 'NONE',  ( 2.155845792290829621, -5.355296610169490101, 3.756158857535770057 ) ) ;
#4406=CARTESIAN_POINT ( 'NONE',  ( 0.2564439965879030114, -1.055298816558370101, 7.039440566481209416 ) ) ;
#4409=CARTESIAN_POINT ( 'NONE',  ( -0.5302109551885640926, -1.800524041783588824, 2.716624547488271979 ) ) ;
#4411=CARTESIAN_POINT ( 'NONE',  ( -3.161120280659493168E-15, -5.600000000000000533, 2.050000000000001155 ) ) ;
#4414=CARTESIAN_POINT ( 'NONE',  ( -2.519547246525518425, -0.5402542372881364852, 3.866491354109200529 ) ) ;
#4416=CARTESIAN_POINT ( 'NONE',  ( -2.296954468777729463, -4.963890372630819670, 4.187412587068699565 ) ) ;
#4419=CARTESIAN_POINT ( 'NONE',  ( 2.224278379903029901, -5.090889830508480429, 5.468825643806100700 ) ) ;
#4423=PLANE ( 'NONE',  #17962 ) ;
#4425=CARTESIAN_POINT ( 'NONE',  ( -2.325590009395030133, -4.870737219477670799, 5.061077271074069905 ) ) ;
#4427=CARTESIAN_POINT ( 'NONE',  ( 1.330034674284700458, -0.7763906680874423927, 3.132218110693851809 ) ) ;
#4430=CARTESIAN_POINT ( 'NONE',  ( -2.100188519621619676, -1.590929447189000090, 3.637948273607420013 ) ) ;
#4432=CARTESIAN_POINT ( 'NONE',  ( 2.262450597846779932, -4.195376859117310175, 5.348122657979680561 ) ) ;
#4435=CARTESIAN_POINT ( 'NONE',  ( 1.741179788930650840, -4.265241723982168942, 5.787747574231955738 ) ) ;
#4437=CARTESIAN_POINT ( 'NONE',  ( -1.449568901432419343, -0.5625000000000005551, 3.250431098567584165 ) ) ;
#4444=CARTESIAN_POINT ( 'NONE',  ( -1.921786527979019166, -5.542161016949150643, 3.977907449687794195 ) ) ;
#4445=CARTESIAN_POINT ( 'NONE',  ( -0.2683982510037440927, -3.407415933675483899, 2.059720455735791322 ) ) ;
#4447=CARTESIAN_POINT ( 'NONE',  ( 1.670747152266691016, -0.4963810343603142217, 3.047345280935851441 ) ) ;
#4449=CARTESIAN_POINT ( 'NONE',  ( -1.652654650382400003, -4.804713230972780025, 3.029252778805629820 ) ) ;
#4453=CARTESIAN_POINT ( 'NONE',  ( 0.3413183941262679655, -2.914521003261450360, 7.028571974690709823 ) ) ;
#4454=CARTESIAN_POINT ( 'NONE',  ( -0.6713553523422816083, -2.732055573315119723, 6.640150466718877098 ) ) ;
#4455=CARTESIAN_POINT ( 'NONE',  ( 1.846259792136599076, -0.05338983050847485173, 3.802221692020924415 ) ) ;
#4459=CARTESIAN_POINT ( 'NONE',  ( -1.818868030982659700, -3.244397915657463827, 2.767428454397828919 ) ) ;
#4460=CARTESIAN_POINT ( 'NONE',  ( -2.332582362116870200, -0.2313559322033900134, 4.387643303570819775 ) ) ;
#4461=CARTESIAN_POINT ( 'NONE',  ( 1.687170344132030042, -2.751502985243429844, 6.340793075730549511 ) ) ;
#4464=CARTESIAN_POINT ( 'NONE',  ( -1.764807890102219501, -3.221109627369170170, 3.143016121304770039 ) ) ;
#4465=CARTESIAN_POINT ( 'NONE',  ( 2.625437065641401446, -5.081991525423726230, 5.087214675345139270 ) ) ;
#4467=CARTESIAN_POINT ( 'NONE',  ( 1.921786527979010062, -0.3578389830508479363, 3.977907449687776431 ) ) ;
#4471=CARTESIAN_POINT ( 'NONE',  ( -1.750352751699820963, -1.913124606865061139, 3.627075451280493468 ) ) ;
#4475=CARTESIAN_POINT ( 'NONE',  ( -0.2453710345350140487, -0.4557203389830515317, 6.738252723719333481 ) ) ;
#4478=CARTESIAN_POINT ( 'NONE',  ( -1.754713504580578842, -5.551059322033894183, 3.634325740584633646 ) ) ;
#4481=CARTESIAN_POINT ( 'NONE',  ( -1.943632316591239473, -0.2536016949152540279, 3.373048379518170936 ) ) ;
#4486=CARTESIAN_POINT ( 'NONE',  ( -1.397172971746989845, -1.707370888630439953, 2.806153814454939610 ) ) ;
#4488=CARTESIAN_POINT ( 'NONE',  ( 0.8259795455966094657, -2.545749267008810435, 6.579537079411867495 ) ) ;
#4494=CARTESIAN_POINT ( 'NONE',  ( 0.4221287159901364605, -0.4423728813559331119, 7.320050063945812369 ) ) ;
#4495=CARTESIAN_POINT ( 'NONE',  ( 2.342931736853870017, -4.102223705964150646, 4.477701633099130163 ) ) ;
#4498=CARTESIAN_POINT ( 'NONE',  ( -1.925836318347889931, -5.188771186440680694, 6.525927015348141680 ) ) ;
#4507=CARTESIAN_POINT ( 'NONE',  ( -2.543624461644929724, -1.703530012270459970, 5.457025951420040322 ) ) ;
#4510=B_SPLINE_CURVE_WITH_KNOTS ( 'NONE', 3,
 ( #13406, #9037, #1715, #8741, #7877, #15018, #14826, #13631, #12234, #941, #7694, #6579, #14919, #12047, #14389, #7369 ),
 .UNSPECIFIED., .F., .F.,
 ( 4, 1, 1, 1, 1, 1, 1, 1, 1, 1, 1, 1, 1, 4 ),
 ( 0.4999998211434326656, 0.5106244842457859923, 0.5531978902116679864, 0.5957712970450619316, 0.6383447191100900531, 0.6809180289764420468, 0.7234918990885960133, 0.7660634153086809395, 0.8086437809559909873, 0.8511815656861039248, 0.8935997744639799789, 0.9363910903529559793, 0.9718312009674719976, 1.000000000000000000 ),
 .UNSPECIFIED. ) ;
#4511=CARTESIAN_POINT ( 'NONE',  ( 0.04278372834676710118, -1.870388906648450034, 2.346934926511239805 ) ) ;
#4512=CARTESIAN_POINT ( 'NONE',  ( 1.449568901432419343, -5.337500000000000355, 3.250431098567584165 ) ) ;
#4513=SHAPE_REPRESENTATION ( 'Actuator Return Helical Spring', ( #17681 ), #7087 ) ;
#4514=CARTESIAN_POINT ( 'NONE',  ( -2.260671505268489145, -1.913124606865061139, 3.309864021662289435 ) ) ;
#4516=CARTESIAN_POINT ( 'NONE',  ( -0.2220816246931631155, -4.544701183441625325, 6.740975647723836950 ) ) ;
#4525=CARTESIAN_POINT ( 'NONE',  ( -0.8731223871104993872, -5.470974576271190770, 6.558046933601121786 ) ) ;
#4526=CARTESIAN_POINT ( 'NONE',  ( 1.883442729065728960, -2.452596113855660676, 6.569694408006650832 ) ) ;
#4529=CARTESIAN_POINT ( 'NONE',  ( 2.053221424930760097, -0.8651516338920849369, 3.549770689668250157 ) ) ;
#4531=CARTESIAN_POINT ( 'NONE',  ( -0.3159454637156809409, -2.984385868126319785, 7.032150113402090064 ) ) ;
#4532=CARTESIAN_POINT ( 'NONE',  ( 0.6965028529799376367, -4.129352870612409632, 6.631265289497767057 ) ) ;
#4533=CARTESIAN_POINT ( 'NONE',  ( -0.005674314996644000582, -5.239933087847700399, 2.472195840738729888 ) ) ;
#4536=CARTESIAN_POINT ( 'NONE',  ( 2.260671505268459391, -3.686875393134939394, 3.309864021662241029 ) ) ;
#4538=CARTESIAN_POINT ( 'NONE',  ( 0.1365430262726380628, -0.1468220338983061424, 6.748423079423377047 ) ) ;
#4539=CARTESIAN_POINT ( 'NONE',  ( 1.902324933209389890, -2.402178660919109809, 3.314393441133530072 ) ) ;
#4542=CARTESIAN_POINT ( 'NONE',  ( -0.2365712905368978769, -3.407415933675479902, 2.358466376073659720 ) ) ;
#4544=CARTESIAN_POINT ( 'NONE',  ( 2.630358833876468960, -5.068644067796615360, 4.347767980622404771 ) ) ;
#4550=CARTESIAN_POINT ( 'NONE',  ( -2.002297259025881182, -3.287133615874059611, 5.153549919110945510 ) ) ;
#4551=CARTESIAN_POINT ( 'NONE',  ( 2.653602652190420574, -0.3756355932203404024, 4.735326402787084277 ) ) ;
#4553=CARTESIAN_POINT ( 'NONE',  ( -0.8298945877350979439, -5.211074464177370302, 2.494426474263899962 ) ) ;
#4558=CARTESIAN_POINT ( 'NONE',  ( -1.821706171509118954, -5.502118644067805597, 5.646608543709410455 ) ) ;
#4560=CARTESIAN_POINT ( 'NONE',  ( 0.009452110982654783611, -0.3001920447045380858, 2.050000000000001155 ) ) ;
#4562=CARTESIAN_POINT ( 'NONE',  ( -0.7785957873162068221, -3.659746228486683073, 2.162894899107379754 ) ) ;
#4565=CARTESIAN_POINT ( 'NONE',  ( -2.102728310581289950, -1.358046564306109927, 5.757014351541099195 ) ) ;
#4567=CARTESIAN_POINT ( 'NONE',  ( 0.6470883152343921418, -2.569037555297099651, 6.648378442427241630 ) ) ;
#4572=CARTESIAN_POINT ( 'NONE',  ( 1.447263454062181598, -0.9388573751169233539, 6.924531903016430512 ) ) ;
#4573=CARTESIAN_POINT ( 'NONE',  ( -1.670747221194380128, -5.103620102360550526, 3.047345349617600174 ) ) ;
#4576=CARTESIAN_POINT ( 'NONE',  ( -2.645377369053839356, -5.228813559322024851, 4.488260618344918740 ) ) ;
#4583=CARTESIAN_POINT ( 'NONE',  ( -2.049607015837349167, -3.170692174432623744, 6.385889905549041679 ) ) ;
#4589=CARTESIAN_POINT ( 'NONE',  ( 1.145304265383909836, -2.522460978720529656, 6.755972720436079548 ) ) ;
#4592=CARTESIAN_POINT ( 'NONE',  ( -2.325590009395030133, -4.870737219477670799, 5.061077271074069905 ) ) ;
#4596=CARTESIAN_POINT ( 'NONE',  ( 2.151546283159470274, -0.8884399221803740421, 3.746273477677459773 ) ) ;
#4600=CARTESIAN_POINT ( 'NONE',  ( 1.000896394980339998, -0.4290254237288140260, 6.829956240957369751 ) ) ;
#4610=CARTESIAN_POINT ( 'NONE',  ( 1.449568901432419343, -5.337500000000000355, 3.250431098567584165 ) ) ;
#4611=CARTESIAN_POINT ( 'NONE',  ( 2.226511124464869873, -1.074746228486680000, 5.462491901673799610 ) ) ;
#4612=CARTESIAN_POINT ( 'NONE',  ( -2.212163452524020357, -2.895073591333140239, 6.166099093621881799 ) ) ;
#4621=CARTESIAN_POINT ( 'NONE',  ( -2.281778813005780115, -4.847448931189379806, 5.276394947932169899 ) ) ;
#4622=CARTESIAN_POINT ( 'NONE',  ( 1.491388273269019571, -4.012911429170968880, 6.110908523251506352 ) ) ;
#4628=CARTESIAN_POINT ( 'NONE',  ( -1.468674196027810686, -4.362235753495300905, 6.910454658870877509 ) ) ;
#4629=CARTESIAN_POINT ( 'NONE',  ( 0.6964468257805941365, -0.1334745762711869732, 6.631228347243847132 ) ) ;
#4630=CARTESIAN_POINT ( 'NONE',  ( 2.245209214543399945, -2.635061543801989981, 5.405536158119010004 ) ) ;
#4637=CARTESIAN_POINT ( 'NONE',  ( 1.197297565406180153, -4.082776294035841858, 6.726135293448178842 ) ) ;
#4639=CARTESIAN_POINT ( 'NONE',  ( -1.925836318347889931, -5.188771186440680694, 6.525927015348141680 ) ) ;
#4643=CARTESIAN_POINT ( 'NONE',  ( 1.378221871957440170, -0.4201271186440679872, 6.607619368096269596 ) ) ;
#4649=CARTESIAN_POINT ( 'NONE',  ( 1.661700935788380074, -5.337500000000000355, 3.038299064211610112 ) ) ;
#4651=CARTESIAN_POINT ( 'NONE',  ( -2.051695471449629160, -3.333710192450643373, 4.773807418740784847 ) ) ;
#4652=CARTESIAN_POINT ( 'NONE',  ( 2.638803263991410741, -0.08008474576271243373, 4.982085668537405532 ) ) ;
#4655=CARTESIAN_POINT ( 'NONE',  ( -1.229686204202100175, -5.164643153926309793, 2.674737924334550154 ) ) ;
#4661=CARTESIAN_POINT ( 'NONE',  ( -1.489797906646480596, -5.488771186440680516, 6.112509577910826941 ) ) ;
#4666=CARTESIAN_POINT ( 'NONE',  ( 2.470260739716200860, -4.032358841099289215, 3.729986819255199926 ) ) ;
#4670=CARTESIAN_POINT ( 'NONE',  ( 2.159566522375460096, -2.359442960702510028, 5.635424033751039730 ) ) ;
#4674=CARTESIAN_POINT ( 'NONE',  ( 2.002297259025890064, -2.312866384125929820, 5.153549919110900213 ) ) ;
#4679=CARTESIAN_POINT ( 'NONE',  ( -1.576846334488060553, -1.707370888630439065, 2.565364356520430267 ) ) ;
#4681=CARTESIAN_POINT ( 'NONE',  ( 2.343457872958619959, -4.148800282540729967, 4.916681529328559286 ) ) ;
#4684=CARTESIAN_POINT ( 'NONE',  ( 1.467041701146838406, -5.122033898305085486, 6.911479965439912831 ) ) ;
#4691=CARTESIAN_POINT ( 'NONE',  ( 1.315254646989809872, -2.821367850108300157, 7.005042061779697349 ) ) ;
#4693=CARTESIAN_POINT ( 'NONE',  ( -3.760880495917719358E-15, -5.299999999999999822, 2.350000000000000089 ) ) ;
#4695=CARTESIAN_POINT ( 'NONE',  ( -1.687170344131989852, -2.848497014756560475, 6.340793075730589479 ) ) ;
#4696=CARTESIAN_POINT ( 'NONE',  ( 0.9866023595736967966, -5.020626044399130627, 2.560054107758459985 ) ) ;
#4697=CARTESIAN_POINT ( 'NONE',  ( -2.612083973477999699, -1.819971453711898945, 4.230818789270855085 ) ) ;
#4700=CARTESIAN_POINT ( 'NONE',  ( -1.272929729338609262, -4.684430913171365063, 6.310761232086878003 ) ) ;
#4701=CARTESIAN_POINT ( 'NONE',  ( 0.3743405594629510280, -0.4423728813559330009, 7.023440622744399953 ) ) ;
#4713=CARTESIAN_POINT ( 'NONE',  ( 2.337178851518220135, -2.588484967225419986, 4.976298214796759822 ) ) ;
#4716=CARTESIAN_POINT ( 'NONE',  ( -1.981271652668300298, -1.633665147405599871, 5.970160748022450115 ) ) ;
#4717=CARTESIAN_POINT ( 'NONE',  ( -0.04278372834682089842, -3.729611093351540063, 2.346934926511239805 ) ) ;
#4718=CARTESIAN_POINT ( 'NONE',  ( 1.485933537025759366, -0.8030495317899833951, 3.286232459959989249 ) ) ;
#4724=CARTESIAN_POINT ( 'NONE',  ( -1.432215783582709401, -0.1868644067796619845, 6.170863372171116801 ) ) ;
#4725=CARTESIAN_POINT ( 'NONE',  ( 1.869848057046569867, -4.288530012270459935, 6.129130480762009725 ) ) ;
#4731=CARTESIAN_POINT ( 'NONE',  ( -1.303621121494419777, -4.362235753495302681, 6.659417683669698995 ) ) ;
#4734=CARTESIAN_POINT ( 'NONE',  ( -1.554165089654128584, -5.179872881355935377, 6.851145244874527584 ) ) ;
#4740=CARTESIAN_POINT ( 'NONE',  ( 1.736825397686149852, -3.985782264522713447, 3.605313112995111702 ) ) ;
#4742=CARTESIAN_POINT ( 'NONE',  ( 2.484260633728970546, -0.05783898305084796132, 3.766563288620793593 ) ) ;
#4744=CARTESIAN_POINT ( 'NONE',  ( 0.2189795514005130062, -0.3044491525423729805, 2.356806637999009801 ) ) ;
#4747=CARTESIAN_POINT ( 'NONE',  ( 0.009452039534070141164, -0.3001931771041043140, 2.350000000173209092 ) ) ;
#4751=CARTESIAN_POINT ( 'NONE',  ( -2.523518139275819916, -3.263845327585779277, 5.521565513971835593 ) ) ;
#4753=CARTESIAN_POINT ( 'NONE',  ( -0.2365712905368979879, -3.407415933675480346, 2.358466376073659720 ) ) ;
#4757=CARTESIAN_POINT ( 'NONE',  ( -1.683529720875190705, -4.455388906648449776, 5.875001924065656134 ) ) ;
#4759=CARTESIAN_POINT ( 'NONE',  ( -1.503314099254069447, -1.660794312053860633, 3.301805249040033363 ) ) ;
#4763=CARTESIAN_POINT ( 'NONE',  ( -2.607432201095288615, -1.521064582324129777, 4.205620581240213873 ) ) ;
#4765=CARTESIAN_POINT ( 'NONE',  ( 2.313035575219750228, -4.172088570829020071, 5.134294963419709923 ) ) ;
#4768=CARTESIAN_POINT ( 'NONE',  ( -1.549742865090599997, -5.184322033898309812, 6.471102547561460305 ) ) ;
#4776=CARTESIAN_POINT ( 'NONE',  ( -2.479511223993290603, -1.866548030288480042, 3.753882785753710483 ) ) ;
#4778=CARTESIAN_POINT ( 'NONE',  ( 0.5637478356992829953, -0.6606104644819250638, 2.398845082743519708 ) ) ;
#4780=CARTESIAN_POINT ( 'NONE',  ( -1.115198193348240219, -4.338947465207009913, 6.772457159276569882 ) ) ;
#4782=CARTESIAN_POINT ( 'NONE',  ( 1.151392222988870895, -5.028306595106930565, 2.990827770388080342 ) ) ;
#4783=CARTESIAN_POINT ( 'NONE',  ( 1.853635285637830865, -1.191187669928120529, 6.599249831075482575 ) ) ;
#4795=CARTESIAN_POINT ( 'NONE',  ( -2.345213174852959881, -1.796683165423619943, 4.503223853122380049 ) ) ;
#4797=CARTESIAN_POINT ( 'NONE',  ( 1.718313768400149932, -0.5108663019338149924, 2.998025103714370143 ) ) ;
#4799=CARTESIAN_POINT ( 'NONE',  ( 2.231116159141619981, -0.9117282104686620370, 3.951089877392439664 ) ) ;
#4800=CARTESIAN_POINT ( 'NONE',  ( -1.781655196750479897, -3.520016498756949996, 3.162323035427820450 ) ) ;
#4801=CARTESIAN_POINT ( 'NONE',  ( 1.436030008293490701, -1.191187669928120529, 6.167214932417436124 ) ) ;
#4803=CARTESIAN_POINT ( 'NONE',  ( 0.5889081234606849957, -0.4379237288135600092, 6.978529000034869867 ) ) ;
#4808=CARTESIAN_POINT ( 'NONE',  ( 1.088937603231269646, -0.3266949152542383272, 2.959627624143540192 ) ) ;
#4809=CARTESIAN_POINT ( 'NONE',  ( -2.349464193210359930, -3.356998480738930368, 4.563019372514619754 ) ) ;
#4816=CARTESIAN_POINT ( 'NONE',  ( -0.4221287159901280228, -5.157627118644064979, 7.320050063945812369 ) ) ;
#4818=CARTESIAN_POINT ( 'NONE',  ( -2.058670345754650022, -0.5491525423728820243, 3.559656372813929881 ) ) ;
#4823=CARTESIAN_POINT ( 'NONE',  ( 1.217499609005879613, -3.892629111369556139, 3.046943272389411206 ) ) ;
#4826=CARTESIAN_POINT ( 'NONE',  ( 2.645377369053839356, -0.07118644067796667252, 4.488260618344900088 ) ) ;
#4828=CARTESIAN_POINT ( 'NONE',  ( 0.8570167067220200163, -0.3177966101694920664, 2.508190348879349774 ) ) ;
#4832=CARTESIAN_POINT ( 'NONE',  ( 1.747582379783020778, -0.4156779661016956062, 6.697200745122486865 ) ) ;
#4836=CARTESIAN_POINT ( 'NONE',  ( 0.2812789908084389889, -5.444279661016950378, 7.036533610117280624 ) ) ;
#4839=CARTESIAN_POINT ( 'NONE',  ( -1.494590226124050014, -0.2673043920988010247, 2.870965838437660178 ) ) ;
#4840=CARTESIAN_POINT ( 'NONE',  ( -2.502804106625960756, -3.426863345603793576, 3.817341913956430410 ) ) ;
#4842=CARTESIAN_POINT ( 'NONE',  ( 1.044181395669780077, -3.547145663405210314, 2.590869634085890105 ) ) ;
#4846=CARTESIAN_POINT ( 'NONE',  ( 1.919159680931818990, -3.733451969711523155, 3.970803207828129455 ) ) ;
#4850=CARTESIAN_POINT ( 'NONE',  ( 1.549925137359331462, -0.8689925102520592581, 6.046340934239826659 ) ) ;
#4853=CARTESIAN_POINT ( 'NONE',  ( 1.835211330903820937, -0.8922807985403484743, 6.617058440403981834 ) ) ;
#4858=CARTESIAN_POINT ( 'NONE',  ( -1.851073041990159984, -5.193220338983049800, 6.153284478378270528 ) ) ;
#4867=CARTESIAN_POINT ( 'NONE',  ( -1.963178672446121098, -1.959701183441630024, 2.914210764660470687 ) ) ;
#4870=CARTESIAN_POINT ( 'NONE',  ( 2.182690844914370043, -3.919758276017820453, 5.580117243900430068 ) ) ;
#4871=CARTESIAN_POINT ( 'NONE',  ( 1.147638118088980086, -5.328211948015596278, 2.987995008461610702 ) ) ;
#4873=CARTESIAN_POINT ( 'NONE',  ( -2.349129089426440054, -4.894025507765950245, 4.842612091679129982 ) ) ;
#4877=CARTESIAN_POINT ( 'NONE',  ( 2.253200202764420013, -0.3889830508474579895, 5.379408587037500133 ) ) ;
#4879=CARTESIAN_POINT ( 'NONE',  ( -2.203023580853999963, -5.542161016949149754, 3.872235369154300333 ) ) ;
#4887=CARTESIAN_POINT ( 'NONE',  ( 0.2365712905368450025, -2.192584066324519743, 2.358466376073659720 ) ) ;
#4889=CARTESIAN_POINT ( 'NONE',  ( 0.4974685680287860290, -5.439830508474580384, 7.000224381598740386 ) ) ;
#4891=CARTESIAN_POINT ( 'NONE',  ( 1.803891155489780074, -0.8185750573155089471, 3.188470185434109982 ) ) ;
#4892=CARTESIAN_POINT ( 'NONE',  ( 1.994983296312400123, -4.265241723982169830, 5.948514050749290405 ) ) ;
#4893=CARTESIAN_POINT ( 'NONE',  ( 1.996236309555640798, -1.051457940198389673, 5.179523137126535559 ) ) ;
#4900=CARTESIAN_POINT ( 'NONE',  ( -2.000624272291700034, -0.2358050847457631438, 4.239366054776020576 ) ) ;
#4901=CARTESIAN_POINT ( 'NONE',  ( 2.102728310581320148, -4.241953435693879726, 5.757014351541050345 ) ) ;
#4907=CARTESIAN_POINT ( 'NONE',  ( -2.306642602145299925, -5.215466101694909540, 5.166805192608490138 ) ) ;
#4910=CARTESIAN_POINT ( 'NONE',  ( 0.5889081234606849957, -0.4379237288135600092, 6.978529000034869867 ) ) ;
#4913=CARTESIAN_POINT ( 'NONE',  ( 2.053018524985070314, -4.125511994252439862, 4.695903819313355321 ) ) ;
#4915=CARTESIAN_POINT ( 'NONE',  ( 1.610878918935058524, -0.03114406779661053892, 2.590989782159081933 ) ) ;
#4918=CARTESIAN_POINT ( 'NONE',  ( -2.171642826483958899, -0.4957627118644069575, 6.225392547715731695 ) ) ;
#4922=CARTESIAN_POINT ( 'NONE',  ( -1.000896394980330006, -5.470974576271190770, 6.829956240957379521 ) ) ;
#4925=CARTESIAN_POINT ( 'NONE',  ( -1.401708661791369437, -1.241605122864669619, 6.590491606684078185 ) ) ;
#4926=CARTESIAN_POINT ( 'NONE',  ( 1.661700935788380074, -5.337500000000000355, 3.038299064211610112 ) ) ;
#4930=CARTESIAN_POINT ( 'NONE',  ( 2.642463257358089734, -4.148800282540726414, 4.945970783863369746 ) ) ;
#4932=CARTESIAN_POINT ( 'NONE',  ( -1.458615186838411626, -5.103620102360555855, 3.259477383973569786 ) ) ;
#4934=CARTESIAN_POINT ( 'NONE',  ( 1.507201387236020151, -2.475884402143949892, 6.507509243627189299 ) ) ;
#4940=CARTESIAN_POINT ( 'NONE',  ( -0.7616804549307533145, -3.337551068810613142, 2.793499350326739350 ) ) ;
#4943=CARTESIAN_POINT ( 'NONE',  ( -1.741179788930630190, -1.334758276017820267, 5.787747574231985936 ) ) ;
#4946=APPLICATION_CONTEXT ( 'automotive_design' ) ;
#4948=CARTESIAN_POINT ( 'NONE',  ( -0.009452110982655142699, -0.5998079552954631577, 2.050000000000001155 ) ) ;
#4949=CARTESIAN_POINT ( 'NONE',  ( -1.771358649600341284, -1.264893411152960834, 6.676209054601235593 ) ) ;
#4952=CARTESIAN_POINT ( 'NONE',  ( 1.936998685628529948, -0.8418633456037969420, 3.363294429306519895 ) ) ;
#4954=CARTESIAN_POINT ( 'NONE',  ( 1.949083719010301197, -5.059745762711855832, 4.055210292801453953 ) ) ;
#4956=CIRCLE ( 'NONE', #15335, 0.1499999999999999667 ) ;
#4960=CARTESIAN_POINT ( 'NONE',  ( 0.9724415447670879953, -0.7068739681193980662, 2.553509270169310064 ) ) ;
#4963=CARTESIAN_POINT ( 'NONE',  ( -1.647941990407690627, -5.555508474576275724, 3.475676388127094896 ) ) ;
#4965=CARTESIAN_POINT ( 'NONE',  ( -2.531332855772528756, -2.964938456198001671, 5.497162258444521221 ) ) ;
#4966=CARTESIAN_POINT ( 'NONE',  ( -1.883442729065680776, -3.147403886144331420, 6.569694408006696129 ) ) ;
#4970=CARTESIAN_POINT ( 'NONE',  ( 2.353343516942209668, -3.826605122864669806, 4.722803042560139275 ) ) ;
#4974=CARTESIAN_POINT ( 'NONE',  ( 0.5134687485628864900, -2.215872354612800521, 2.096259702418241222 ) ) ;
#4979=CARTESIAN_POINT ( 'NONE',  ( 1.794646911016580137, -1.167899381639829981, 6.222494056560660347 ) ) ;
#4980=CARTESIAN_POINT ( 'NONE',  ( 1.549742865090599997, -0.4156779661016959948, 6.471102547561449647 ) ) ;
#4983=CARTESIAN_POINT ( 'NONE',  ( -0.4360591020458099987, -5.591101694915249887, 2.387347919655840034 ) ) ;
#4988=CARTESIAN_POINT ( 'NONE',  ( 2.155845792290829177, -5.055296610169488503, 3.756158857535770945 ) ) ;
#4995=CARTESIAN_POINT ( 'NONE',  ( 1.611907055891590002, -2.355602084342530045, 2.985210995296850189 ) ) ;
#5001=CARTESIAN_POINT ( 'NONE',  ( 1.764807890102179977, -2.378890372630820149, 3.143016121304719857 ) ) ;
#5002=CARTESIAN_POINT ( 'NONE',  ( 0.8189529353761060282, -3.822764246504690266, 2.493631540942729874 ) ) ;
#5003=CARTESIAN_POINT ( 'NONE',  ( -0.3681613504765444134, -2.122719201459649874, 2.680257674196191431 ) ) ;
#5008=CARTESIAN_POINT ( 'NONE',  ( 0.8189529353761060282, -3.822764246504690266, 2.493631540942729874 ) ) ;
#5017=CARTESIAN_POINT ( 'NONE',  ( -1.610878918935079840, -5.268855932203385883, 2.590989782159090815 ) ) ;
#5020=CARTESIAN_POINT ( 'NONE',  ( -1.272929729338609262, -4.684430913171365063, 6.310761232086878003 ) ) ;
#5021=CARTESIAN_POINT ( 'NONE',  ( -2.321479326063761395, -0.5491525423728815802, 3.414080590619972710 ) ) ;
#5023=CARTESIAN_POINT ( 'NONE',  ( 2.116444151961470066, -0.05338983050847490031, 3.670839500609349937 ) ) ;
#5029=CARTESIAN_POINT ( 'NONE',  ( 2.350067830300900162, -5.377542372881360500, 4.825253242917690422 ) ) ;
#5030=CARTESIAN_POINT ( 'NONE',  ( -2.051568858000911266, -5.080331814072260421, 3.016498023208352919 ) ) ;
#5033=CARTESIAN_POINT ( 'NONE',  ( 1.802718065953961002, -0.5662447625043125488, 3.717600174934180046 ) ) ;
#5034=CARTESIAN_POINT ( 'NONE',  ( -2.524473153133541814, -4.987178660919110662, 3.881373716577405819 ) ) ;
#5037=CARTESIAN_POINT ( 'NONE',  ( 1.823404397755048700, -3.943046564306109669, 5.643450181448720571 ) ) ;
#5040=CARTESIAN_POINT ( 'NONE',  ( -1.974086094277271108, -1.404623140882690580, 5.263813741415750869 ) ) ;
#5046=CARTESIAN_POINT ( 'NONE',  ( -0.009452110982655128821, -0.5998079552954630467, 2.350000000000000089 ) ) ;
#5047=CARTESIAN_POINT ( 'NONE',  ( -2.531332855772528756, -2.964938456198001671, 5.497162258444521221 ) ) ;
#5051=CARTESIAN_POINT ( 'NONE',  ( 1.480680413335799805, -1.214475958216410190, 6.529298007719799735 ) ) ;
#5053=CARTESIAN_POINT ( 'NONE',  ( 0.4974685680287860290, -5.139830508474580562, 7.000224381598740386 ) ) ;
#5060=CARTESIAN_POINT ( 'NONE',  ( 2.030998484741458832, -5.381991525423726053, 4.999543428097175557 ) ) ;
#5061=CARTESIAN_POINT ( 'NONE',  ( -2.567863625471609179, -3.104668185927728974, 4.029783546918099368 ) ) ;
#5065=CARTESIAN_POINT ( 'NONE',  ( -1.902324933209429858, -3.197821339080880065, 3.314393441133570040 ) ) ;
#5068=CARTESIAN_POINT ( 'NONE',  ( 1.213493134184789657, -2.285737219477670390, 2.339799138571409642 ) ) ;
#5075=CARTESIAN_POINT ( 'NONE',  ( -2.111627294540180166, -1.889836318576769925, 3.660877362176710559 ) ) ;
#5076=CARTESIAN_POINT ( 'NONE',  ( 0.002826310976695059745, -5.105205364259369993, 2.204978094066150085 ) ) ;
#5078=CARTESIAN_POINT ( 'NONE',  ( -1.194742379459959869, -5.475423728813559876, 6.727584234649759409 ) ) ;
#5081=CARTESIAN_POINT ( 'NONE',  ( 1.811729841638689775, -5.041949152542367862, 3.197954009834290456 ) ) ;
#5086=CARTESIAN_POINT ( 'NONE',  ( 0.5570002967656469961, -2.891232714973159812, 6.986590552960210587 ) ) ;
#5088=CARTESIAN_POINT ( 'NONE',  ( -3.766169468773179610E-15, -5.599999999999999645, 2.349999999999999645 ) ) ;
#5090=CARTESIAN_POINT ( 'NONE',  ( 1.611907055891590002, -2.355602084342530045, 2.985210995296850189 ) ) ;
#5091=CARTESIAN_POINT ( 'NONE',  ( -2.239137794397029868, -4.987178660919110662, 3.975425900939220103 ) ) ;
#5092=CARTESIAN_POINT ( 'NONE',  ( 0.9742769543504904428, -1.261052534792989288, 6.507120986223561054 ) ) ;
#5094=CARTESIAN_POINT ( 'NONE',  ( 0.1565249325564390115, -0.4468220338983060480, 7.048192310558509810 ) ) ;
#5095=CARTESIAN_POINT ( 'NONE',  ( -0.1869574461324000070, -0.5962015548080630278, 2.350675676344399889 ) ) ;
#5100=CARTESIAN_POINT ( 'NONE',  ( 1.571912189623089873, -4.335106588847041031, 6.451524409078630562 ) ) ;
#5107=CARTESIAN_POINT ( 'NONE',  ( -1.978267656359410154, -5.197669491525420682, 5.974740860598790171 ) ) ;
#5111=CARTESIAN_POINT ( 'NONE',  ( 2.296954468777709923, -0.6361096273691760894, 4.187412587068650716 ) ) ;
#5113=CARTESIAN_POINT ( 'NONE',  ( 2.053221424930760097, -0.8651516338920849369, 3.549770689668250157 ) ) ;
#5114=CARTESIAN_POINT ( 'NONE',  ( -0.3171869470818471370, -0.1557203389830511819, 7.334814496515233095 ) ) ;
#5118=CARTESIAN_POINT ( 'NONE',  ( 0.4360591020457930123, -0.3088983050847460277, 2.387347919655840034 ) ) ;
#5119=CARTESIAN_POINT ( 'NONE',  ( -2.020286629067959971, -0.1913135593220339215, 6.420841923842841581 ) ) ;
#5121=CARTESIAN_POINT ( 'NONE',  ( 0.7093417302541469294, -5.435381355932199732, 6.943956659919690466 ) ) ;
#5123=CARTESIAN_POINT ( 'NONE',  ( 2.033393610350128888, -0.8224159336754828242, 5.884928737465322079 ) ) ;
#5124=CARTESIAN_POINT ( 'NONE',  ( -0.009452110982655715157, -0.5998079552954631577, 2.649999999999998579 ) ) ;
#5125=CARTESIAN_POINT ( 'NONE',  ( 1.008962495263989956, -0.9854339516935015642, 7.154609617872576877 ) ) ;
#5127=CARTESIAN_POINT ( 'NONE',  ( -0.7252674547190166576, -5.211074464177385401, 2.776474344060209987 ) ) ;
#5128=CARTESIAN_POINT ( 'NONE',  ( -1.115198193348240219, -4.338947465207009913, 6.772457159276569882 ) ) ;
#5129=CARTESIAN_POINT ( 'NONE',  ( -2.501774541437291610, -4.824160642901089702, 5.585572039315926496 ) ) ;
#5132=CARTESIAN_POINT ( 'NONE',  ( -1.928470600873600782, -3.127956474216021299, 3.995796205495660391 ) ) ;
#5135=CARTESIAN_POINT ( 'NONE',  ( -0.3509990757148119811, -1.125163681423229756, 6.722795464567655976 ) ) ;
#5139=CARTESIAN_POINT ( 'NONE',  ( 0.2751970330256541808, -0.3251990024832501214, 2.050771348498781066 ) ) ;
#5140=CARTESIAN_POINT ( 'NONE',  ( 0.5385843327681005821, -1.916965483225031130, 2.101338688959521139 ) ) ;
#5144=CARTESIAN_POINT ( 'NONE',  ( 1.679950111053631900, -5.104237288135595740, 5.880020650119711867 ) ) ;
#5151=CARTESIAN_POINT ( 'NONE',  ( 1.713314936023349944, -5.338983050847460277, 3.089913064446569546 ) ) ;
#5152=CARTESIAN_POINT ( 'NONE',  ( -1.256119432346030962, -4.338947465207014353, 7.037793332329566276 ) ) ;
#5157=CARTESIAN_POINT ( 'NONE',  ( 2.091095264232530226, -3.943046564306110113, 5.779845490516200002 ) ) ;
#5160=CARTESIAN_POINT ( 'NONE',  ( -1.392767620582729293, -2.029566048306499670, 2.440948861123721780 ) ) ;
#5162=CARTESIAN_POINT ( 'NONE',  ( 1.596341326794969984, -0.3355932203389830337, 2.970780074643809776 ) ) ;
#5163=CARTESIAN_POINT ( 'NONE',  ( 1.902324933209389890, -2.402178660919109809, 3.314393441133530072 ) ) ;
#5166=CARTESIAN_POINT ( 'NONE',  ( -1.428515267734880023, -5.568855932203390147, 2.829745655876930055 ) ) ;
#5171=CARTESIAN_POINT ( 'NONE',  ( -0.1565249325564299632, -5.153177966101688767, 7.048192310558507145 ) ) ;
#5176=CARTESIAN_POINT ( 'NONE',  ( 2.192143888961729736, -4.218665147405599392, 5.556300681753580051 ) ) ;
#5179=CARTESIAN_POINT ( 'NONE',  ( 2.043308330018790198, -5.399788135593220240, 5.867646457774659652 ) ) ;
#5184=CARTESIAN_POINT ( 'NONE',  ( 0.4539185741479240255, -2.215872354612800521, 2.390735265170440105 ) ) ;
#5186=CARTESIAN_POINT ( 'NONE',  ( 0.009452039534068971960, -5.000193177104105047, 2.350000000173209536 ) ) ;
#5187=CARTESIAN_POINT ( 'NONE',  ( -1.203420131881960398, -1.540511994252448780, 6.363334551077827861 ) ) ;
#5189=CARTESIAN_POINT ( 'NONE',  ( 0.009452110982654783611, -0.3001920447045380858, 2.050000000000001155 ) ) ;
#5193=CARTESIAN_POINT ( 'NONE',  ( -2.349129089426440054, -4.894025507765950245, 4.842612091679129982 ) ) ;
#5200=CARTESIAN_POINT ( 'NONE',  ( -0.5889081234606770021, -5.162076271186439413, 6.978529000034869867 ) ) ;
#5205=CARTESIAN_POINT ( 'NONE',  ( -1.401708661791369881, -1.241605122864670063, 6.590491606684079962 ) ) ;
#5208=CARTESIAN_POINT ( 'NONE',  ( 1.936998685628529948, -0.8418633456037969420, 3.363294429306519895 ) ) ;
#5209=CARTESIAN_POINT ( 'NONE',  ( 2.011500846714319835, -0.04894067796610199889, 3.478373409938460448 ) ) ;
#5214=CARTESIAN_POINT ( 'NONE',  ( -2.311987889326990064, -1.521064582324129777, 4.260161748947140836 ) ) ;
#5215=FACE_OUTER_BOUND ( 'NONE', #14266, .T. ) ;
#5216=CARTESIAN_POINT ( 'NONE',  ( -1.771358649600341284, -1.264893411152960834, 6.676209054601235593 ) ) ;
#5220=CARTESIAN_POINT ( 'NONE',  ( 1.710920205120059823, -4.012911429170970656, 6.316012914303540171 ) ) ;
#5221=CARTESIAN_POINT ( 'NONE',  ( -1.233489123281609645, -4.637854336594775084, 7.049812391606588236 ) ) ;
#5225=CARTESIAN_POINT ( 'NONE',  ( -1.996236309555629251, -4.548542059801595094, 5.179523137126564869 ) ) ;
#5229=CARTESIAN_POINT ( 'NONE',  ( -0.01333550863832440661, -3.430704221963769562, 2.647020699851690306 ) ) ;
#5234=CARTESIAN_POINT ( 'NONE',  ( -1.869504824896970119, -0.2046610169491529518, 5.548311746956866131 ) ) ;
#5235=CARTESIAN_POINT ( 'NONE',  ( 1.349044826018420906, -0.4774152569121725143, 3.148480103883603221 ) ) ;
#5236=CARTESIAN_POINT ( 'NONE',  ( -2.647661051184980519, -3.058091609351150986, 4.518328177639144627 ) ) ;
#5241=CARTESIAN_POINT ( 'NONE',  ( -1.647941990407690627, -5.255508474576275901, 3.475676388127094896 ) ) ;
#5249=CARTESIAN_POINT ( 'NONE',  ( -2.253200202764409799, -5.511016949152540256, 5.379408587037509903 ) ) ;
#5251=CARTESIAN_POINT ( 'NONE',  ( -2.629224451638860760, -4.641695212954759064, 4.339039509243916015 ) ) ;
#5253=CARTESIAN_POINT ( 'NONE',  ( -1.236224677598320332, -3.613169651910099756, 2.351625617688101411 ) ) ;
#5256=CARTESIAN_POINT ( 'NONE',  ( 0.7778405029480717214, -0.9854339516935015642, 6.599964735094206780 ) ) ;
#5261=CARTESIAN_POINT ( 'NONE',  ( 0.1366863161731129428, -2.937809291549738688, 7.350364228549148393 ) ) ;
#5265=CARTESIAN_POINT ( 'NONE',  ( -2.351526912647309953, -0.5269067796610169552, 4.606040641882809261 ) ) ;
#5266=CARTESIAN_POINT ( 'NONE',  ( 1.707817112497189926, -0.4112288135593229477, 6.319218296629480314 ) ) ;
#5267=CARTESIAN_POINT ( 'NONE',  ( 0.2365712905368450025, -2.192584066324519743, 2.358466376073659720 ) ) ;
#5268=CARTESIAN_POINT ( 'NONE',  ( 0.009452039534068971960, -5.000193177104105047, 2.350000000173209536 ) ) ;
#5270=CARTESIAN_POINT ( 'NONE',  ( -1.973760952634090238, -5.559957627118640389, 2.925986839873730982 ) ) ;
#5279=CARTESIAN_POINT ( 'NONE',  ( -1.465095039565370127, -3.566593075333519991, 2.858195935359880480 ) ) ;
#5281=CARTESIAN_POINT ( 'NONE',  ( -2.306642602145299925, -5.515466101694909362, 5.166805192608490138 ) ) ;
#5284=CARTESIAN_POINT ( 'NONE',  ( 2.322440385110930094, -2.518620102360550117, 4.319189883157390497 ) ) ;
#5288=CARTESIAN_POINT ( 'NONE',  ( 1.712910428781929006, -2.704926408666860738, 5.831741890007691609 ) ) ;
#5303=CARTESIAN_POINT ( 'NONE',  ( -1.428515267734880023, -5.268855932203390324, 2.829745655876930055 ) ) ;
#5307=CARTESIAN_POINT ( 'NONE',  ( 1.777964140657680048, -0.8689925102520590361, 6.241943319976220650 ) ) ;
#5310=CARTESIAN_POINT ( 'NONE',  ( -2.051973656473811136, -4.917313796054240349, 4.634380218157504672 ) ) ;
#5311=CARTESIAN_POINT ( 'NONE',  ( 1.851073041990159984, -0.1067796610169499949, 6.153284478378259870 ) ) ;
#5313=CARTESIAN_POINT ( 'NONE',  ( 2.340070819011249803, -0.3800847457627120063, 4.950151441910540129 ) ) ;
#5315=ORIENTED_EDGE ( 'NONE', *, *, #14128, .T. ) ;
#5317=CARTESIAN_POINT ( 'NONE',  ( -1.932035991685910004, -0.2610169491525428653, 2.884370051397200818 ) ) ;
#5321=CARTESIAN_POINT ( 'NONE',  ( -0.8189529353761558772, -1.777235753495300052, 2.493631540942750302 ) ) ;
#5323=CARTESIAN_POINT ( 'NONE',  ( 2.351526912647309953, -5.373093220338979847, 4.606040641882800379 ) ) ;
#5324=CARTESIAN_POINT ( 'NONE',  ( -2.550815101416269659, -1.404623140882690580, 5.432431574543720387 ) ) ;
#5326=CARTESIAN_POINT ( 'NONE',  ( -1.670747221194380128, -5.103620102360550526, 3.047345349617600174 ) ) ;
#5328=CARTESIAN_POINT ( 'NONE',  ( 1.381042549632460092, -4.059488005747549977, 6.605640880016110827 ) ) ;
#5329=CARTESIAN_POINT ( 'NONE',  ( -0.04351999560413650353, -4.521412895153344103, 7.353529668759054339 ) ) ;
#5333=CARTESIAN_POINT ( 'NONE',  ( 1.138568046961060176, -1.237764246504700072, 6.408380708468512488 ) ) ;
#5334=ADVANCED_BREP_SHAPE_REPRESENTATION ( '', ( #1876, #17681 ), #7087 ) ;
#5339=CARTESIAN_POINT ( 'NONE',  ( 1.088937603231269646, -0.3266949152542383272, 2.959627624143540192 ) ) ;
#5341=CARTESIAN_POINT ( 'NONE',  ( -1.315254646989760134, -2.778632149891700376, 7.005042061779727547 ) ) ;
#5343=CARTESIAN_POINT ( 'NONE',  ( 2.030998484741458832, -5.381991525423726053, 4.999543428097175557 ) ) ;
#5346=CARTESIAN_POINT ( 'NONE',  ( 2.043308330018790198, -5.399788135593220240, 5.867646457774659652 ) ) ;
#5349=CARTESIAN_POINT ( 'NONE',  ( 1.477796163681079911, -5.417584745762709986, 6.531563725478140015 ) ) ;
#5350=CARTESIAN_POINT ( 'NONE',  ( 1.820241257191439921, -0.5196681859277348936, 3.208199930689769719 ) ) ;
#5351=CARTESIAN_POINT ( 'NONE',  ( 1.576846334488021473, -3.892629111369556139, 2.565364356520400513 ) ) ;
#5353=CARTESIAN_POINT ( 'NONE',  ( 1.438959988998139914E-16, 0.000000000000000000, 2.350000000000000089 ) ) ;
#5355=CARTESIAN_POINT ( 'NONE',  ( 0.03076623656506880661, -1.078587104846650213, 6.752792069673816400 ) ) ;
#5361=CARTESIAN_POINT ( 'NONE',  ( 2.130266475405040882, -0.3444915254237289615, 3.117337770017949428 ) ) ;
#5362=CARTESIAN_POINT ( 'NONE',  ( 2.322440385110930094, -2.518620102360550117, 4.319189883157390497 ) ) ;
#5364=CARTESIAN_POINT ( 'NONE',  ( -0.8147348917079838548, -0.2831443699174389095, 2.488757019513870627 ) ) ;
#5365=CARTESIAN_POINT ( 'NONE',  ( -0.6640878839024662028, -5.462076271186444565, 7.269405042592523181 ) ) ;
#5369=CARTESIAN_POINT ( 'NONE',  ( -1.707817112497179712, -5.188771186440678918, 6.319218296629480314 ) ) ;
#5375=CARTESIAN_POINT ( 'NONE',  ( -0.8934014991059870958, -4.614566048306490309, 6.877287176483410924 ) ) ;
#5376=CARTESIAN_POINT ( 'NONE',  ( 1.652654650382400003, -0.7952867690272209522, 3.029252778805620050 ) ) ;
#5377=CARTESIAN_POINT ( 'NONE',  ( 1.340185291429730974, -5.033893599512585304, 3.140995886557053307 ) ) ;
#5379=CARTESIAN_POINT ( 'NONE',  ( -2.267872052190610166, -1.843259742000189938, 4.071110468860649867 ) ) ;
#5381=CARTESIAN_POINT ( 'NONE',  ( -0.2739924515130059968, -2.984385868126320673, 6.734657214162127481 ) ) ;
#5383=CARTESIAN_POINT ( 'NONE',  ( -1.372722144827311475, -0.2742238837839081067, 2.407683403867349803 ) ) ;
#5385=PRESENTATION_STYLE_ASSIGNMENT (( #16589 ) ) ;
#5387=EDGE_LOOP ( 'NONE', ( #6407, #11713, #3997, #7827 ) ) ;
#5391=CARTESIAN_POINT ( 'NONE',  ( 0.9707742057416334225, -5.126483050847465250, 6.508944043303927174 ) ) ;
#5392=CARTESIAN_POINT ( 'NONE',  ( -1.576846334488060553, -1.707370888630439065, 2.565364356520430267 ) ) ;
#5397=CARTESIAN_POINT ( 'NONE',  ( 2.145694642186089851, -1.098034516774969882, 5.666819626392539888 ) ) ;
#5398=CARTESIAN_POINT ( 'NONE',  ( 2.306642602145299925, -0.08453389830508530045, 5.166805192608480368 ) ) ;
#5399=CARTESIAN_POINT ( 'NONE',  ( 1.194742379459969861, -0.4245762711864409789, 6.727584234649759409 ) ) ;
#5401=CARTESIAN_POINT ( 'NONE',  ( -2.650076489488250697, -0.2224576271186441134, 4.841243018609314497 ) ) ;
#5405=CARTESIAN_POINT ( 'NONE',  ( -0.1226612266410539165, -2.662190708450249410, 7.050255286338656724 ) ) ;
#5407=CARTESIAN_POINT ( 'NONE',  ( 2.651721837666119796, -5.373093220338980736, 4.594045830208265180 ) ) ;
#5408=CARTESIAN_POINT ( 'NONE',  ( 0.7756407636289058827, -1.008722239981790558, 7.238010066725317770 ) ) ;
#5411=CARTESIAN_POINT ( 'NONE',  ( 1.803891155489780074, -0.8185750573155089471, 3.188470185434109982 ) ) ;
#5413=CARTESIAN_POINT ( 'NONE',  ( 1.981271652668330052, -3.966334852594400662, 5.970160748022399488 ) ) ;
#5420=CARTESIAN_POINT ( 'NONE',  ( -1.616473591439278712, -1.610376859117309767, 5.965667796385567101 ) ) ;
#5426=CARTESIAN_POINT ( 'NONE',  ( -0.4339619423229766348, -0.1601694915254239793, 6.706578715862737461 ) ) ;
#5427=CARTESIAN_POINT ( 'NONE',  ( 1.071153154657499718, -2.545749267008810435, 7.128115444592616257 ) ) ;
#5429=CARTESIAN_POINT ( 'NONE',  ( -0.9345217207511814506, -5.211074464177369414, 2.212378604467589494 ) ) ;
#5430=CARTESIAN_POINT ( 'NONE',  ( 0.9707742057416334225, -5.426483050847465073, 6.508944043303927174 ) ) ;
#5432=CARTESIAN_POINT ( 'NONE',  ( 2.116444151961469178, -0.05338983050847489337, 3.670839500609350381 ) ) ;
#5436=CARTESIAN_POINT ( 'NONE',  ( -2.270487904532170198, -5.537711864406779760, 4.080813552109679776 ) ) ;
#5437=CARTESIAN_POINT ( 'NONE',  ( -1.468674196027810686, -4.362235753495300905, 6.910454658870877509 ) ) ;
#5438=CARTESIAN_POINT ( 'NONE',  ( -0.5385843327681574255, -3.683034516774964295, 2.101338688959530465 ) ) ;
#5441=CARTESIAN_POINT ( 'NONE',  ( 2.004091155098369104, -0.6361096273691766445, 4.254443623407341057 ) ) ;
#5444=CARTESIAN_POINT ( 'NONE',  ( 1.764243121571529960, -5.142630151795009930, 2.935756878428469996 ) ) ;
#5446=CARTESIAN_POINT ( 'NONE',  ( 1.000896394980339998, -0.4290254237288140260, 6.829956240957369751 ) ) ;
#5447=CARTESIAN_POINT ( 'NONE',  ( 0.9719602541832789155, -2.844656138396589817, 6.843370931913530519 ) ) ;
#5450=CARTESIAN_POINT ( 'NONE',  ( -2.484260633728970546, -5.542161016949150643, 3.766563288620799366 ) ) ;
#5457=CARTESIAN_POINT ( 'NONE',  ( 1.214457691475989920, -3.869340823081270031, 2.684103622926340194 ) ) ;
#5460=CARTESIAN_POINT ( 'NONE',  ( 1.536215498768950027, -5.033893599512579975, 2.912754292501710474 ) ) ;
#5464=CARTESIAN_POINT ( 'NONE',  ( -2.326448859701059746, -3.380286769027220029, 4.344498395672320434 ) ) ;
#5466=CARTESIAN_POINT ( 'NONE',  ( -0.4194839839382230595, -3.683034516774964295, 2.690289814463939777 ) ) ;
#5476=CARTESIAN_POINT ( 'NONE',  ( -1.846259792136611066, -5.246610169491530584, 3.802221692020929744 ) ) ;
#5477=CARTESIAN_POINT ( 'NONE',  ( -2.653886076156968699, -1.474488005747551567, 4.698454755023434792 ) ) ;
#5483=CARTESIAN_POINT ( 'NONE',  ( 1.652654650382400003, -0.7952867690272209522, 3.029252778805620050 ) ) ;
#5484=CARTESIAN_POINT ( 'NONE',  ( -2.508228811380011081, -0.2091101694915259990, 5.566973598334550744 ) ) ;
#5487=CARTESIAN_POINT ( 'NONE',  ( 1.526871680339569659, -0.04004237288135625850, 3.327650196883443101 ) ) ;
#5488=CARTESIAN_POINT ( 'NONE',  ( 2.329383452786330189, -1.028169651910100013, 5.035735636132829818 ) ) ;
#5491=CARTESIAN_POINT ( 'NONE',  ( -2.169623098572329489, -2.941650167909711122, 5.611855963201050734 ) ) ;
#5493=CARTESIAN_POINT ( 'NONE',  ( -2.354888465609351389, -5.502118644067805597, 5.923664702843871588 ) ) ;
#5496=FACE_OUTER_BOUND ( 'NONE', #11935, .T. ) ;
#5497=CARTESIAN_POINT ( 'NONE',  ( 2.022304719220918479, -0.3667372881355940861, 4.346496488058688712 ) ) ;
#5501=CARTESIAN_POINT ( 'NONE',  ( -0.1352600594605981310, -1.400782264522720366, 6.748562071049556188 ) ) ;
#5508=CARTESIAN_POINT ( 'NONE',  ( 2.046424002475610404, -0.3711864406779670222, 4.536201610417760044 ) ) ;
#5510=EDGE_CURVE ( 'NONE', #6595, #4345, #14683, .T. ) ;
#5512=CARTESIAN_POINT ( 'NONE',  ( -0.2683982510037440927, -3.407415933675483899, 2.059720455735791322 ) ) ;
#5514=CARTESIAN_POINT ( 'NONE',  ( 1.782460458101500889, -5.399788135593215799, 5.718585207845976015 ) ) ;
#5517=CARTESIAN_POINT ( 'NONE',  ( -1.661700935788390288, -0.2625000000000000111, 3.038299064211610112 ) ) ;
#5524=CARTESIAN_POINT ( 'NONE',  ( -2.035218756299248977, -4.781424942684484591, 2.996768277952679860 ) ) ;
#5528=CARTESIAN_POINT ( 'NONE',  ( 2.028464043723889887, -0.7292627805223297344, 5.016599851465070259 ) ) ;
#5535=CARTESIAN_POINT ( 'NONE',  ( 1.378221871957440170, -0.4201271186440679872, 6.607619368096269596 ) ) ;
#5536=CARTESIAN_POINT ( 'NONE',  ( -2.349464193210359930, -3.356998480738930368, 4.563019372514619754 ) ) ;
#5539=CARTESIAN_POINT ( 'NONE',  ( -2.130266475405059090, -5.555508474576275724, 3.117337770017961418 ) ) ;
#5545=CARTESIAN_POINT ( 'NONE',  ( -2.270487904532169754, -5.237711864406779050, 4.080813552109680664 ) ) ;
#5552=CARTESIAN_POINT ( 'NONE',  ( 1.401708661791409849, -4.358394877135329359, 6.590491606684049763 ) ) ;
#5553=CARTESIAN_POINT ( 'NONE',  ( -0.009452110982655099330, -5.299807955295455564, 2.649999999999998579 ) ) ;
#5557=CARTESIAN_POINT ( 'NONE',  ( -0.6918414964982418924, -3.659746228486680408, 2.450533167346770291 ) ) ;
#5560=CARTESIAN_POINT ( 'NONE',  ( 1.736825397686149852, -3.985782264522713447, 3.605313112995111702 ) ) ;
#5574=CARTESIAN_POINT ( 'NONE',  ( -1.392553072310521278, -5.264406779661021218, 3.191531554476531252 ) ) ;
#5575=CARTESIAN_POINT ( 'NONE',  ( -1.370891210199559618, -1.730659176918718956, 2.427606771969371469 ) ) ;
#5582=CARTESIAN_POINT ( 'NONE',  ( 2.322440385110930094, -2.518620102360550117, 4.319189883157390497 ) ) ;
#5583=CARTESIAN_POINT ( 'NONE',  ( -1.928470600873600782, -3.127956474216021299, 3.995796205495660391 ) ) ;
#5584=CARTESIAN_POINT ( 'NONE',  ( -2.293398556041709835, -0.2358050847457629773, 4.171956209133480975 ) ) ;
#5587=CARTESIAN_POINT ( 'NONE',  ( -2.000624272291700034, -0.5358050847457624943, 4.239366054776020576 ) ) ;
#5591=CARTESIAN_POINT ( 'NONE',  ( 0.2818998297622880012, -1.354205687946139935, 7.036509827384409554 ) ) ;
#5596=CARTESIAN_POINT ( 'NONE',  ( 1.948278411993589421, -2.406019537279080467, 6.020210936495999476 ) ) ;
#5597=CARTESIAN_POINT ( 'NONE',  ( 1.932035991685901122, -5.338983050847455836, 2.884370051397200818 ) ) ;
#5600=CARTESIAN_POINT ( 'NONE',  ( 1.480680413335799805, -1.214475958216410190, 6.529298007719799735 ) ) ;
#5601=CARTESIAN_POINT ( 'NONE',  ( 1.821706171509118954, -0.3978813559322044724, 5.646608543709396244 ) ) ;
#5606=CARTESIAN_POINT ( 'NONE',  ( 1.996236309555640798, -1.051457940198389673, 5.179523137126535559 ) ) ;
#5608=CARTESIAN_POINT ( 'NONE',  ( 2.354888465609351389, -0.3978813559322044724, 5.923664702843856489 ) ) ;
#5612=CARTESIAN_POINT ( 'NONE',  ( -1.289141334274979789, -0.1824152542372889096, 6.297747079672432413 ) ) ;
#5614=CARTESIAN_POINT ( 'NONE',  ( 0.1785884594055070773, -4.199217735477280833, 7.347870815423032553 ) ) ;
#5616=CARTESIAN_POINT ( 'NONE',  ( -1.294880990849879732, -4.829629811528119987, 3.097365952343163364 ) ) ;
#5617=CARTESIAN_POINT ( 'NONE',  ( -1.821706171509118954, -5.202118644067803999, 5.646608543709410455 ) ) ;
#5619=CARTESIAN_POINT ( 'NONE',  ( 1.750316316486830059, -0.04004237288135629319, 3.126818518378580158 ) ) ;
#5620=CARTESIAN_POINT ( 'NONE',  ( 2.155845792290829621, -5.355296610169490101, 3.756158857535770057 ) ) ;
#5625=CARTESIAN_POINT ( 'NONE',  ( 1.282210379528780031, -0.9388573751169240200, 6.673494927815259992 ) ) ;
#5627=CARTESIAN_POINT ( 'NONE',  ( -1.971820545011380821, -1.544352870612421880, 4.128313389260230615 ) ) ;
#5633=CARTESIAN_POINT ( 'NONE',  ( -0.7093417302541390468, -0.4646186440677970153, 6.943956659919700236 ) ) ;
#5634=CARTESIAN_POINT ( 'NONE',  ( -0.8986180677147959095, -3.636457940198390304, 2.524860635301629852 ) ) ;
#5637=CARTESIAN_POINT ( 'NONE',  ( -0.4221287159901280228, -5.457627118644064801, 7.320050063945812369 ) ) ;
#5640=CARTESIAN_POINT ( 'NONE',  ( -2.345900685764729765, -5.228813559322029292, 4.512231114381338948 ) ) ;
#5644=CARTESIAN_POINT ( 'NONE',  ( -0.1785884594054470975, -1.400782264522720366, 7.347870815423047652 ) ) ;
#5646=CARTESIAN_POINT ( 'NONE',  ( 0.2254033459420760055, -0.6247245358507570456, 2.348900562125120217 ) ) ;
#5647=CARTESIAN_POINT ( 'NONE',  ( 1.534924416212170017, -5.333856471232000018, 2.911460733964629899 ) ) ;
#5649=CARTESIAN_POINT ( 'NONE',  ( -2.192143888961709752, -1.381334852594400031, 5.556300681753639559 ) ) ;
#5650=EDGE_CURVE ( 'NONE', #10555, #7787, #6948, .T. ) ;
#5652=CARTESIAN_POINT ( 'NONE',  ( 2.192143888961729736, -4.218665147405599392, 5.556300681753580051 ) ) ;
#5655=CARTESIAN_POINT ( 'NONE',  ( -0.6470883152343470668, -3.030962444702889780, 6.648378442427256729 ) ) ;
#5660=CARTESIAN_POINT ( 'NONE',  ( 0.009452039534068971960, -5.000193177104105047, 2.350000000173209536 ) ) ;
#5668=CARTESIAN_POINT ( 'NONE',  ( 1.449568901432419343, -5.037500000000000533, 3.250431098567584165 ) ) ;
#5669=CARTESIAN_POINT ( 'NONE',  ( 1.837442528958791010, -2.056695212954759100, 2.785079989718789673 ) ) ;
#5676=CARTESIAN_POINT ( 'NONE',  ( 0.6673090596498160165, -2.239160642901090181, 2.443133963569570355 ) ) ;
#5677=CARTESIAN_POINT ( 'NONE',  ( 0.4625564304288019568, -2.592325843585391532, 6.700235833919842676 ) ) ;
#5678=CARTESIAN_POINT ( 'NONE',  ( 1.614765845140360589, -0.1067796610169500227, 5.967758800287426446 ) ) ;
#5681=EDGE_LOOP ( 'NONE', ( #17526, #11833, #11028, #12614 ) ) ;
#5682=CARTESIAN_POINT ( 'NONE',  ( -1.943632316591239917, -0.2536016949152539723, 3.373048379518170048 ) ) ;
#5683=CARTESIAN_POINT ( 'NONE',  ( -0.3159454637156809409, -2.984385868126319785, 7.032150113402090064 ) ) ;
#5687=CARTESIAN_POINT ( 'NONE',  ( -1.991984774470508590, -1.614217735477280202, 3.446707398186050764 ) ) ;
#5689=CARTESIAN_POINT ( 'NONE',  ( 2.043014502273419186, -5.341949152542365908, 3.006203457898239062 ) ) ;
#5691=CARTESIAN_POINT ( 'NONE',  ( 0.06276132972186961034, -1.377493976234430040, 7.052616990284530374 ) ) ;
#5693=CARTESIAN_POINT ( 'NONE',  ( 1.889104232906359870, -0.3444915254237289615, 3.296507079072520163 ) ) ;
#5699=CARTESIAN_POINT ( 'NONE',  ( 1.404946080800569375, -2.355602084342530933, 3.202993536195909208 ) ) ;
#5701=CARTESIAN_POINT ( 'NONE',  ( 1.973760952634081134, -0.3400423728813561364, 2.925986839873718992 ) ) ;
#5704=CARTESIAN_POINT ( 'NONE',  ( -0.7982439214406890082, -0.4690677966101705065, 6.591424794228156081 ) ) ;
#5705=ORIENTED_EDGE ( 'NONE', *, *, #5510, .F. ) ;
#5706=CARTESIAN_POINT ( 'NONE',  ( -0.1458667720079689645, -4.981295943764795453, 2.649245313618650677 ) ) ;
#5707=CARTESIAN_POINT ( 'NONE',  ( 2.058670345754650022, -5.350847457627120107, 3.559656372813920111 ) ) ;
#5714=CARTESIAN_POINT ( 'NONE',  ( 1.286937324407710026, -2.010118636378180224, 2.729584305145179801 ) ) ;
#5716=CARTESIAN_POINT ( 'NONE',  ( 0.6050872056802326648, -1.940253771513320125, 2.738171435586128410 ) ) ;
#5720=CARTESIAN_POINT ( 'NONE',  ( 1.192209327851080136, -0.02224576271186471527, 2.329031440774910422 ) ) ;
#5721=CARTESIAN_POINT ( 'NONE',  ( 0.6096110657044089276, -3.799475958216410376, 2.426869991387509806 ) ) ;
#5724=CARTESIAN_POINT ( 'NONE',  ( -2.560337424259679917, -5.237711864406785267, 4.001768473655595848 ) ) ;
#5732=CARTESIAN_POINT ( 'NONE',  ( 2.629224451638851434, -0.9583047870452394701, 4.339039509243856507 ) ) ;
#5734=CARTESIAN_POINT ( 'NONE',  ( 0.5677251586959709551, -5.311531839079339790, 2.399563163165729929 ) ) ;
#5736=CARTESIAN_POINT ( 'NONE',  ( -1.869848057046539891, -1.311469987729539932, 6.129130480762059463 ) ) ;
#5738=CARTESIAN_POINT ( 'NONE',  ( -0.4735094604798580353, -4.567989471729919870, 7.005327412390699671 ) ) ;
#5740=CARTESIAN_POINT ( 'NONE',  ( 1.503314099254039471, -3.939205687946139900, 3.301805249039985402 ) ) ;
#5742=CARTESIAN_POINT ( 'NONE',  ( 1.596341326794969984, -0.3355932203389830337, 2.970780074643809776 ) ) ;
#5754=CARTESIAN_POINT ( 'NONE',  ( 1.869504824896970119, -5.095338983050850423, 5.548311746956850143 ) ) ;
#5759=CARTESIAN_POINT ( 'NONE',  ( -1.882879255550339082, -5.103620102360555855, 2.835213315261639000 ) ) ;
#5762=CARTESIAN_POINT ( 'NONE',  ( 2.301223891756920104, -2.611773255513699876, 5.193066210047949660 ) ) ;
#5763=CARTESIAN_POINT ( 'NONE',  ( -0.8493734496527890476, -2.755343861603408939, 6.569081749323187225 ) ) ;
#5764=CARTESIAN_POINT ( 'NONE',  ( 1.202278654260740876, -0.1201271186440679706, 6.364093491318035589 ) ) ;
#5766=CARTESIAN_POINT ( 'NONE',  ( -1.880631435828179265, -0.5447033898305090327, 3.876649216148230437 ) ) ;
#5770=CARTESIAN_POINT ( 'NONE',  ( 0.5664586606772286093, -0.01334745762711899916, 2.726727161522279452 ) ) ;
#5771=CARTESIAN_POINT ( 'NONE',  ( -2.345213174852959881, -1.796683165423619943, 4.503223853122380049 ) ) ;
#5776=CARTESIAN_POINT ( 'NONE',  ( 2.353343516942209668, -3.826605122864669362, 4.722803042560139275 ) ) ;
#5778=CARTESIAN_POINT ( 'NONE',  ( -2.484260633728970546, -5.542161016949150643, 3.766563288620799366 ) ) ;
#5780=CARTESIAN_POINT ( 'NONE',  ( 2.116444151961470066, -0.3533898305084750002, 3.670839500609349937 ) ) ;
#5784=CARTESIAN_POINT ( 'NONE',  ( 1.985741519624368845, -2.495331814072259569, 4.178720363079467148 ) ) ;
#5788=CARTESIAN_POINT ( 'NONE',  ( 1.351903350398191206, -0.4156779661016956062, 6.245004350000406212 ) ) ;
#5791=CARTESIAN_POINT ( 'NONE',  ( -1.042222075699109407, -5.475423728813556323, 6.468743694056166227 ) ) ;
#5794=CARTESIAN_POINT ( 'NONE',  ( 2.088297318559229065, -0.09788135593220401165, 5.785136623276630807 ) ) ;
#5797=CARTESIAN_POINT ( 'NONE',  ( 2.326448859701049976, -2.219713230972780060, 4.344498395672269808 ) ) ;
#5799=CARTESIAN_POINT ( 'NONE',  ( 1.937109463115360253, -2.173136654396201184, 4.019920026366761157 ) ) ;
#5803=CARTESIAN_POINT ( 'NONE',  ( -2.058670345754650022, -0.5491525423728820243, 3.559656372813929881 ) ) ;
#5804=CARTESIAN_POINT ( 'NONE',  ( 2.354888465609351389, -0.3978813559322044724, 5.923664702843856489 ) ) ;
#5805=CARTESIAN_POINT ( 'NONE',  ( -0.9485663501270049647, -3.054250732991179440, 6.853826262002260528 ) ) ;
#5808=CARTESIAN_POINT ( 'NONE',  ( 2.332582362116870200, -5.068644067796610031, 4.387643303570810005 ) ) ;
#5816=CARTESIAN_POINT ( 'NONE',  ( -2.065623031241579977, -5.033755237495680213, 3.572193642975310279 ) ) ;
#5817=CARTESIAN_POINT ( 'NONE',  ( 1.864786684738361178, -0.7952867690272208412, 2.817120744449660652 ) ) ;
#5819=CARTESIAN_POINT ( 'NONE',  ( 2.326448859701049976, -2.219713230972780060, 4.344498395672269808 ) ) ;
#5822=CARTESIAN_POINT ( 'NONE',  ( 1.991984774470479946, -3.985782264522710339, 3.446707398186009907 ) ) ;
#5824=CARTESIAN_POINT ( 'NONE',  ( 1.372465729645801602, -4.335106588847043696, 6.226839763556046847 ) ) ;
#5829=CARTESIAN_POINT ( 'NONE',  ( -0.009452110982655715157, -0.5998079552954631577, 2.649999999999998579 ) ) ;
#5836=CARTESIAN_POINT ( 'NONE',  ( 0.7982439214406963357, -5.430932203389830626, 6.591424794228156081 ) ) ;
#5837=CARTESIAN_POINT ( 'NONE',  ( -2.445954350973251312, -2.941650167909708458, 5.729767452368195180 ) ) ;
#5843=CARTESIAN_POINT ( 'NONE',  ( -1.676695548152530968, -4.829629811528105776, 2.630596693608521885 ) ) ;
#5846=CARTESIAN_POINT ( 'NONE',  ( 2.352760675243219968, -2.565196678937129882, 4.757121734156020132 ) ) ;
#5848=CARTESIAN_POINT ( 'NONE',  ( 1.919159680931818990, -3.733451969711523155, 3.970803207828129455 ) ) ;
#5851=CARTESIAN_POINT ( 'NONE',  ( -1.943632316591239917, -0.2536016949152539723, 3.373048379518170048 ) ) ;
#5852=CARTESIAN_POINT ( 'NONE',  ( 1.978267656359410154, -0.4023305084745769644, 5.974740860598790171 ) ) ;
#5859=CARTESIAN_POINT ( 'NONE',  ( 0.5889081234606849957, -0.1379237288135600203, 6.978529000034869867 ) ) ;
#5860=CARTESIAN_POINT ( 'NONE',  ( -1.854177340199669954, -1.610376859117309989, 6.149404042554720284 ) ) ;
#5863=CARTESIAN_POINT ( 'NONE',  ( 2.199335452462551022, -3.733451969711521379, 3.862342996790889771 ) ) ;
#5864=CARTESIAN_POINT ( 'NONE',  ( -2.614198783383141045, -5.233262711864406391, 4.243032045539295360 ) ) ;
#5868=CARTESIAN_POINT ( 'NONE',  ( 1.725722849164588624, -0.4023305084745772420, 5.812007984777676661 ) ) ;
#5874=CARTESIAN_POINT ( 'NONE',  ( 1.472933559740161602, -2.751502985243430288, 6.130163826706326091 ) ) ;
#5882=CARTESIAN_POINT ( 'NONE',  ( 0.8731223871105069367, -0.4290254237288141370, 6.558046933601105799 ) ) ;
#5884=CARTESIAN_POINT ( 'NONE',  ( -0.7476103186298618253, -5.582203389830510787, 2.787995836256459636 ) ) ;
#5886=CARTESIAN_POINT ( 'NONE',  ( -0.4974685680287777023, -0.1601694915254239793, 7.000224381598740386 ) ) ;
#5887=CARTESIAN_POINT ( 'NONE',  ( -3.766169468773179610E-15, -5.599999999999999645, 2.349999999999999645 ) ) ;
#5891=CARTESIAN_POINT ( 'NONE',  ( -1.571912189623050127, -1.264893411152959946, 6.451524409078659872 ) ) ;
#5893=CARTESIAN_POINT ( 'NONE',  ( -0.1526488871098711508, -1.847100618360169699, 2.652660223633551251 ) ) ;
#5898=CARTESIAN_POINT ( 'NONE',  ( -1.666450993087168930, -0.4824152542372879826, 6.765380371283871597 ) ) ;
#5900=CARTESIAN_POINT ( 'NONE',  ( -1.626408692231610109, -4.707719201459649838, 6.401040991074980369 ) ) ;
#5904=CARTESIAN_POINT ( 'NONE',  ( -2.653602652190420574, -5.224364406779660186, 4.735326402787099376 ) ) ;
#5908=DIRECTION ( 'NONE',  ( 1.000000000000000000, 0.000000000000000000, -6.123233995736769734E-17 ) ) ;
#5911=CARTESIAN_POINT ( 'NONE',  ( -1.722199153441400066, -5.095857339597789526, 3.099360556065549943 ) ) ;
#5912=APPLICATION_CONTEXT ( 'automotive_design' ) ;
#5913=CARTESIAN_POINT ( 'NONE',  ( 0.2751970330256541808, -0.3251990024832501214, 2.050771348498781066 ) ) ;
#5916=CARTESIAN_POINT ( 'NONE',  ( 1.332058588847409908, -2.499172690432239996, 6.640197310420189680 ) ) ;
#5919=CARTESIAN_POINT ( 'NONE',  ( -2.461935615161759294, -1.680241723982170754, 5.690952430644365734 ) ) ;
#5920=DIRECTION ( 'NONE',  ( 1.000000000000000000, 9.028005242978079560E-48, -6.123233995736769734E-17 ) ) ;
#5921=CARTESIAN_POINT ( 'NONE',  ( -1.703239418290670049, -5.057043525783965876, 3.553755118148739900 ) ) ;
#5930=CARTESIAN_POINT ( 'NONE',  ( 0.05465110135556765225, -5.448728813559320372, 6.752241303418941243 ) ) ;
#5931=CARTESIAN_POINT ( 'NONE',  ( -2.635341251434490495, -3.011515032774579215, 5.013193520829514860 ) ) ;
#5938=CARTESIAN_POINT ( 'NONE',  ( 1.611907055891590002, -2.355602084342530045, 2.985210995296850189 ) ) ;
#5939=CARTESIAN_POINT ( 'NONE',  ( 1.566607907718229553, -1.167899381639830203, 6.026891670824254810 ) ) ;
#5940=CARTESIAN_POINT ( 'NONE',  ( -0.06264882350515391107, -0.1512711864406779960, 7.052569299041220319 ) ) ;
#5941=CARTESIAN_POINT ( 'NONE',  ( 0.007887181101543709258, -5.024994858181869972, 2.435887274406050462 ) ) ;
#5945=CARTESIAN_POINT ( 'NONE',  ( 2.235075160050071119, -3.966334852594401994, 6.130927224539736820 ) ) ;
#5946=CARTESIAN_POINT ( 'NONE',  ( -1.449568901432419343, -0.2625000000000002331, 3.250431098567584165 ) ) ;
#5947=CARTESIAN_POINT ( 'NONE',  ( -2.005512128484160161, -1.913124606865060029, 3.468469736471389897 ) ) ;
#5951=CARTESIAN_POINT ( 'NONE',  ( -2.322440385110939864, -3.081379897639439758, 4.319189883157441123 ) ) ;
#5953=CARTESIAN_POINT ( 'NONE',  ( -0.08231150243516484333, -5.598516949152545941, 2.050000000000001155 ) ) ;
#5957=CARTESIAN_POINT ( 'NONE',  ( -2.234315482767910144, -0.5402542372881360411, 3.960850823455329905 ) ) ;
#5961=CARTESIAN_POINT ( 'NONE',  ( 1.333132471082870918, -2.774791273531719060, 6.261300629978916454 ) ) ;
#5968=CARTESIAN_POINT ( 'NONE',  ( -1.725722849164588624, -5.497669491525425833, 5.812007984777676661 ) ) ;
#5970=FACE_OUTER_BOUND ( 'NONE', #15749, .T. ) ;
#5972=CARTESIAN_POINT ( 'NONE',  ( 2.549960444629811640, -4.055647129387581984, 3.964598460822105874 ) ) ;
#5975=CARTESIAN_POINT ( 'NONE',  ( -1.021156010535440029, -1.753947465207009948, 2.579625955254300163 ) ) ;
#5979=CARTESIAN_POINT ( 'NONE',  ( 1.777111910197639810, -2.126560077819629413, 3.672004328189181432 ) ) ;
#5984=CARTESIAN_POINT ( 'NONE',  ( 2.589817782457058737, -0.6361096273691766445, 4.120381550729950604 ) ) ;
#5987=CARTESIAN_POINT ( 'NONE',  ( -1.460675875430050175, -4.684430913171359734, 6.545310725710059785 ) ) ;
#5990=CARTESIAN_POINT ( 'NONE',  ( -2.087380238839969593, -5.193220338983044471, 6.338810156469112833 ) ) ;
#5997=CARTESIAN_POINT ( 'NONE',  ( 2.651429253058529945, -0.9815930753335269099, 4.585822029124893895 ) ) ;
#5998=CARTESIAN_POINT ( 'NONE',  ( -0.009452110982655099330, -0.5998079552954631577, 2.649999999999998579 ) ) ;
#6000=CARTESIAN_POINT ( 'NONE',  ( 1.948278411993589865, -2.406019537279080467, 6.020210936496000365 ) ) ;
#6002=CARTESIAN_POINT ( 'NONE',  ( -0.4247583764260595141, -1.424070552811000701, 7.319674410047512403 ) ) ;
#6004=CARTESIAN_POINT ( 'NONE',  ( -1.117157304995339606, -4.661142624883069630, 6.422457952614126775 ) ) ;
#6006=CARTESIAN_POINT ( 'NONE',  ( 2.270487904532159984, -0.3622881355932209835, 4.080813552109670894 ) ) ;
#6009=STYLED_ITEM ( 'NONE', ( #5385 ), #1876 ) ;
#6016=CARTESIAN_POINT ( 'NONE',  ( -1.614765845140348821, -5.493220338983046069, 5.967758800287426446 ) ) ;
#6018=CARTESIAN_POINT ( 'NONE',  ( 0.7137241095604313079, -3.500569086828633658, 2.143887406933319362 ) ) ;
#6023=CARTESIAN_POINT ( 'NONE',  ( -0.1569242594330230167, -1.400782264522720144, 7.048216443236290374 ) ) ;
#6025=CARTESIAN_POINT ( 'NONE',  ( -1.914021115237000137, -4.754295778036220277, 6.069404563272239983 ) ) ;
#6026=CARTESIAN_POINT ( 'NONE',  ( -1.436030008293460503, -4.408812330071866015, 6.167214932417466322 ) ) ;
#6027=CARTESIAN_POINT ( 'NONE',  ( 0.001589539283869510202, -5.124807148327449546, 2.499688892524289496 ) ) ;
#6029=CARTESIAN_POINT ( 'NONE',  ( 0.9038768003982520227, -4.129352870612409632, 7.195219513931331967 ) ) ;
#6030=CARTESIAN_POINT ( 'NONE',  ( 2.046424002475610404, -0.07118644067796651986, 4.536201610417760044 ) ) ;
#6031=CARTESIAN_POINT ( 'NONE',  ( 2.337178851518220135, -2.588484967225419986, 4.976298214796759822 ) ) ;
#6033=ORIENTED_EDGE ( 'NONE', *, *, #8895, .F. ) ;
#6037=CARTESIAN_POINT ( 'NONE',  ( -0.9170541073686518940, -4.315659176918721585, 6.867431071947199150 ) ) ;
#6039=CARTESIAN_POINT ( 'NONE',  ( 2.304156201936080617, -5.099788135593215976, 6.016707707703351282 ) ) ;
#6042=CARTESIAN_POINT ( 'NONE',  ( 2.353194804772640314, -0.3756355932203400139, 4.731327187377229571 ) ) ;
#6047=CARTESIAN_POINT ( 'NONE',  ( -2.029711248330079876, -3.380286769027221805, 4.391497016172549728 ) ) ;
#6048=CARTESIAN_POINT ( 'NONE',  ( 2.386628511786341722, -0.05338983050847501133, 3.539457309197775459 ) ) ;
#6053=CARTESIAN_POINT ( 'NONE',  ( 0.4339619423229844619, -5.439830508474575943, 6.706578715862737461 ) ) ;
#6055=CARTESIAN_POINT ( 'NONE',  ( -2.623186471072040504, -3.380286769027221805, 4.297499775172091141 ) ) ;
#6057=CARTESIAN_POINT ( 'NONE',  ( 2.351999299633229956, -2.266289807549350055, 4.782734406438239994 ) ) ;
#6060=CARTESIAN_POINT ( 'NONE',  ( 0.4194839839381755975, -1.916965483225031130, 2.690289814463930895 ) ) ;
#6068=CARTESIAN_POINT ( 'NONE',  ( -2.470260739716218179, -1.567641158900710430, 3.729986819255259878 ) ) ;
#6070=CARTESIAN_POINT ( 'NONE',  ( -0.4617942143426889690, -0.5906145504024210569, 2.383143958488499692 ) ) ;
#6074=CARTESIAN_POINT ( 'NONE',  ( 2.143090896833110381, -5.095338983050850423, 5.672454929438339732 ) ) ;
#6082=CARTESIAN_POINT ( 'NONE',  ( -2.612083973477999699, -1.819971453711898945, 4.230818789270855085 ) ) ;
#6086=CARTESIAN_POINT ( 'NONE',  ( 1.781655196750449921, -2.079983501243049648, 3.162323035427780482 ) ) ;
#6087=CARTESIAN_POINT ( 'NONE',  ( 1.730954623551391736, -5.333856471231995577, 2.683219139909288842 ) ) ;
#6089=CARTESIAN_POINT ( 'NONE',  ( -0.6672256841320821641, -1.447358841099289251, 7.268642361138727637 ) ) ;
#6091=CARTESIAN_POINT ( 'NONE',  ( -2.036910256464079971, -4.940602084342534894, 4.443293066459140128 ) ) ;
#6095=CARTESIAN_POINT ( 'NONE',  ( 0.5677251586959709551, -5.311531839079339790, 2.399563163165729929 ) ) ;
#6101=CARTESIAN_POINT ( 'NONE',  ( 2.245209214543399945, -2.635061543801989981, 5.405536158119010004 ) ) ;
#6103=CARTESIAN_POINT ( 'NONE',  ( 2.332582362116870200, -5.368644067796609853, 4.387643303570810005 ) ) ;
#6107=CARTESIAN_POINT ( 'NONE',  ( -1.552749016687749783, -1.563800282540730002, 6.468535037441760061 ) ) ;
#6109=CARTESIAN_POINT ( 'NONE',  ( -0.2620510901103649815, -3.706322805063249959, 2.361180871966390260 ) ) ;
#6110=CARTESIAN_POINT ( 'NONE',  ( 1.876226141297899774, -0.8884399221803740421, 3.866526959224306115 ) ) ;
#6117=CARTESIAN_POINT ( 'NONE',  ( 0.7476103186298468373, -0.3177966101694921219, 2.787995836256459636 ) ) ;
#6118=CARTESIAN_POINT ( 'NONE',  ( 0.1768565782245979934, -3.752899381639830168, 2.353200596935780098 ) ) ;
#6125=CARTESIAN_POINT ( 'NONE',  ( -0.06276132972181576453, -4.222506023765570937, 7.052616990284527709 ) ) ;
#6127=CARTESIAN_POINT ( 'NONE',  ( 2.650076489488250697, -5.077542372881359789, 4.841243018609314497 ) ) ;
#6129=CARTESIAN_POINT ( 'NONE',  ( -1.943632316591239917, -0.5536016949152539057, 3.373048379518170048 ) ) ;
#6135=CARTESIAN_POINT ( 'NONE',  ( -1.279347147864589251, -3.566593075333521767, 3.094331068408299412 ) ) ;
#6136=CARTESIAN_POINT ( 'NONE',  ( -2.651721837666119796, -0.5269067796610176213, 4.594045830208265180 ) ) ;
#6145=CARTESIAN_POINT ( 'NONE',  ( -0.2189795514005259958, -5.595550847457629651, 2.356806637999020015 ) ) ;
#6148=CARTESIAN_POINT ( 'NONE',  ( -0.4478021372196530070, -0.2909039927201509945, 2.380136890750930156 ) ) ;
#6149=CARTESIAN_POINT ( 'NONE',  ( 1.576846334488021473, -3.892629111369556139, 2.565364356520400513 ) ) ;
#6152=CARTESIAN_POINT ( 'NONE',  ( -1.074829861819750043, -3.314262780522330143, 2.606322265575609975 ) ) ;
#6156=CARTESIAN_POINT ( 'NONE',  ( 1.520647680314149541, -3.640298816558361406, 3.320676805464615633 ) ) ;
#6161=CARTESIAN_POINT ( 'NONE',  ( 0.7854158957161911925, -1.963542059801608897, 2.803154272645130618 ) ) ;
#6164=CARTESIAN_POINT ( 'NONE',  ( -2.642463257358080853, -1.451199717459271454, 4.945970783863430142 ) ) ;
#6166=CARTESIAN_POINT ( 'NONE',  ( -0.009452110982655708218, -0.5998079552954630467, 2.350000000000000089 ) ) ;
#6170=CARTESIAN_POINT ( 'NONE',  ( -0.7983658734557950165, -5.166525423728809407, 6.913847129767330735 ) ) ;
#6177=CARTESIAN_POINT ( 'NONE',  ( 1.213493134184789657, -2.285737219477670390, 2.339799138571409642 ) ) ;
#6183=CARTESIAN_POINT ( 'NONE',  ( 0.9485663501270550357, -2.545749267008810435, 6.853826262002240988 ) ) ;
#6185=CARTESIAN_POINT ( 'NONE',  ( 2.306572132003631648, -1.121322805063259542, 6.012569500204132389 ) ) ;
#6199=CARTESIAN_POINT ( 'NONE',  ( 1.265407828724300021, -2.309025507765960050, 2.715689360385540319 ) ) ;
#6202=CARTESIAN_POINT ( 'NONE',  ( 1.694257473570984995, -0.4987256491549267312, 3.023551124676525426 ) ) ;
#6207=CARTESIAN_POINT ( 'NONE',  ( 0.8242394280877100021, -4.428259742000189902, 6.904399023015010073 ) ) ;
#6208=CARTESIAN_POINT ( 'NONE',  ( 2.050563521385710075, -1.004881363621820567, 4.800454404529174823 ) ) ;
#6212=CARTESIAN_POINT ( 'NONE',  ( -1.880631435828179265, -0.2447033898305090438, 3.876649216148230437 ) ) ;
#6213=CARTESIAN_POINT ( 'NONE',  ( 2.260890494820590124, -4.055647129387580208, 4.046455925041149371 ) ) ;
#6219=CARTESIAN_POINT ( 'NONE',  ( -2.386628511786350160, -5.246610169491530584, 3.539457309197792778 ) ) ;
#6223=CARTESIAN_POINT ( 'NONE',  ( 2.318251751302029984, -0.3667372881355940306, 4.294764266798990704 ) ) ;
#6225=CARTESIAN_POINT ( 'NONE',  ( 1.912899118714319169, -4.218665147405596727, 5.445465495009710111 ) ) ;
#6226=CARTESIAN_POINT ( 'NONE',  ( -0.3171869470818471370, -0.4557203389830515317, 7.334814496515233095 ) ) ;
#6229=CARTESIAN_POINT ( 'NONE',  ( -1.467041701146829746, -0.4779661016949154906, 6.911479965439912831 ) ) ;
#6234=CARTESIAN_POINT ( 'NONE',  ( -0.06264882350515386944, -0.1512711864406780238, 7.052569299041217654 ) ) ;
#6235=CARTESIAN_POINT ( 'NONE',  ( 2.550815101416278541, -4.195376859117311064, 5.432431574543660879 ) ) ;
#6238=CARTESIAN_POINT ( 'NONE',  ( -1.526791597786389953, -2.825208726468269926, 6.490992212270280781 ) ) ;
#6241=CARTESIAN_POINT ( 'NONE',  ( -0.5805547688319036004, -3.360839357098899693, 2.730772231808969774 ) ) ;
#6243=CARTESIAN_POINT ( 'NONE',  ( -0.8893259633308450152, -1.753947465207011058, 2.849594321892158888 ) ) ;
#6246=CARTESIAN_POINT ( 'NONE',  ( 1.722095088963199405, -0.7763906680874423927, 2.675734922583239861 ) ) ;
#6247=CARTESIAN_POINT ( 'NONE',  ( -0.2041457401073759059, -1.101875393134940984, 7.346023093209487875 ) ) ;
#6252=CARTESIAN_POINT ( 'NONE',  ( -1.596341326794979976, -5.264406779661020330, 2.970780074643819990 ) ) ;
#6257=CARTESIAN_POINT ( 'NONE',  ( 0.2254033459420760055, -0.6247245358507570456, 2.348900562125120217 ) ) ;
#6259=CARTESIAN_POINT ( 'NONE',  ( -0.9490039995899379743, -2.076142624883081211, 2.221592224478750488 ) ) ;
#6262=CARTESIAN_POINT ( 'NONE',  ( 0.6343239990445400656, -3.500569086828630105, 2.433641963034069988 ) ) ;
#6264=CARTESIAN_POINT ( 'NONE',  ( 0.4944444514933294954, -5.311531839079339790, 2.693008931300498787 ) ) ;
#6266=CARTESIAN_POINT ( 'NONE',  ( -2.639965200365840037, -1.750106588847040845, 4.971472712918284742 ) ) ;
#6268=CARTESIAN_POINT ( 'NONE',  ( -2.350067830300900162, -0.5224576271186440746, 4.825253242917699303 ) ) ;
#6272=CARTESIAN_POINT ( 'NONE',  ( -1.978267656359410154, -5.497669491525420504, 5.974740860598790171 ) ) ;
#6280=CARTESIAN_POINT ( 'NONE',  ( 1.167621112247380077, -2.821367850108300157, 6.743381174846749815 ) ) ;
#6281=CARTESIAN_POINT ( 'NONE',  ( 1.943632316591230147, -5.346398305084740343, 3.373048379518159834 ) ) ;
#6283=CARTESIAN_POINT ( 'NONE',  ( -2.308170020371289599, -1.726818300558750074, 5.159452766389659217 ) ) ;
#6284=CARTESIAN_POINT ( 'NONE',  ( -1.917298190932639868, -3.496728210468659892, 3.335187436117939885 ) ) ;
#6285=CARTESIAN_POINT ( 'NONE',  ( 2.032257487115179728, -1.028169651910100679, 4.991258216523873692 ) ) ;
#6292=CARTESIAN_POINT ( 'NONE',  ( 1.392553072310509510, -0.3355932203389832558, 3.191531554476519261 ) ) ;
#6293=CARTESIAN_POINT ( 'NONE',  ( 2.353452300571019506, -4.125511994252439862, 4.697179287168359529 ) ) ;
#6297=EDGE_CURVE ( 'NONE', #12628, #2833, #4510, .T. ) ;
#6300=CARTESIAN_POINT ( 'NONE',  ( -2.151546283159489814, -4.711560077819619607, 3.746273477677510844 ) ) ;
#6301=CARTESIAN_POINT ( 'NONE',  ( 0.2812789908084389889, -5.144279661016950556, 7.036533610117280624 ) ) ;
#6304=CARTESIAN_POINT ( 'NONE',  ( 2.345900685764729765, -0.3711864406779670222, 4.512231114381330066 ) ) ;
#6307=CARTESIAN_POINT ( 'NONE',  ( -0.03076623656502111559, -4.521412895153344103, 6.752792069673816400 ) ) ;
#6308=CARTESIAN_POINT ( 'NONE',  ( -2.625437065641401446, -0.5180084745762725262, 5.087214675345155257 ) ) ;
#6310=CARTESIAN_POINT ( 'NONE',  ( -1.782460458101500889, -0.5002118644067795605, 5.718585207845990226 ) ) ;
#6312=CARTESIAN_POINT ( 'NONE',  ( 1.347262683220810553, -0.4245762711864407013, 6.986424775243341045 ) ) ;
#6314=CARTESIAN_POINT ( 'NONE',  ( -2.011500846714319835, -5.551059322033900401, 3.478373409938470218 ) ) ;
#6316=CARTESIAN_POINT ( 'NONE',  ( -0.8242394280876598200, -1.171740257999809964, 6.904399023015030501 ) ) ;
#6317=CARTESIAN_POINT ( 'NONE',  ( -1.061361729696689515, -0.2742238837839081067, 2.926312958971010847 ) ) ;
#6318=CARTESIAN_POINT ( 'NONE',  ( -2.008025181017680794, -3.520016498756949552, 2.964791492240541171 ) ) ;
#6320=CARTESIAN_POINT ( 'NONE',  ( -2.322440385110939864, -3.081379897639439758, 4.319189883157439347 ) ) ;
#6323=CARTESIAN_POINT ( 'NONE',  ( 2.041954431566909367, -3.849893411152959910, 4.912894203848615859 ) ) ;
#6326=CARTESIAN_POINT ( 'NONE',  ( -1.736825397686170502, -1.614217735477279536, 3.605313112995154334 ) ) ;
#6335=CARTESIAN_POINT ( 'NONE',  ( -2.353194804772640314, -5.224364406779660186, 4.731327187377240229 ) ) ;
#6342=CARTESIAN_POINT ( 'NONE',  ( -1.965557623688110933, -5.511016949152534927, 5.292675575926340414 ) ) ;
#6343=CARTESIAN_POINT ( 'NONE',  ( 2.574214976178930137, -2.196424942684489956, 4.054607910322744146 ) ) ;
#6345=CARTESIAN_POINT ( 'NONE',  ( -1.071153154657450202, -3.054250732991181216, 7.128115444592631356 ) ) ;
#6348=CARTESIAN_POINT ( 'NONE',  ( -1.611907055891630192, -3.244397915657459830, 2.985210995296889713 ) ) ;
#6351=CARTESIAN_POINT ( 'NONE',  ( 1.901407128523888934, -2.751502985243430288, 6.551422324754781812 ) ) ;
#6356=CARTESIAN_POINT ( 'NONE',  ( -2.091095264232510242, -1.656953435693890198, 5.779845490516250628 ) ) ;
#6358=CARTESIAN_POINT ( 'NONE',  ( -2.088297318559229954, -5.502118644067800268, 5.785136623276639689 ) ) ;
#6361=CARTESIAN_POINT ( 'NONE',  ( 0.2270348434643680025, -5.304612347394249916, 2.348896311281980065 ) ) ;
#6367=CARTESIAN_POINT ( 'NONE',  ( 0.1226612266411070129, -2.937809291549740021, 7.050255286338659388 ) ) ;
#6369=CARTESIAN_POINT ( 'NONE',  ( -1.596341326794979976, -5.564406779661021041, 2.970780074643819990 ) ) ;
#6372=CARTESIAN_POINT ( 'NONE',  ( 1.902324933209389890, -2.402178660919109809, 3.314393441133530072 ) ) ;
#6373=CARTESIAN_POINT ( 'NONE',  ( -0.8986180677147959095, -3.636457940198390304, 2.524860635301629852 ) ) ;
#6374=CARTESIAN_POINT ( 'NONE',  ( 0.2475374578675958726, -1.354205687946139491, 6.738044908627027318 ) ) ;
#6380=CARTESIAN_POINT ( 'NONE',  ( -0.6918414964982418924, -3.659746228486680408, 2.450533167346770291 ) ) ;
#6387=CARTESIAN_POINT ( 'NONE',  ( 1.112838723655040107, -5.126483050847459921, 6.773667561836210105 ) ) ;
#6393=CARTESIAN_POINT ( 'NONE',  ( -1.555285212483289659, -3.520016498756949552, 3.359854578615099285 ) ) ;
#6395=CARTESIAN_POINT ( 'NONE',  ( -2.171642826483958899, -0.4957627118644069575, 6.225392547715731695 ) ) ;
#6399=CARTESIAN_POINT ( 'NONE',  ( 2.458531667407859889, -0.09343220338983100615, 5.699238225248945966 ) ) ;
#6403=CARTESIAN_POINT ( 'NONE',  ( 0.2564439965879029004, -1.055298816558370323, 7.039440566481206751 ) ) ;
#6404=CARTESIAN_POINT ( 'NONE',  ( 2.155845792290829621, -5.355296610169490101, 3.756158857535770057 ) ) ;
#6406=CARTESIAN_POINT ( 'NONE',  ( 2.649108131072720695, -0.7059744922340407403, 4.859184807329644862 ) ) ;
#6407=ORIENTED_EDGE ( 'NONE', *, *, #9830, .F. ) ;
#6410=CARTESIAN_POINT ( 'NONE',  ( 0.9485663501270550357, -2.545749267008810435, 6.853826262002240988 ) ) ;
#6411=CARTESIAN_POINT ( 'NONE',  ( 2.550815101416278541, -4.195376859117311064, 5.432431574543660879 ) ) ;
#6418=CARTESIAN_POINT ( 'NONE',  ( -2.025702773739959106, -3.081379897639443310, 4.366188503657674858 ) ) ;
#6421=CARTESIAN_POINT ( 'NONE',  ( 0.03076623656506880661, -1.078587104846650213, 6.752792069673816400 ) ) ;
#6426=CARTESIAN_POINT ( 'NONE',  ( 0.2151249875495270247, -0.3251990024832489556, 2.650810719223910983 ) ) ;
#6427=CARTESIAN_POINT ( 'NONE',  ( -2.146130664537640786, -3.197821339080880065, 3.138834773724098692 ) ) ;
#6430=CARTESIAN_POINT ( 'NONE',  ( 0.06276132972186961034, -1.377493976234430040, 7.052616990284530374 ) ) ;
#6432=CARTESIAN_POINT ( 'NONE',  ( -2.088297318559229954, -5.202118644067800446, 5.785136623276639689 ) ) ;
#6435=EDGE_CURVE ( 'NONE', #11001, #14847, #336, .T. ) ;
#6442=CARTESIAN_POINT ( 'NONE',  ( -0.7476103186298618253, -5.582203389830510787, 2.787995836256459636 ) ) ;
#6445=CARTESIAN_POINT ( 'NONE',  ( -2.594645788401189090, -2.988226744486289999, 5.257608218854294968 ) ) ;
#6447=CARTESIAN_POINT ( 'NONE',  ( 2.065789008933020199, -2.728214696955149510, 6.366022047745297563 ) ) ;
#6451=CARTESIAN_POINT ( 'NONE',  ( -1.644832646965619816, -4.408812330071869567, 6.383232381746489992 ) ) ;
#6452=CARTESIAN_POINT ( 'NONE',  ( 1.661700935788380074, -5.337500000000000355, 3.038299064211610112 ) ) ;
#6455=CARTESIAN_POINT ( 'NONE',  ( -1.788074174585561060, -1.982989471729918352, 2.738902236199820539 ) ) ;
#6459=CARTESIAN_POINT ( 'NONE',  ( 1.057242234132090175, -0.3222457627118650025, 2.597442975781520058 ) ) ;
#6461=CARTESIAN_POINT ( 'NONE',  ( 1.265407828724300021, -2.309025507765960050, 2.715689360385540319 ) ) ;
#6462=CARTESIAN_POINT ( 'NONE',  ( -0.009452110982656868748, -5.299807955295460005, 2.350000000000000089 ) ) ;
#6465=CARTESIAN_POINT ( 'NONE',  ( -2.180207327701300102, -5.506567796610169374, 5.586116916730199833 ) ) ;
#6475=CARTESIAN_POINT ( 'NONE',  ( 2.126557263589630153, -2.448755237495689574, 3.691783806836010040 ) ) ;
#6477=CARTESIAN_POINT ( 'NONE',  ( -2.011500846714319835, -5.551059322033900401, 3.478373409938470218 ) ) ;
#6480=CARTESIAN_POINT ( 'NONE',  ( 1.832842064134690085, -2.728214696955149954, 6.176291182464479945 ) ) ;
#6482=CARTESIAN_POINT ( 'NONE',  ( -1.043047520545169471, -1.517223705964159786, 6.468319459971155538 ) ) ;
#6486=CARTESIAN_POINT ( 'NONE',  ( 1.568166175152220010, -0.5822263355386709804, 3.139533976446129859 ) ) ;
#6488=CARTESIAN_POINT ( 'NONE',  ( 2.313035575219750228, -4.172088570829020071, 5.134294963419709923 ) ) ;
#6497=CARTESIAN_POINT ( 'NONE',  ( 1.300961508564179914, -5.122033898305089927, 6.661123742937279602 ) ) ;
#6500=CARTESIAN_POINT ( 'NONE',  ( -2.262450597846770162, -1.404623140882689913, 5.348122657979730299 ) ) ;
#6503=CARTESIAN_POINT ( 'NONE',  ( 0.8967027089123184025, -4.404971453711897134, 6.546842195331636916 ) ) ;
#6505=CARTESIAN_POINT ( 'NONE',  ( 0.7983658734558030101, -0.1334745762711870010, 6.913847129767330735 ) ) ;
#6507=CARTESIAN_POINT ( 'NONE',  ( -2.651721837666119796, -0.2269067796610169385, 4.594045830208265180 ) ) ;
#6509=CARTESIAN_POINT ( 'NONE',  ( -1.750316316486840051, -5.559957627118639500, 3.126818518378589928 ) ) ;
#6510=CARTESIAN_POINT ( 'NONE',  ( -1.728413393879669968, -1.288181699441249606, 6.297289212178331042 ) ) ;
#6511=ADVANCED_FACE ( 'NONE', ( #16837 ), #4423, .F. ) ;
#6513=CARTESIAN_POINT ( 'NONE',  ( 0.4974685680287860290, -5.439830508474580384, 7.000224381598740386 ) ) ;
#6514=CARTESIAN_POINT ( 'NONE',  ( -2.649108131072720695, -4.894025507765944916, 4.859184807329705258 ) ) ;
#6517=CARTESIAN_POINT ( 'NONE',  ( 2.345213174852950111, -3.803316834576380145, 4.503223853122319653 ) ) ;
#6520=CARTESIAN_POINT ( 'NONE',  ( -0.3943683997330095781, -3.384127645387192018, 2.685210827922659860 ) ) ;
#6524=CARTESIAN_POINT ( 'NONE',  ( -0.3429245540020551819, -1.823812330071880705, 2.675820019639910452 ) ) ;
#6531=CARTESIAN_POINT ( 'NONE',  ( 1.864786684738361178, -0.7952867690272208412, 2.817120744449660652 ) ) ;
#6532=CARTESIAN_POINT ( 'NONE',  ( 2.502804106625939440, -2.173136654396201184, 3.817341913956370458 ) ) ;
#6534=CARTESIAN_POINT ( 'NONE',  ( -1.229686204202100175, -5.164643153926309793, 2.674737924334550154 ) ) ;
#6535=CARTESIAN_POINT ( 'NONE',  ( 1.869504824896970119, -5.095338983050850423, 5.548311746956850143 ) ) ;
#6545=CARTESIAN_POINT ( 'NONE',  ( -0.7983658734557950165, -5.466525423728810118, 6.913847129767330735 ) ) ;
#6546=CARTESIAN_POINT ( 'NONE',  ( 2.479511223993269287, -3.733451969711523155, 3.753882785753661633 ) ) ;
#6548=CARTESIAN_POINT ( 'NONE',  ( -2.632194480419669080, -3.310421904162345719, 5.038623552414950524 ) ) ;
#6551=CARTESIAN_POINT ( 'NONE',  ( -1.794646911016549939, -4.432100618360159672, 6.222494056560700315 ) ) ;
#6554=CARTESIAN_POINT ( 'NONE',  ( 1.991177874369370882, -2.378890372630820149, 2.945484578117438801 ) ) ;
#6558=CARTESIAN_POINT ( 'NONE',  ( 0.4539185741479240255, -2.215872354612800521, 2.390735265170440105 ) ) ;
#6559=CARTESIAN_POINT ( 'NONE',  ( 0.007090208766911279895, -5.037626194832210302, 2.248104425785700133 ) ) ;
#6561=CARTESIAN_POINT ( 'NONE',  ( -2.318251751302029984, -5.533262711864409766, 4.294764266798999586 ) ) ;
#6565=CARTESIAN_POINT ( 'NONE',  ( 2.351526912647309953, -5.073093220338978249, 4.606040641882800379 ) ) ;
#6569=CARTESIAN_POINT ( 'NONE',  ( 1.991984774470479946, -3.985782264522710339, 3.446707398186009907 ) ) ;
#6571=CARTESIAN_POINT ( 'NONE',  ( -2.088297318559229954, -5.502118644067800268, 5.785136623276639689 ) ) ;
#6573=CARTESIAN_POINT ( 'NONE',  ( -0.3159454637156809409, -2.984385868126319785, 7.032150113402090064 ) ) ;
#6574=CARTESIAN_POINT ( 'NONE',  ( -1.820241257191459905, -5.080331814072259533, 3.208199930689799917 ) ) ;
#6575=CARTESIAN_POINT ( 'NONE',  ( -0.3257255101953093757, -1.424070552811000701, 6.727018681373241549 ) ) ;
#6579=CARTESIAN_POINT ( 'NONE',  ( 1.595232607690389992, -5.306696984248650217, 3.104767392309609964 ) ) ;
#6582=CARTESIAN_POINT ( 'NONE',  ( -1.092567884283820012, -4.637854336594780413, 6.784476218553590066 ) ) ;
#6588=CARTESIAN_POINT ( 'NONE',  ( -2.270487904532170198, -5.237711864406779938, 4.080813552109679776 ) ) ;
#6591=CARTESIAN_POINT ( 'NONE',  ( -2.629224451638860760, -4.641695212954759064, 4.339039509243916015 ) ) ;
#6593=CARTESIAN_POINT ( 'NONE',  ( -2.345213174852959881, -1.796683165423619943, 4.503223853122380049 ) ) ;
#6594=CARTESIAN_POINT ( 'NONE',  ( 1.000896394980339998, -0.1290254237288140093, 6.829956240957369751 ) ) ;
#6595=VERTEX_POINT ( 'NONE', #7478 ) ;
#6596=CARTESIAN_POINT ( 'NONE',  ( 2.203023580853990193, -0.3578389830508479919, 3.872235369154280349 ) ) ;
#6597=CARTESIAN_POINT ( 'NONE',  ( 0.2189795514005130062, -0.3044491525423729805, 2.356806637999009801 ) ) ;
#6601=CARTESIAN_POINT ( 'NONE',  ( -2.343457872958619959, -1.451199717459270122, 4.916681529328610800 ) ) ;
#6602=CARTESIAN_POINT ( 'NONE',  ( -2.180207327701300102, -5.506567796610169374, 5.586116916730199833 ) ) ;
#6603=CARTESIAN_POINT ( 'NONE',  ( -1.373536515609910191, -1.218316834576379737, 6.970795264502737787 ) ) ;
#6606=CARTESIAN_POINT ( 'NONE',  ( 2.004091155098369104, -0.6361096273691766445, 4.254443623407341057 ) ) ;
#6607=CARTESIAN_POINT ( 'NONE',  ( 1.882879255550339082, -0.4963798976394455664, 2.835213315261639000 ) ) ;
#6610=CARTESIAN_POINT ( 'NONE',  ( -2.050563521385710075, -4.595118636378185073, 4.800454404529219232 ) ) ;
#6613=CARTESIAN_POINT ( 'NONE',  ( 0.7368491673939637776, -3.523857375116919322, 2.783765372628159263 ) ) ;
#6617=CARTESIAN_POINT ( 'NONE',  ( 1.327748599278330000, -0.4480353997208159633, 2.745754414290000334 ) ) ;
#6618=CARTESIAN_POINT ( 'NONE',  ( -1.524497189778160289, -2.801920438179980710, 6.872331008700187205 ) ) ;
#6622=CARTESIAN_POINT ( 'NONE',  ( -2.041338374031088865, -5.219915254237295521, 4.918217215283674726 ) ) ;
#6630=CARTESIAN_POINT ( 'NONE',  ( 0.4974685680287860290, -5.439830508474580384, 7.000224381598740386 ) ) ;
#6631=CARTESIAN_POINT ( 'NONE',  ( 2.091881088960109825, -3.989623140882676555, 6.333140288723826394 ) ) ;
#6633=CARTESIAN_POINT ( 'NONE',  ( -2.327043743583479429, -3.217268751009201289, 5.975923629552665872 ) ) ;
#6635=CARTESIAN_POINT ( 'NONE',  ( -0.06276132972181580616, -4.222506023765570049, 7.052616990284530374 ) ) ;
#6639=CARTESIAN_POINT ( 'NONE',  ( -0.2266049403550400299, -2.146007489747939090, 2.055805624768001216 ) ) ;
#6644=CARTESIAN_POINT ( 'NONE',  ( 2.270487904532159984, -0.3622881355932209835, 4.080813552109670894 ) ) ;
#6645=CARTESIAN_POINT ( 'NONE',  ( -2.182690844914350059, -1.680241723982170088, 5.580117243900479806 ) ) ;
#6646=CARTESIAN_POINT ( 'NONE',  ( -2.224278379903029901, -0.5091101694915259879, 5.468825643806110470 ) ) ;
#6647=CARTESIAN_POINT ( 'NONE',  ( -1.217041937262000273, -0.2742238837839080512, 2.666998181419180547 ) ) ;
#6648=CARTESIAN_POINT ( 'NONE',  ( -1.378221871957430178, -5.479872881355929870, 6.607619368096279366 ) ) ;
#6652=CARTESIAN_POINT ( 'NONE',  ( -1.000896394980329340, -5.170974576271190060, 6.829956240957378633 ) ) ;
#6656=CARTESIAN_POINT ( 'NONE',  ( 0.8242394280877100021, -4.428259742000189902, 6.904399023015010073 ) ) ;
#6658=CARTESIAN_POINT ( 'NONE',  ( -2.340070819011249803, -5.519915254237290014, 4.950151441910549899 ) ) ;
#6662=CARTESIAN_POINT ( 'NONE',  ( 0.2365712905368450025, -2.192584066324519743, 2.358466376073659720 ) ) ;
#6665=CARTESIAN_POINT ( 'NONE',  ( -1.823404397755031159, -1.656953435693890864, 5.643450181448764980 ) ) ;
#6667=CARTESIAN_POINT ( 'NONE',  ( 1.248294325655350034, -0.3266949152542379942, 2.704938983774300088 ) ) ;
#6672=CARTESIAN_POINT ( 'NONE',  ( -1.670747221194377685, -5.103620102360557631, 3.047345349617607724 ) ) ;
#6677=CARTESIAN_POINT ( 'NONE',  ( -1.596341326794979976, -5.264406779661020330, 2.970780074643819990 ) ) ;
#6682=CARTESIAN_POINT ( 'NONE',  ( 2.161802606005190253, -0.5895330507925999886, 3.769755311421790545 ) ) ;
#6686=CARTESIAN_POINT ( 'NONE',  ( -2.004091155098381094, -4.963890372630814340, 4.254443623407394348 ) ) ;
#6687=CARTESIAN_POINT ( 'NONE',  ( 0.1765068388402390998, -0.1468220338983061424, 7.347961541693647902 ) ) ;
#6688=CARTESIAN_POINT ( 'NONE',  ( -2.351526912647309953, -0.5269067796610169552, 4.606040641882809261 ) ) ;
#6689=CARTESIAN_POINT ( 'NONE',  ( -2.030998484741458832, -0.5180084745762725262, 4.999543428097190656 ) ) ;
#6691=CARTESIAN_POINT ( 'NONE',  ( 0.4360591020457930123, -0.008898305084746040497, 2.387347919655840034 ) ) ;
#6695=CARTESIAN_POINT ( 'NONE',  ( 2.325590009395039903, -0.7292627805223300674, 5.061077271074019279 ) ) ;
#6696=( NAMED_UNIT ( * ) SI_UNIT ( $, .STERADIAN. ) SOLID_ANGLE_UNIT ( ) );
#6697=CARTESIAN_POINT ( 'NONE',  ( -1.378221871957430178, -5.479872881355929870, 6.607619368096279366 ) ) ;
#6698=CARTESIAN_POINT ( 'NONE',  ( -2.370419177058770366, -1.358046564306109261, 5.893409660608596390 ) ) ;
#6702=CARTESIAN_POINT ( 'NONE',  ( -1.644832646965619816, -4.408812330071869567, 6.383232381746489992 ) ) ;
#6704=CARTESIAN_POINT ( 'NONE',  ( 1.155768864438629695, -4.404971453711897134, 7.088998121597438029 ) ) ;
#6709=CARTESIAN_POINT ( 'NONE',  ( 2.033547680391670998, -0.9583047870452394701, 4.417890669792418734 ) ) ;
#6716=CARTESIAN_POINT ( 'NONE',  ( -2.050059171113549183, -0.2224576271186441134, 4.809263467226075228 ) ) ;
#6717=EDGE_CURVE ( 'NONE', #14300, #14847, #16853, .T. ) ;
#6718=CARTESIAN_POINT ( 'NONE',  ( -1.094547058713670085, -2.755343861603408939, 7.117660114503937763 ) ) ;
#6722=CARTESIAN_POINT ( 'NONE',  ( -1.725722849164588624, -5.197669491525426011, 5.812007984777676661 ) ) ;
#6725=CARTESIAN_POINT ( 'NONE',  ( 2.224278379903029901, -5.390889830508481140, 5.468825643806100700 ) ) ;
#6729=CARTESIAN_POINT ( 'NONE',  ( 2.293398556041700065, -5.364194915254239859, 4.171956209133470317 ) ) ;
#6731=CARTESIAN_POINT ( 'NONE',  ( -2.510208264418979596, -4.525253771513313872, 5.561375738133230939 ) ) ;
#6732=CARTESIAN_POINT ( 'NONE',  ( 1.370891210199511434, -3.869340823081269587, 2.427606771969341715 ) ) ;
#6734=CARTESIAN_POINT ( 'NONE',  ( 0.2220816246932099114, -1.055298816558370101, 6.740975647723836950 ) ) ;
#6742=CARTESIAN_POINT ( 'NONE',  ( 1.716288473737299869, -5.318200384451399643, 2.983711526262690317 ) ) ;
#6743=CARTESIAN_POINT ( 'NONE',  ( -2.293398556041709835, -0.5358050847457630494, 4.171956209133480975 ) ) ;
#6744=CARTESIAN_POINT ( 'NONE',  ( -0.6343239990445920240, -2.099430913171359769, 2.433641963034089972 ) ) ;
#6746=CARTESIAN_POINT ( 'NONE',  ( -1.661700935788390066, -0.4124999999999999778, 3.038299064211610112 ) ) ;
#6747=CARTESIAN_POINT ( 'NONE',  ( 0.5609751937345880402, -5.439830508474575943, 7.293870047334757523 ) ) ;
#6750=CARTESIAN_POINT ( 'NONE',  ( 0.007887181101542477604, -0.3249948581819089855, 2.435887274406100200 ) ) ;
#6756=CARTESIAN_POINT ( 'NONE',  ( 0.8189529353761060282, -3.822764246504690266, 2.493631540942729874 ) ) ;
#6759=CARTESIAN_POINT ( 'NONE',  ( 0.9150601050661639757, -5.430932203389830626, 6.868218666554230190 ) ) ;
#6762=CARTESIAN_POINT ( 'NONE',  ( -2.111627294540180166, -1.889836318576769925, 3.660877362176710559 ) ) ;
#6764=CARTESIAN_POINT ( 'NONE',  ( -1.485788269501199910, -4.829629811528119987, 2.863981322975840182 ) ) ;
#6766=CARTESIAN_POINT ( 'NONE',  ( -1.353302556710470395, -1.563800282540731779, 6.243850391919187892 ) ) ;
#6781=CARTESIAN_POINT ( 'NONE',  ( -0.8570167067220350043, -5.282203389830510076, 2.508190348879359988 ) ) ;
#6786=CARTESIAN_POINT ( 'NONE',  ( -2.111627294540180166, -1.889836318576769925, 3.660877362176710559 ) ) ;
#6787=CARTESIAN_POINT ( 'NONE',  ( -2.578017356471871135, -0.2135593220338991571, 5.329826563567776176 ) ) ;
#6792=CARTESIAN_POINT ( 'NONE',  ( 1.925836318347889931, -0.1112288135593229726, 6.525927015348126581 ) ) ;
#6797=CARTESIAN_POINT ( 'NONE',  ( 0.04278372834676708036, -1.870388906648450478, 2.346934926511239805 ) ) ;
#6799=CARTESIAN_POINT ( 'NONE',  ( -2.318251751302029984, -5.533262711864409766, 4.294764266798999586 ) ) ;
#6800=CARTESIAN_POINT ( 'NONE',  ( 2.437122747866759198, -0.5895330507926000996, 3.649501829874934433 ) ) ;
#6802=CARTESIAN_POINT ( 'NONE',  ( -0.5902886515192680150, -1.447358841099289917, 6.978224088050050788 ) ) ;
#6804=CARTESIAN_POINT ( 'NONE',  ( 1.990095963740240004, -0.7525510688106187285, 5.204400533041760646 ) ) ;
#6805=CARTESIAN_POINT ( 'NONE',  ( 2.328527996529149657, -0.5662447625043111055, 3.426787111016343701 ) ) ;
#6809=CARTESIAN_POINT ( 'NONE',  ( -1.572563554680370679, -4.781424942684484591, 3.380172092915589843 ) ) ;
#6815=CARTESIAN_POINT ( 'NONE',  ( 1.883442729065728960, -2.452596113855660676, 6.569694408006650832 ) ) ;
#6819=CARTESIAN_POINT ( 'NONE',  ( -0.1914205519645679199, -4.981295943764795453, 2.049234377954000319 ) ) ;
#6820=CARTESIAN_POINT ( 'NONE',  ( 1.869504824896970119, -5.395338983050850246, 5.548311746956850143 ) ) ;
#6827=CARTESIAN_POINT ( 'NONE',  ( -0.06367493584607197832, -5.598516949152545941, 2.649999999999998579 ) ) ;
#6828=CARTESIAN_POINT ( 'NONE',  ( 0.1785884594055070773, -4.199217735477280833, 7.347870815423032553 ) ) ;
#6829=CARTESIAN_POINT ( 'NONE',  ( 2.653886076156968699, -4.125511994252439862, 4.698454755023375284 ) ) ;
#6832=CARTESIAN_POINT ( 'NONE',  ( -2.351212046067109984, -4.618406924666470736, 4.597298481426070893 ) ) ;
#6836=CARTESIAN_POINT ( 'NONE',  ( 1.671117483942869963, -5.337498512511849924, 3.028882516057120000 ) ) ;
#6837=CARTESIAN_POINT ( 'NONE',  ( 0.7983658734558030101, -0.4334745762711870176, 6.913847129767330735 ) ) ;
#6838=CARTESIAN_POINT ( 'NONE',  ( -1.669205944673819886, -3.147403886144329643, 6.359065158982450505 ) ) ;
#6841=CARTESIAN_POINT ( 'NONE',  ( -1.347262683220810553, -5.475423728813556323, 6.986424775243341045 ) ) ;
#6845=CARTESIAN_POINT ( 'NONE',  ( 2.058670345754649134, -5.050847457627118509, 3.559656372813920111 ) ) ;
#6849=CARTESIAN_POINT ( 'NONE',  ( -1.781655196750479897, -3.520016498756949996, 3.162323035427820450 ) ) ;
#6851=CARTESIAN_POINT ( 'NONE',  ( 1.487835687536851470, -5.028306595106930565, 2.490167689244129789 ) ) ;
#6854=CARTESIAN_POINT ( 'NONE',  ( 0.8189529353761060282, -3.822764246504690266, 2.493631540942729874 ) ) ;
#6856=CARTESIAN_POINT ( 'NONE',  ( 0.4874850653660255384, -2.891232714973161144, 6.694306935672937442 ) ) ;
#6857=CARTESIAN_POINT ( 'NONE',  ( -0.9150601050661559821, -0.4690677966101700069, 6.868218666554230190 ) ) ;
#6867=CARTESIAN_POINT ( 'NONE',  ( -1.921786527979019166, -5.242161016949150820, 3.977907449687794195 ) ) ;
#6871=CARTESIAN_POINT ( 'NONE',  ( -1.695999708020951013, -5.128627060139315574, 2.646274854235481921 ) ) ;
#6874=CARTESIAN_POINT ( 'NONE',  ( -1.854177340199669954, -1.610376859117309989, 6.149404042554720284 ) ) ;
#6876=CARTESIAN_POINT ( 'NONE',  ( -2.171642826483958899, -0.1957627118644069686, 6.225392547715731695 ) ) ;
#6877=CARTESIAN_POINT ( 'NONE',  ( -1.477796163681079911, -0.4824152542372879826, 6.531563725478150673 ) ) ;
#6881=CARTESIAN_POINT ( 'NONE',  ( -0.9150601050661559821, -0.1690677966101700180, 6.868218666554230190 ) ) ;
#6882=CARTESIAN_POINT ( 'NONE',  ( 1.803891155489780074, -0.8185750573155089471, 3.188470185434109982 ) ) ;
#6885=CARTESIAN_POINT ( 'NONE',  ( -1.687170344131989630, -2.848497014756560919, 6.340793075730589479 ) ) ;
#6886=CARTESIAN_POINT ( 'NONE',  ( -1.347262683220810553, -5.475423728813556323, 6.986424775243341045 ) ) ;
#6888=CARTESIAN_POINT ( 'NONE',  ( -1.710920205120030069, -1.587088570829020107, 6.316012914303580139 ) ) ;
#6890=CARTESIAN_POINT ( 'NONE',  ( 1.503462833636809881, -0.5041426604022095637, 3.304888304972889657 ) ) ;
#6895=CARTESIAN_POINT ( 'NONE',  ( 1.876226141297899774, -0.8884399221803740421, 3.866526959224306115 ) ) ;
#6901=CARTESIAN_POINT ( 'NONE',  ( -1.695509042132779864, -0.2536016949152540834, 3.542446458728619518 ) ) ;
#6902=CARTESIAN_POINT ( 'NONE',  ( 2.479511223993269287, -3.733451969711523155, 3.753882785753661633 ) ) ;
#6905=CARTESIAN_POINT ( 'NONE',  ( -1.882879255550339082, -5.103620102360555855, 2.835213315261639000 ) ) ;
#6906=CARTESIAN_POINT ( 'NONE',  ( -0.8731223871104993872, -5.170974576271189171, 6.558046933601121786 ) ) ;
#6908=CARTESIAN_POINT ( 'NONE',  ( 1.549742865090599997, -0.1156779661016950206, 6.471102547561450535 ) ) ;
#6912=CARTESIAN_POINT ( 'NONE',  ( -0.2189795514005259958, -5.595550847457629651, 2.356806637999020015 ) ) ;
#6913=CARTESIAN_POINT ( 'NONE',  ( -1.032615103526609568, -4.315659176918716255, 7.144753513336388195 ) ) ;
#6914=CARTESIAN_POINT ( 'NONE',  ( 2.642175029090480631, -4.102223705964154199, 4.450952196049445142 ) ) ;
#6916=CARTESIAN_POINT ( 'NONE',  ( -1.936998685628559924, -4.758136654396199816, 3.363294429306559863 ) ) ;
#6921=CARTESIAN_POINT ( 'NONE',  ( -0.4974685680287780354, -0.4601694915254240237, 7.000224381598740386 ) ) ;
#6922=CARTESIAN_POINT ( 'NONE',  ( 2.245209214543399945, -2.635061543801989981, 5.405536158119010004 ) ) ;
#6925=CARTESIAN_POINT ( 'NONE',  ( 2.651721837666119796, -5.073093220338980025, 4.594045830208265180 ) ) ;
#6930=CARTESIAN_POINT ( 'NONE',  ( -0.009452110982655708218, -0.5998079552954630467, 2.350000000000000089 ) ) ;
#6932=CARTESIAN_POINT ( 'NONE',  ( 1.567709126316360058, -3.915917399657849796, 2.944712621036570166 ) ) ;
#6934=CARTESIAN_POINT ( 'NONE',  ( 0.2270348434643680025, -5.304612347394249916, 2.348896311281980065 ) ) ;
#6938=CARTESIAN_POINT ( 'NONE',  ( -0.2564439965878500538, -4.544701183441629766, 7.039440566481220074 ) ) ;
#6940=CARTESIAN_POINT ( 'NONE',  ( -0.7854158957162378218, -3.636457940198391636, 2.803154272645148826 ) ) ;
#6945=CARTESIAN_POINT ( 'NONE',  ( -2.352190863465239978, -4.917313796054239461, 4.622903765856379188 ) ) ;
#6948=B_SPLINE_CURVE_WITH_KNOTS ( 'NONE', 3,
 ( #1781, #2996, #15952, #387, #5941, #11672, #17130, #6027, #15588, #2902, #4533, #17297, #11501, #3252, #8896, #14544 ),
 .UNSPECIFIED., .F., .F.,
 ( 4, 1, 1, 1, 1, 1, 1, 1, 1, 1, 1, 1, 1, 4 ),
 ( 0.4999998212288473409, 0.5105793490763189668, 0.5531463519624459924, 0.5957147871421379914, 0.6382850093031660066, 0.6808567369984199757, 0.7234300338917259987, 0.7660011046591950201, 0.8085801951440879654, 0.8511153557611940146, 0.8935297551198210231, 0.9363130006847799613, 0.9717764100584680431, 1.000000000000000000 ),
 .UNSPECIFIED. ) ;
#6952=CARTESIAN_POINT ( 'NONE',  ( -1.901882987994748975, -5.206567796610170440, 5.472995608211450147 ) ) ;
#6953=CARTESIAN_POINT ( 'NONE',  ( -2.369027826908540302, -1.590929447188999646, 3.503830760997904470 ) ) ;
#6960=CARTESIAN_POINT ( 'NONE',  ( 0.06276132972186961034, -1.377493976234430040, 7.052616990284530374 ) ) ;
#6961=CARTESIAN_POINT ( 'NONE',  ( -0.4874850653659789645, -2.708767285026830951, 6.694306935672950765 ) ) ;
#6962=CARTESIAN_POINT ( 'NONE',  ( 0.3803919826356921829, -0.008898305084746057844, 2.682580100125298461 ) ) ;
#6964=CARTESIAN_POINT ( 'NONE',  ( 0.7983658734558030101, -0.4334745762711870176, 6.913847129767330735 ) ) ;
#6967=CARTESIAN_POINT ( 'NONE',  ( 1.378221871957440170, -0.1201271186440679983, 6.607619368096269596 ) ) ;
#6968=CARTESIAN_POINT ( 'NONE',  ( 1.303621121494459967, -1.237764246504700072, 6.659417683669679455 ) ) ;
#6972=CARTESIAN_POINT ( 'NONE',  ( 1.145304265383909836, -2.522460978720528768, 6.755972720436078660 ) ) ;
#6973=CARTESIAN_POINT ( 'NONE',  ( -0.4221287159901280228, -5.457627118644064801, 7.320050063945812369 ) ) ;
#6977=CARTESIAN_POINT ( 'NONE',  ( 2.151546283159470274, -0.8884399221803740421, 3.746273477677459773 ) ) ;
#6979=CARTESIAN_POINT ( 'NONE',  ( 1.428515267734870031, -0.3311440677966109858, 2.829745655876919841 ) ) ;
#6984=CARTESIAN_POINT ( 'NONE',  ( 1.683529720875211799, -1.144611093351550091, 5.875001924065625936 ) ) ;
#6987=CARTESIAN_POINT ( 'NONE',  ( 0.08231150243515643339, -0.3014830508474583004, 2.050000000000001155 ) ) ;
#6992=CARTESIAN_POINT ( 'NONE',  ( -0.05465110135555984600, -0.1512711864406780515, 6.752241303418941243 ) ) ;
#6995=CARTESIAN_POINT ( 'NONE',  ( 2.091881088960109825, -3.989623140882676555, 6.333140288723826394 ) ) ;
#6997=CARTESIAN_POINT ( 'NONE',  ( -1.314185150718290895, -5.128627060139315574, 3.113044112970123400 ) ) ;
#6998=CARTESIAN_POINT ( 'NONE',  ( -0.5664586606772434862, -5.286652542372874741, 2.726727161522279452 ) ) ;
#7001=CARTESIAN_POINT ( 'NONE',  ( 1.596341326794970206, -0.03559322033898329463, 2.970780074643810664 ) ) ;
#7003=FACE_OUTER_BOUND ( 'NONE', #16438, .T. ) ;
#7005=VERTEX_POINT ( 'NONE', #5887 ) ;
#7008=CARTESIAN_POINT ( 'NONE',  ( 1.914021115237030113, -0.8457042219637709302, 6.069404563272200015 ) ) ;
#7012=CARTESIAN_POINT ( 'NONE',  ( 1.272929729338649674, -0.9155690868286361361, 6.310761232086846917 ) ) ;
#7020=( BOUNDED_SURFACE ( )  B_SPLINE_SURFACE ( 3, 3, ( 
 ( #12211, #16371, #10633, #16281, #9232, #820, #6459, #3676, #17828, #5162, #10813, #3775, #2408, #13697, #1007, #6644, #12299, #16564, #9523, #11087, #2764, #17920, #15182, #2490, #3871, #18181, #5266, #1188, #5535, #7125, #5446, #6837, #8137, #8409, #9607, #16917, #1361, #6921, #5633, #16728, #14045, #10918, #13773, #16827, #11276, #18099, #4226, #2849, #9886, #16651, #15546, #11182, #2670, #1094, #6743, #8323, #1466, #8496, #9700, #12481, #12568, #13958 ),
 ( #12394, #3957, #1278, #4138, #15367, #7021, #18014, #11003, #9796, #14146, #4044, #5361, #15456, #12668, #17694, #15267, #2573, #8226, #13872, #17510, #11974, #8671, #9185, #5804, #15726, #1557, #7287, #4832, #13272, #6312, #672, #2061, #3030, #4494, #3110, #17586, #16232, #75, #10074, #4315, #14848, #6229, #5898, #2951, #158, #4918, #11453, #7202, #1963, #16136, #14748, #17088, #13360, #12844, #12933, #4414, #590, #262, #1640, #10148, #10480, #14238 ),
 ( #11541, #7624, #15804, #9980, #10577, #17174, #5720, #14320, #8762, #11889, #14412, #9085, #8592, #3435, #7716, #3538, #2162, #11366, #12762, #16999, #15645, #18059, #6399, #14940, #16691, #12349, #6792, #3718, #3998, #868, #10770, #2250, #2356, #17971, #8095, #1146, #13826, #15224, #16413, #16514, #9474, #12440, #11041, #13453, #5119, #17690, #9652, #1054, #960, #16324, #13551, #5401, #6507, #7902, #15137, #10964, #9566, #12254, #12166, #2449, #5317, #15321 ),
 ( #3629, #10679, #13736, #6691, #17783, #7804, #3910, #765, #9375, #9280, #2529, #8178, #12068, #5023, #15048, #8004, #2907, #14004, #12615, #4187, #14287, #8552, #12893, #16783, #7171, #2628, #9846, #1320, #6967, #15502, #4097, #9753, #5859, #15418, #2999, #2724, #7251, #8371, #18239, #6881, #8640, #8280, #11235, #16879, #2811, #13920, #212, #1519, #14087, #11505, #12722, #17135, #17045, #4460, #8452, #14199, #1419, #38, #5682, #10117, #12809, #1237 ),
 ( #11327, #16964, #4274, #122, #5770, #4369, #12526, #10030, #18139, #15689, #5487, #11129, #13073, #1691, #3416, #3078, #11585, #6030, #17216, #8721, #9065, #14629, #8901, #13341, #1787, #16118, #10190, #15956, #7431, #16038, #3257, #4629, #13156, #1944, #4538, #13250, #11952, #10289, #2040, #307, #569, #15854, #7344, #4724, #14547, #7511, #12986, #1863, #3337, #17301, #14467, #8982, #391, #14725, #4900, #15770, #6212, #7599, #654, #14366, #11869, #5946 ),
 ( #11677, #17566, #8816, #473, #3160, #6117, #17488, #4808, #7695, #6292, #10457, #11781, #17404, #10374, #4467, #3088, #5497, #15515, #9766, #1703, #11423, #11338, #8380, #5601, #5868, #11246, #12626, #7178, #3007, #1616, #16973, #16889, #4285, #4381, #8731, #15697, #8649, #1330, #12732, #10042, #7356, #18150, #14295, #131, #18251, #9857, #4197, #15605, #2820, #9943, #8563, #10125, #14378, #11140, #8464, #15429, #16795, #17056, #2919, #14015, #14103, #11514 ),
 ( #4108, #7261, #1431, #17145, #14210, #15779, #1530, #2735, #6979, #7089, #49, #5693, #12818, #5780, #12905, #227, #6223, #6304, #6042, #3176, #580, #17416, #10564, #9076, #11962, #8831, #13261, #11688, #4643, #14559, #17575, #11880, #4910, #14480, #17500, #12996, #1874, #17316, #10304, #7522, #1800, #7442, #16222, #13086, #13352, #403, #3529, #15969, #3271, #17227, #665, #318, #8911, #13167, #484, #5957, #9177, #4818, #6129, #14838, #11794, #2152 ) ),
 .UNSPECIFIED., .T., .F., .F. ) 
 B_SPLINE_SURFACE_WITH_KNOTS ( ( 4, 3, 4 ),
 ( 4, 1, 1, 1, 1, 1, 1, 1, 1, 1, 1, 1, 1, 1, 1, 1, 1, 1, 1, 1, 1, 1, 1, 1, 1, 1, 1, 1, 1, 1, 1, 1, 1, 1, 1, 1, 1, 1, 1, 1, 1, 1, 1, 1, 1, 1, 1, 1, 1, 1, 1, 1, 1, 1, 1, 1, 1, 1, 1, 4 ),
 ( 0.000000000000000000, 3.141592653589790007, 6.283185307179590673 ),
 ( 0.000000000000000000, 0.09318283294545999518, 0.1863656658909199904, 0.2795484988363799994, 0.3727313317818399807, 0.4659141647273000175, 0.5590969976727599988, 0.6522798306182200356, 0.7454626635636799614, 0.8386454965091399982, 0.9318283294545990358, 1.025011162400059961, 1.118193995345519998, 1.211376828290979812, 1.304559661236440071, 1.397742494181900108, 1.490925327127359923, 1.584108160072819960, 1.677290993018279996, 1.770473825963740033, 1.863656658909200070, 1.956839491854659885, 2.050022324800119922, 2.143205157745580181, 2.236387990691039995, 2.329570823636499810, 2.422753656581960069, 2.515936489527420328, 2.609119322472880143, 2.702302155418339957, 2.795484988363799772, 2.888667821309260031, 2.981850654254720290, 3.075033487200180105, 3.168216320145639919, 3.261399153091099734, 3.354581986036559993, 3.447764818982019808, 3.540947651927480067, 3.634130484872939881, 3.727313317818400140, 3.820496150763859955, 3.913678983709319770, 4.006861816654780029, 4.100044649600239843, 4.193227482545699658, 4.286410315491160361, 4.379593148436620176, 4.472775981382079991, 4.565958814327539805, 4.659141647272999620, 4.752324480218450553, 4.845507313163910368, 4.938690146109370183, 5.031872979054829997, 5.125055812000289812, 5.218238644945749627, 5.311421477891210330, 5.404604310836670145, 5.497787143782139729 ),
 .UNSPECIFIED. ) 
 GEOMETRIC_REPRESENTATION_ITEM ( )  RATIONAL_B_SPLINE_SURFACE ( (
 ( 1.000000000000000000, 1.000000000000000000, 1.000000000000000000, 1.000000000000000000, 1.000000000000000000, 1.000000000000000000, 1.000000000000000000, 1.000000000000000000, 1.000000000000000000, 1.000000000000000000, 1.000000000000000000, 1.000000000000000000, 1.000000000000000000, 1.000000000000000000, 1.000000000000000000, 1.000000000000000000, 1.000000000000000000, 1.000000000000000000, 1.000000000000000000, 1.000000000000000000, 1.000000000000000000, 1.000000000000000000, 1.000000000000000000, 1.000000000000000000, 1.000000000000000000, 1.000000000000000000, 1.000000000000000000, 1.000000000000000000, 1.000000000000000000, 1.000000000000000000, 1.000000000000000000, 1.000000000000000000, 1.000000000000000000, 1.000000000000000000, 1.000000000000000000, 1.000000000000000000, 1.000000000000000000, 1.000000000000000000, 1.000000000000000000, 1.000000000000000000, 1.000000000000000000, 1.000000000000000000, 1.000000000000000000, 1.000000000000000000, 1.000000000000000000, 1.000000000000000000, 1.000000000000000000, 1.000000000000000000, 1.000000000000000000, 1.000000000000000000, 1.000000000000000000, 1.000000000000000000, 1.000000000000000000, 1.000000000000000000, 1.000000000000000000, 1.000000000000000000, 1.000000000000000000, 1.000000000000000000, 1.000000000000000000, 1.000000000000000000, 1.000000000000000000, 1.000000000000000000),
 ( 0.3333333333333329818, 0.3333333333333329818, 0.3333333333333329818, 0.3333333333333329818, 0.3333333333333329818, 0.3333333333333329818, 0.3333333333333329818, 0.3333333333333329818, 0.3333333333333329818, 0.3333333333333329818, 0.3333333333333329818, 0.3333333333333329818, 0.3333333333333329818, 0.3333333333333329818, 0.3333333333333329818, 0.3333333333333329818, 0.3333333333333329818, 0.3333333333333329818, 0.3333333333333329818, 0.3333333333333329818, 0.3333333333333329818, 0.3333333333333329818, 0.3333333333333329818, 0.3333333333333329818, 0.3333333333333329818, 0.3333333333333329818, 0.3333333333333329818, 0.3333333333333329818, 0.3333333333333329818, 0.3333333333333329818, 0.3333333333333329818, 0.3333333333333329818, 0.3333333333333329818, 0.3333333333333329818, 0.3333333333333329818, 0.3333333333333329818, 0.3333333333333329818, 0.3333333333333329818, 0.3333333333333329818, 0.3333333333333329818, 0.3333333333333329818, 0.3333333333333329818, 0.3333333333333329818, 0.3333333333333329818, 0.3333333333333329818, 0.3333333333333329818, 0.3333333333333329818, 0.3333333333333329818, 0.3333333333333329818, 0.3333333333333329818, 0.3333333333333329818, 0.3333333333333329818, 0.3333333333333329818, 0.3333333333333329818, 0.3333333333333329818, 0.3333333333333329818, 0.3333333333333329818, 0.3333333333333329818, 0.3333333333333329818, 0.3333333333333329818, 0.3333333333333329818, 0.3333333333333329818),
 ( 0.3333333333333329818, 0.3333333333333329818, 0.3333333333333329818, 0.3333333333333329818, 0.3333333333333329818, 0.3333333333333329818, 0.3333333333333329818, 0.3333333333333329818, 0.3333333333333329818, 0.3333333333333329818, 0.3333333333333329818, 0.3333333333333329818, 0.3333333333333329818, 0.3333333333333329818, 0.3333333333333329818, 0.3333333333333329818, 0.3333333333333329818, 0.3333333333333329818, 0.3333333333333329818, 0.3333333333333329818, 0.3333333333333329818, 0.3333333333333329818, 0.3333333333333329818, 0.3333333333333329818, 0.3333333333333329818, 0.3333333333333329818, 0.3333333333333329818, 0.3333333333333329818, 0.3333333333333329818, 0.3333333333333329818, 0.3333333333333329818, 0.3333333333333329818, 0.3333333333333329818, 0.3333333333333329818, 0.3333333333333329818, 0.3333333333333329818, 0.3333333333333329818, 0.3333333333333329818, 0.3333333333333329818, 0.3333333333333329818, 0.3333333333333329818, 0.3333333333333329818, 0.3333333333333329818, 0.3333333333333329818, 0.3333333333333329818, 0.3333333333333329818, 0.3333333333333329818, 0.3333333333333329818, 0.3333333333333329818, 0.3333333333333329818, 0.3333333333333329818, 0.3333333333333329818, 0.3333333333333329818, 0.3333333333333329818, 0.3333333333333329818, 0.3333333333333329818, 0.3333333333333329818, 0.3333333333333329818, 0.3333333333333329818, 0.3333333333333329818, 0.3333333333333329818, 0.3333333333333329818),
 ( 1.000000000000000000, 1.000000000000000000, 1.000000000000000000, 1.000000000000000000, 1.000000000000000000, 1.000000000000000000, 1.000000000000000000, 1.000000000000000000, 1.000000000000000000, 1.000000000000000000, 1.000000000000000000, 1.000000000000000000, 1.000000000000000000, 1.000000000000000000, 1.000000000000000000, 1.000000000000000000, 1.000000000000000000, 1.000000000000000000, 1.000000000000000000, 1.000000000000000000, 1.000000000000000000, 1.000000000000000000, 1.000000000000000000, 1.000000000000000000, 1.000000000000000000, 1.000000000000000000, 1.000000000000000000, 1.000000000000000000, 1.000000000000000000, 1.000000000000000000, 1.000000000000000000, 1.000000000000000000, 1.000000000000000000, 1.000000000000000000, 1.000000000000000000, 1.000000000000000000, 1.000000000000000000, 1.000000000000000000, 1.000000000000000000, 1.000000000000000000, 1.000000000000000000, 1.000000000000000000, 1.000000000000000000, 1.000000000000000000, 1.000000000000000000, 1.000000000000000000, 1.000000000000000000, 1.000000000000000000, 1.000000000000000000, 1.000000000000000000, 1.000000000000000000, 1.000000000000000000, 1.000000000000000000, 1.000000000000000000, 1.000000000000000000, 1.000000000000000000, 1.000000000000000000, 1.000000000000000000, 1.000000000000000000, 1.000000000000000000, 1.000000000000000000, 1.000000000000000000),
 ( 0.3333333333333329818, 0.3333333333333329818, 0.3333333333333329818, 0.3333333333333329818, 0.3333333333333329818, 0.3333333333333329818, 0.3333333333333329818, 0.3333333333333329818, 0.3333333333333329818, 0.3333333333333329818, 0.3333333333333329818, 0.3333333333333329818, 0.3333333333333329818, 0.3333333333333329818, 0.3333333333333329818, 0.3333333333333329818, 0.3333333333333329818, 0.3333333333333329818, 0.3333333333333329818, 0.3333333333333329818, 0.3333333333333329818, 0.3333333333333329818, 0.3333333333333329818, 0.3333333333333329818, 0.3333333333333329818, 0.3333333333333329818, 0.3333333333333329818, 0.3333333333333329818, 0.3333333333333329818, 0.3333333333333329818, 0.3333333333333329818, 0.3333333333333329818, 0.3333333333333329818, 0.3333333333333329818, 0.3333333333333329818, 0.3333333333333329818, 0.3333333333333329818, 0.3333333333333329818, 0.3333333333333329818, 0.3333333333333329818, 0.3333333333333329818, 0.3333333333333329818, 0.3333333333333329818, 0.3333333333333329818, 0.3333333333333329818, 0.3333333333333329818, 0.3333333333333329818, 0.3333333333333329818, 0.3333333333333329818, 0.3333333333333329818, 0.3333333333333329818, 0.3333333333333329818, 0.3333333333333329818, 0.3333333333333329818, 0.3333333333333329818, 0.3333333333333329818, 0.3333333333333329818, 0.3333333333333329818, 0.3333333333333329818, 0.3333333333333329818, 0.3333333333333329818, 0.3333333333333329818),
 ( 0.3333333333333329818, 0.3333333333333329818, 0.3333333333333329818, 0.3333333333333329818, 0.3333333333333329818, 0.3333333333333329818, 0.3333333333333329818, 0.3333333333333329818, 0.3333333333333329818, 0.3333333333333329818, 0.3333333333333329818, 0.3333333333333329818, 0.3333333333333329818, 0.3333333333333329818, 0.3333333333333329818, 0.3333333333333329818, 0.3333333333333329818, 0.3333333333333329818, 0.3333333333333329818, 0.3333333333333329818, 0.3333333333333329818, 0.3333333333333329818, 0.3333333333333329818, 0.3333333333333329818, 0.3333333333333329818, 0.3333333333333329818, 0.3333333333333329818, 0.3333333333333329818, 0.3333333333333329818, 0.3333333333333329818, 0.3333333333333329818, 0.3333333333333329818, 0.3333333333333329818, 0.3333333333333329818, 0.3333333333333329818, 0.3333333333333329818, 0.3333333333333329818, 0.3333333333333329818, 0.3333333333333329818, 0.3333333333333329818, 0.3333333333333329818, 0.3333333333333329818, 0.3333333333333329818, 0.3333333333333329818, 0.3333333333333329818, 0.3333333333333329818, 0.3333333333333329818, 0.3333333333333329818, 0.3333333333333329818, 0.3333333333333329818, 0.3333333333333329818, 0.3333333333333329818, 0.3333333333333329818, 0.3333333333333329818, 0.3333333333333329818, 0.3333333333333329818, 0.3333333333333329818, 0.3333333333333329818, 0.3333333333333329818, 0.3333333333333329818, 0.3333333333333329818, 0.3333333333333329818),
 ( 1.000000000000000000, 1.000000000000000000, 1.000000000000000000, 1.000000000000000000, 1.000000000000000000, 1.000000000000000000, 1.000000000000000000, 1.000000000000000000, 1.000000000000000000, 1.000000000000000000, 1.000000000000000000, 1.000000000000000000, 1.000000000000000000, 1.000000000000000000, 1.000000000000000000, 1.000000000000000000, 1.000000000000000000, 1.000000000000000000, 1.000000000000000000, 1.000000000000000000, 1.000000000000000000, 1.000000000000000000, 1.000000000000000000, 1.000000000000000000, 1.000000000000000000, 1.000000000000000000, 1.000000000000000000, 1.000000000000000000, 1.000000000000000000, 1.000000000000000000, 1.000000000000000000, 1.000000000000000000, 1.000000000000000000, 1.000000000000000000, 1.000000000000000000, 1.000000000000000000, 1.000000000000000000, 1.000000000000000000, 1.000000000000000000, 1.000000000000000000, 1.000000000000000000, 1.000000000000000000, 1.000000000000000000, 1.000000000000000000, 1.000000000000000000, 1.000000000000000000, 1.000000000000000000, 1.000000000000000000, 1.000000000000000000, 1.000000000000000000, 1.000000000000000000, 1.000000000000000000, 1.000000000000000000, 1.000000000000000000, 1.000000000000000000, 1.000000000000000000, 1.000000000000000000, 1.000000000000000000, 1.000000000000000000, 1.000000000000000000, 1.000000000000000000, 1.000000000000000000) ) ) 
 REPRESENTATION_ITEM ( '' )  SURFACE ( )  );
#7021=CARTESIAN_POINT ( 'NONE',  ( 0.9664230948141925293, -0.3177966101694921219, 2.228384861502251457 ) ) ;
#7022=CARTESIAN_POINT ( 'NONE',  ( 2.169623098572349917, -2.658349832090280529, 5.611855963200990338 ) ) ;
#7025=CARTESIAN_POINT ( 'NONE',  ( 2.171642826483958899, -5.104237288135595740, 6.225392547715717484 ) ) ;
#7030=CARTESIAN_POINT ( 'NONE',  ( -2.116444151961479392, -5.246610169491528808, 3.670839500609360151 ) ) ;
#7037=CARTESIAN_POINT ( 'NONE',  ( -2.352190863465239978, -4.917313796054239461, 4.622903765856379188 ) ) ;
#7040=CARTESIAN_POINT ( 'NONE',  ( 1.534924416212170017, -5.333856471232000018, 2.911460733964629899 ) ) ;
#7042=CARTESIAN_POINT ( 'NONE',  ( 2.352190863465239978, -0.6826862039457530784, 4.622903765856330338 ) ) ;
#7045=CARTESIAN_POINT ( 'NONE',  ( 0.3949552299394610277, -3.776187669928119828, 2.379923265530350385 ) ) ;
#7048=CARTESIAN_POINT ( 'NONE',  ( -1.454969160281959661, -3.147403886144331420, 6.148435909958226198 ) ) ;
#7051=CARTESIAN_POINT ( 'NONE',  ( 1.428515267734870031, -0.3311440677966109858, 2.829745655876919841 ) ) ;
#7054=CARTESIAN_POINT ( 'NONE',  ( -0.8244235255442939891, -0.5829339996946389935, 2.492493020344019872 ) ) ;
#7061=ADVANCED_FACE ( 'NONE', ( #7003 ), #14578, .T. ) ;
#7065=CARTESIAN_POINT ( 'NONE',  ( -0.3265524029357583236, -5.157627118644064979, 6.726831181542982208 ) ) ;
#7072=CARTESIAN_POINT ( 'NONE',  ( 1.074829861819710075, -2.285737219477669946, 2.606322265575589991 ) ) ;
#7073=CARTESIAN_POINT ( 'NONE',  ( 1.385380178477290558, -3.617010528270069525, 3.184868453331423765 ) ) ;
#7074=CARTESIAN_POINT ( 'NONE',  ( 1.965557623688110933, -0.08898305084745804228, 5.292675575926325315 ) ) ;
#7079=CARTESIAN_POINT ( 'NONE',  ( -2.255259958075430227, -1.703530012270459970, 5.372717034856060003 ) ) ;
#7083=CARTESIAN_POINT ( 'NONE',  ( -1.866416942370659804, -1.637506023765569640, 3.266391446483499106 ) ) ;
#7085=CARTESIAN_POINT ( 'NONE',  ( 0.5609751937345880402, -5.439830508474575943, 7.293870047334757523 ) ) ;
#7087=( GEOMETRIC_REPRESENTATION_CONTEXT ( 3 ) GLOBAL_UNCERTAINTY_ASSIGNED_CONTEXT ( ( #12703 ) ) GLOBAL_UNIT_ASSIGNED_CONTEXT ( ( #9480, #14011, #6696 ) ) REPRESENTATION_CONTEXT ( 'NONE', 'WORKASPACE' ) );
#7088=CARTESIAN_POINT ( 'NONE',  ( 2.053221424930760097, -0.8651516338920849369, 3.549770689668250157 ) ) ;
#7089=CARTESIAN_POINT ( 'NONE',  ( 1.596341326794969984, -0.3355932203389830337, 2.970780074643809776 ) ) ;
#7090=ADVANCED_FACE ( 'NONE', ( #5215 ), #12103, .T. ) ;
#7096=CARTESIAN_POINT ( 'NONE',  ( -1.698651900122509995, -3.193980462720909408, 5.853032334688971439 ) ) ;
#7098=CARTESIAN_POINT ( 'NONE',  ( 1.407651048079441525, -0.3266949152542383272, 2.450250343405061759 ) ) ;
#7102=CARTESIAN_POINT ( 'NONE',  ( -0.05465110135555984600, -0.4512711864406789841, 6.752241303418941243 ) ) ;
#7106=CARTESIAN_POINT ( 'NONE',  ( -0.5027094486773525661, -4.952022267818764867, 2.083735201298030137 ) ) ;
#7107=CARTESIAN_POINT ( 'NONE',  ( 1.943632316591230147, -5.346398305084740343, 3.373048379518159834 ) ) ;
#7109=CARTESIAN_POINT ( 'NONE',  ( 0.4360591020457930123, -0.008898305084746038762, 2.387347919655840034 ) ) ;
#7114=CARTESIAN_POINT ( 'NONE',  ( -1.991984774470509922, -1.614217735477279980, 3.446707398186049875 ) ) ;
#7116=CARTESIAN_POINT ( 'NONE',  ( 1.549925137359331462, -0.8689925102520592581, 6.046340934239826659 ) ) ;
#7124=CARTESIAN_POINT ( 'NONE',  ( 1.710144332342950158, -5.052039382343889606, 2.989855667657050020 ) ) ;
#7125=CARTESIAN_POINT ( 'NONE',  ( 1.194742379459969861, -0.4245762711864409789, 6.727584234649759409 ) ) ;
#7127=CARTESIAN_POINT ( 'NONE',  ( 2.075124426334590044, -2.681638120378570189, 5.810227140144509583 ) ) ;
#7131=CARTESIAN_POINT ( 'NONE',  ( 2.431060148753489081, -5.055296610169490279, 3.635668498923322112 ) ) ;
#7138=CARTESIAN_POINT ( 'NONE',  ( 0.3162622016569809347, -1.354205687946139491, 7.334974746141788238 ) ) ;
#7139=CARTESIAN_POINT ( 'NONE',  ( 0.5803392541454069908, -5.011796459788059543, 2.403119802722879950 ) ) ;
#7141=CARTESIAN_POINT ( 'NONE',  ( 1.914021115237030113, -0.8457042219637709302, 6.069404563272200015 ) ) ;
#7144=CARTESIAN_POINT ( 'NONE',  ( 2.260890494820590124, -4.055647129387580208, 4.046455925041149371 ) ) ;
#7146=CARTESIAN_POINT ( 'NONE',  ( -0.6050872056802790722, -3.659746228486683073, 2.738171435586149727 ) ) ;
#7151=CARTESIAN_POINT ( 'NONE',  ( -0.4617942143426889690, -0.5906145504024210569, 2.383143958488499692 ) ) ;
#7152=ORIENTED_EDGE ( 'NONE', *, *, #13307, .T. ) ;
#7157=CARTESIAN_POINT ( 'NONE',  ( 1.940327948426050941, -5.090889830508485758, 5.370677689277660427 ) ) ;
#7161=CARTESIAN_POINT ( 'NONE',  ( -1.229686204202100175, -5.164643153926309793, 2.674737924334550154 ) ) ;
#7164=CARTESIAN_POINT ( 'NONE',  ( 2.245209214543399945, -2.635061543801989981, 5.405536158119010004 ) ) ;
#7165=CARTESIAN_POINT ( 'NONE',  ( 0.9123513484651973870, -3.547145663405211646, 2.860838000723751051 ) ) ;
#7166=CARTESIAN_POINT ( 'NONE',  ( 1.725722849164588624, -0.1023305084745770588, 5.812007984777676661 ) ) ;
#7171=CARTESIAN_POINT ( 'NONE',  ( 1.978267656359410154, -0.1023305084745769894, 5.974740860598790171 ) ) ;
#7172=CARTESIAN_POINT ( 'NONE',  ( -2.353343516942199898, -1.773394877135329839, 4.722803042560189901 ) ) ;
#7173=ORIENTED_EDGE ( 'NONE', *, *, #874, .F. ) ;
#7175=CARTESIAN_POINT ( 'NONE',  ( 1.332058588847409686, -2.499172690432239108, 6.640197310420187904 ) ) ;
#7176=CARTESIAN_POINT ( 'NONE',  ( -2.614198783383141045, -5.533262711864405325, 4.243032045539295360 ) ) ;
#7178=CARTESIAN_POINT ( 'NONE',  ( 1.351903350398191206, -0.4156779661016956062, 6.245004350000406212 ) ) ;
#7183=CARTESIAN_POINT ( 'NONE',  ( -0.08304008649493913041, -2.961097579838030569, 6.751342532748503267 ) ) ;
#7184=CARTESIAN_POINT ( 'NONE',  ( 1.925836318347889931, -0.4112288135593234473, 6.525927015348126581 ) ) ;
#7186=CARTESIAN_POINT ( 'NONE',  ( -0.009452110982656868748, -5.299807955295460005, 2.350000000000000089 ) ) ;
#7190=CARTESIAN_POINT ( 'NONE',  ( -1.526871680339578541, -5.559957627118640389, 3.327650196883449762 ) ) ;
#7193=CARTESIAN_POINT ( 'NONE',  ( 0.7093417302541469294, -5.435381355932199732, 6.943956659919690466 ) ) ;
#7196=CARTESIAN_POINT ( 'NONE',  ( -2.343457872958619959, -1.451199717459269900, 4.916681529328609912 ) ) ;
#7198=CARTESIAN_POINT ( 'NONE',  ( -0.2993653819235400082, -2.685478996738538626, 6.731079075450757898 ) ) ;
#7201=CARTESIAN_POINT ( 'NONE',  ( 0.5637478356992829953, -0.6606104644819250638, 2.398845082743519708 ) ) ;
#7202=CARTESIAN_POINT ( 'NONE',  ( -2.416676968769249090, -0.5046610169491535514, 5.796598111919839980 ) ) ;
#7203=CARTESIAN_POINT ( 'NONE',  ( 1.397172971746949877, -3.892629111369559691, 2.806153814454899642 ) ) ;
#7206=CARTESIAN_POINT ( 'NONE',  ( 1.811729841638690219, -5.041949152542369639, 3.197954009834290012 ) ) ;
#7212=CARTESIAN_POINT ( 'NONE',  ( -1.820241257191459905, -5.080331814072259533, 3.208199930689799917 ) ) ;
#7214=CARTESIAN_POINT ( 'NONE',  ( 1.440522616026430391, -0.7952867690272208412, 3.241384813161591438 ) ) ;
#7218=CARTESIAN_POINT ( 'NONE',  ( -2.352760675243210198, -3.034803321062869763, 4.757121734156080528 ) ) ;
#7221=CARTESIAN_POINT ( 'NONE',  ( 1.397172971746949877, -3.892629111369559691, 2.806153814454899642 ) ) ;
#7223=CARTESIAN_POINT ( 'NONE',  ( 1.974086094277279768, -4.195376859117311064, 5.263813741415705572 ) ) ;
#7234=CARTESIAN_POINT ( 'NONE',  ( -0.5664586606772434862, -5.586652542372875452, 2.726727161522279452 ) ) ;
#7235=CARTESIAN_POINT ( 'NONE',  ( 2.649291707874080970, -2.243001519261071053, 4.543900225523779035 ) ) ;
#7241=CARTESIAN_POINT ( 'NONE',  ( -0.1881942810071039751, -5.280843314568230085, 2.350674491507239949 ) ) ;
#7244=CARTESIAN_POINT ( 'NONE',  ( 1.526791597786429922, -2.774791273531720392, 6.490992212270249695 ) ) ;
#7246=CARTESIAN_POINT ( 'NONE',  ( -1.102492180652080211, -3.290974492234041815, 2.968118700883599193 ) ) ;
#7247=CARTESIAN_POINT ( 'NONE',  ( 0.7476103186298468373, -0.01779661016949178609, 2.787995836256459636 ) ) ;
#7251=CARTESIAN_POINT ( 'NONE',  ( -0.2812789908084309953, -0.1557203389830509876, 7.036533610117280624 ) ) ;
#7252=CARTESIAN_POINT ( 'NONE',  ( 0.6673090596498160165, -2.239160642901090181, 2.443133963569570355 ) ) ;
#7256=CARTESIAN_POINT ( 'NONE',  ( -2.023259452208838738, -3.174533050792599731, 3.497849062500261397 ) ) ;
#7258=CARTESIAN_POINT ( 'NONE',  ( 2.630358833876468960, -5.368644067796615182, 4.347767980622404771 ) ) ;
#7261=CARTESIAN_POINT ( 'NONE',  ( 0.07299321914061039640, -0.3014830508474579673, 2.350000000000000089 ) ) ;
#7265=CARTESIAN_POINT ( 'NONE',  ( -1.520647680314179517, -1.959701183441630024, 3.320676805464663151 ) ) ;
#7269=CARTESIAN_POINT ( 'NONE',  ( 1.725722849164588624, -0.4023305084745772420, 5.812007984777676661 ) ) ;
#7275=CARTESIAN_POINT ( 'NONE',  ( -1.791574935211209363, -0.1913135593220340047, 6.226029630577610163 ) ) ;
#7280=CARTESIAN_POINT ( 'NONE',  ( -1.994983296312370147, -1.334758276017820045, 5.948514050749340143 ) ) ;
#7281=CARTESIAN_POINT ( 'NONE',  ( 1.583713126240741564, -2.429307825567371459, 6.006428174987391344 ) ) ;
#7287=CARTESIAN_POINT ( 'NONE',  ( 1.925836318347889931, -0.4112288135593234473, 6.525927015348126581 ) ) ;
#7288=CARTESIAN_POINT ( 'NONE',  ( 2.192143888961729736, -4.218665147405599392, 5.556300681753580051 ) ) ;
#7291=CARTESIAN_POINT ( 'NONE',  ( 1.666450993087180477, -5.117584745762705722, 6.765380371283858274 ) ) ;
#7299=CARTESIAN_POINT ( 'NONE',  ( 1.652654650382400003, -0.7952867690272209522, 3.029252778805620050 ) ) ;
#7301=CARTESIAN_POINT ( 'NONE',  ( 2.159566522375460096, -2.359442960702510028, 5.635424033751039730 ) ) ;
#7304=CARTESIAN_POINT ( 'NONE',  ( 0.2134934900267039248, -5.004947479095229745, 2.650814970067049803 ) ) ;
#7305=CARTESIAN_POINT ( 'NONE',  ( -1.558664967382870525, -1.540511994252448780, 6.847947208954447973 ) ) ;
#7306=CARTESIAN_POINT ( 'NONE',  ( 1.438959988998139914E-16, -0.1499999999999999944, 2.350000000000000089 ) ) ;
#7307=CARTESIAN_POINT ( 'NONE',  ( -2.004091155098381094, -4.963890372630814340, 4.254443623407394348 ) ) ;
#7309=CARTESIAN_POINT ( 'NONE',  ( -1.791574935211209807, -0.4913135593220339659, 6.226029630577610163 ) ) ;
#7312=CARTESIAN_POINT ( 'NONE',  ( 2.203023580853990193, -0.3578389830508479919, 3.872235369154280349 ) ) ;
#7322=CARTESIAN_POINT ( 'NONE',  ( -2.046424002475610404, -5.528813559322025561, 4.536201610417774255 ) ) ;
#7324=CARTESIAN_POINT ( 'NONE',  ( -2.282375681463830297, -3.174533050792599731, 3.345793611865449435 ) ) ;
#7326=CARTESIAN_POINT ( 'NONE',  ( -0.009452110982656868748, -5.299807955295460005, 2.350000000000000089 ) ) ;
#7331=CARTESIAN_POINT ( 'NONE',  ( -2.334032080503389839, -3.310421904162350160, 5.001728246382240783 ) ) ;
#7333=CARTESIAN_POINT ( 'NONE',  ( 1.440522616026430391, -0.7952867690272208412, 3.241384813161591438 ) ) ;
#7335=CARTESIAN_POINT ( 'NONE',  ( -2.058670345754650022, -0.2491525423728820077, 3.559656372813929881 ) ) ;
#7341=CARTESIAN_POINT ( 'NONE',  ( 1.788074174585509768, -3.617010528270069525, 2.738902236199779239 ) ) ;
#7344=CARTESIAN_POINT ( 'NONE',  ( -1.289141334274979789, -0.1824152542372889096, 6.297747079672432413 ) ) ;
#7345=CARTESIAN_POINT ( 'NONE',  ( 2.211317922628870392, -2.472043525783979678, 3.894507149290419967 ) ) ;
#7348=ORIENTED_EDGE ( 'NONE', *, *, #653, .F. ) ;
#7349=CARTESIAN_POINT ( 'NONE',  ( -0.01716182025094739605, -3.430704221963769562, 2.346608583467349796 ) ) ;
#7351=CARTESIAN_POINT ( 'NONE',  ( -1.128670402850159737, -5.170974576271189171, 7.101865548313641696 ) ) ;
#7356=CARTESIAN_POINT ( 'NONE',  ( -0.9707742057416274273, -0.4735169491525429986, 6.508944043303927174 ) ) ;
#7360=CARTESIAN_POINT ( 'NONE',  ( 1.959085573314239159, -2.635061543801990869, 5.313910057793555630 ) ) ;
#7362=CARTESIAN_POINT ( 'NONE',  ( 2.268288188848061715, -0.3489406779661023417, 3.322421079292310786 ) ) ;
#7369=CARTESIAN_POINT ( 'NONE',  ( 1.661700935788380074, -5.337500000000000355, 3.038299064211610112 ) ) ;
#7370=ORIENTED_EDGE ( 'NONE', *, *, #11743, .F. ) ;
#7371=CARTESIAN_POINT ( 'NONE',  ( -0.6964468257805866980, -5.466525423728811006, 6.631228347243847132 ) ) ;
#7373=CARTESIAN_POINT ( 'NONE',  ( -1.713314936023349722, -0.2610169491525430319, 3.089913064446579760 ) ) ;
#7374=CARTESIAN_POINT ( 'NONE',  ( -1.449568901432419343, -0.5625000000000005551, 3.250431098567584165 ) ) ;
#7375=CARTESIAN_POINT ( 'NONE',  ( 2.607432201095279733, -4.078935417675873865, 4.205620581240154365 ) ) ;
#7379=CARTESIAN_POINT ( 'NONE',  ( 1.781655196750449921, -2.079983501243049648, 3.162323035427780482 ) ) ;
#7381=CARTESIAN_POINT ( 'NONE',  ( -1.712910428781911021, -2.895073591333140239, 5.831741890007735130 ) ) ;
#7388=CARTESIAN_POINT ( 'NONE',  ( -2.349129089426440054, -4.894025507765950245, 4.842612091679129982 ) ) ;
#7391=CARTESIAN_POINT ( 'NONE',  ( 0.3171869470818560743, -5.144279661016955885, 7.334814496515233095 ) ) ;
#7398=CARTESIAN_POINT ( 'NONE',  ( 2.035218756299218779, -0.8185750573155082810, 2.996768277952650106 ) ) ;
#7399=CARTESIAN_POINT ( 'NONE',  ( 1.670747221194369914, -0.4963798976394459550, 3.047345349617600174 ) ) ;
#7402=CARTESIAN_POINT ( 'NONE',  ( 0.3159454637157339540, -2.615614131873679860, 7.032150113402090064 ) ) ;
#7403=FACE_OUTER_BOUND ( 'NONE', #5681, .T. ) ;
#7404=CARTESIAN_POINT ( 'NONE',  ( 2.584100759211419795, -0.9350164987569505870, 4.095403473953104445 ) ) ;
#7415=CARTESIAN_POINT ( 'NONE',  ( -0.3803919826357066158, -5.291101694915254505, 2.682580100125310896 ) ) ;
#7417=CARTESIAN_POINT ( 'NONE',  ( -2.340959815966380031, -1.750106588847040179, 4.942183458383479611 ) ) ;
#7418=CARTESIAN_POINT ( 'NONE',  ( 0.2266049403549809660, -3.453992510252061887, 2.055805624767989226 ) ) ;
#7420=CARTESIAN_POINT ( 'NONE',  ( 1.661700935788380074, -5.337500000000000355, 3.038299064211610112 ) ) ;
#7422=CARTESIAN_POINT ( 'NONE',  ( 2.226511124464869873, -1.074746228486680000, 5.462491901673799610 ) ) ;
#7425=CARTESIAN_POINT ( 'NONE',  ( 2.337178851518220135, -2.588484967225419986, 4.976298214796759822 ) ) ;
#7426=CARTESIAN_POINT ( 'NONE',  ( -1.566607907718199577, -4.432100618360157007, 6.026891670824300107 ) ) ;
#7429=ORIENTED_EDGE ( 'NONE', *, *, #12538, .T. ) ;
#7430=CARTESIAN_POINT ( 'NONE',  ( 2.639965200365849363, -3.849893411152959910, 4.971472712918224346 ) ) ;
#7431=CARTESIAN_POINT ( 'NONE',  ( 1.202278654260740876, -0.1201271186440679706, 6.364093491318035589 ) ) ;
#7432=CARTESIAN_POINT ( 'NONE',  ( 2.276802572547980130, -2.495331814072260013, 4.104251954998760610 ) ) ;
#7437=CARTESIAN_POINT ( 'NONE',  ( 0.2023972492402060508, -3.453992510252061443, 2.355265251465770149 ) ) ;
#7439=CARTESIAN_POINT ( 'NONE',  ( -1.192209327851089240, -5.577754237288145234, 2.329031440774910422 ) ) ;
#7442=CARTESIAN_POINT ( 'NONE',  ( -1.300961508564169922, -0.4779661016949160457, 6.661123742937279602 ) ) ;
#7448=CARTESIAN_POINT ( 'NONE',  ( 0.5805547688318586363, -2.239160642901089293, 2.730772231808960449 ) ) ;
#7450=CARTESIAN_POINT ( 'NONE',  ( 2.268288188848061715, -0.04894067796610205440, 3.322421079292310786 ) ) ;
#7453=CARTESIAN_POINT ( 'NONE',  ( 1.438959988998139914E-16, -0.1499999999999999944, 2.350000000000000089 ) ) ;
#7454=CARTESIAN_POINT ( 'NONE',  ( 0.6964468257805941365, -0.4334745762711874617, 6.631228347243847132 ) ) ;
#7457=CARTESIAN_POINT ( 'NONE',  ( 0.6187874668174475623, -5.435381355932195291, 6.657494107589526422 ) ) ;
#7460=CARTESIAN_POINT ( 'NONE',  ( -2.435897774776361491, -3.240557039297494057, 5.753335522918235689 ) ) ;
#7462=CARTESIAN_POINT ( 'NONE',  ( 2.111627294540149968, -3.710163681423230386, 3.660877362176659933 ) ) ;
#7465=CARTESIAN_POINT ( 'NONE',  ( -1.366362128262280429, -1.684082600342149627, 3.167695729602423516 ) ) ;
#7470=CARTESIAN_POINT ( 'NONE',  ( -1.579331079541819394, -1.241605122864670285, 6.832797935622397567 ) ) ;
#7471=CARTESIAN_POINT ( 'NONE',  ( 0.1824815401350060040, -4.498124606865050445, 7.046368721022729709 ) ) ;
#7474=CARTESIAN_POINT ( 'NONE',  ( 2.058670345754650022, -5.050847457627120285, 3.559656372813920111 ) ) ;
#7478=CARTESIAN_POINT ( 'NONE',  ( 1.438959988998139914E-16, -0.2999999999999999889, 2.350000000000000089 ) ) ;
#7480=CARTESIAN_POINT ( 'NONE',  ( 2.531332855772549184, -2.635061543801990869, 5.497162258444460825 ) ) ;
#7485=CARTESIAN_POINT ( 'NONE',  ( -0.6096110657044609971, -1.800524041783589935, 2.426869991387519576 ) ) ;
#7486=CARTESIAN_POINT ( 'NONE',  ( 0.6410058658986126368, -5.311531839079355777, 2.106117395030960626 ) ) ;
#7487=CARTESIAN_POINT ( 'NONE',  ( 2.579602008086750775, -1.051457940198389673, 5.323511966907245707 ) ) ;
#7489=CARTESIAN_POINT ( 'NONE',  ( -2.051973656473811136, -4.917313796054240349, 4.634380218157504672 ) ) ;
#7490=CARTESIAN_POINT ( 'NONE',  ( 2.318251751302029984, -0.3667372881355940306, 4.294764266798990704 ) ) ;
#7500=CARTESIAN_POINT ( 'NONE',  ( -1.145304265383870090, -3.077539021279469988, 6.755972720436099088 ) ) ;
#7504=CARTESIAN_POINT ( 'NONE',  ( 0.7109160811436110450, -1.307629111369560171, 6.943511536198400336 ) ) ;
#7505=CARTESIAN_POINT ( 'NONE',  ( 2.311987889326980294, -4.078935417675859654, 4.260161748947079552 ) ) ;
#7506=CARTESIAN_POINT ( 'NONE',  ( 1.572563554680340703, -0.8185750573155082810, 3.380172092915559645 ) ) ;
#7507=CARTESIAN_POINT ( 'NONE',  ( 0.7983658734558030101, -0.4334745762711870176, 6.913847129767330735 ) ) ;
#7511=CARTESIAN_POINT ( 'NONE',  ( -1.679950111053631900, -0.1957627118644069686, 5.880020650119711867 ) ) ;
#7512=CARTESIAN_POINT ( 'NONE',  ( 1.219286470748990103, -4.381683165423610582, 6.712979431025659416 ) ) ;
#7518=CARTESIAN_POINT ( 'NONE',  ( -2.226511124464849445, -4.525253771513309431, 5.462491901673850236 ) ) ;
#7520=CARTESIAN_POINT ( 'NONE',  ( 2.321479326063749404, -5.050847457627124726, 3.414080590619961608 ) ) ;
#7522=CARTESIAN_POINT ( 'NONE',  ( -0.9150601050661559821, -0.4690677966101700069, 6.868218666554230190 ) ) ;
#7527=CARTESIAN_POINT ( 'NONE',  ( -2.028464043723881005, -4.870737219477664581, 5.016599851465114668 ) ) ;
#7528=CARTESIAN_POINT ( 'NONE',  ( 2.540842781840729536, -0.08898305084745804228, 5.466141598148674952 ) ) ;
#7533=CARTESIAN_POINT ( 'NONE',  ( -2.116444151961480280, -5.546610169491529518, 3.670839500609359707 ) ) ;
#7537=CARTESIAN_POINT ( 'NONE',  ( -1.217041937262000051, -0.2742238837839079402, 2.666998181419179659 ) ) ;
#7538=CARTESIAN_POINT ( 'NONE',  ( 1.579331079541870686, -4.358394877135324030, 6.832797935622368257 ) ) ;
#7540=CARTESIAN_POINT ( 'NONE',  ( -2.245209214543380405, -2.964938456197999894, 5.405536158119060630 ) ) ;
#7541=CARTESIAN_POINT ( 'NONE',  ( 1.652654650382400003, -0.7952867690272209522, 3.029252778805629820 ) ) ;
#7545=CARTESIAN_POINT ( 'NONE',  ( 0.03895741673415010348, -1.870388906648449812, 2.647347042895590086 ) ) ;
#7549=CARTESIAN_POINT ( 'NONE',  ( 2.006003143956041068, -0.8689925102520592581, 6.437545705712618194 ) ) ;
#7551=CARTESIAN_POINT ( 'NONE',  ( 1.728413393879709936, -4.311818300558750039, 6.297289212178290185 ) ) ;
#7555=CARTESIAN_POINT ( 'NONE',  ( -2.354888465609351389, -5.202118644067803999, 5.923664702843871588 ) ) ;
#7564=CARTESIAN_POINT ( 'NONE',  ( 0.2683982510036849733, -2.192584066324520187, 2.059720455735791322 ) ) ;
#7568=CARTESIAN_POINT ( 'NONE',  ( -2.245209214543380405, -2.964938456197999894, 5.405536158119060630 ) ) ;
#7569=CARTESIAN_POINT ( 'NONE',  ( 0.5070585469427659753, -5.011796459788054214, 2.696565570857651473 ) ) ;
#7570=CARTESIAN_POINT ( 'NONE',  ( -2.358786130709981332, -1.656953435693890864, 5.916240799583737164 ) ) ;
#7571=DIRECTION ( 'NONE',  ( 1.000000000000000000, -1.762990951820104838E-17, 2.220446049250309876E-16 ) ) ;
#7573=CARTESIAN_POINT ( 'NONE',  ( 1.851073041990159984, -0.4067796610169499560, 6.153284478378259870 ) ) ;
#7584=CARTESIAN_POINT ( 'NONE',  ( 0.01716182025089369942, -2.169295778036230082, 2.346608583467340026 ) ) ;
#7589=CARTESIAN_POINT ( 'NONE',  ( -2.255259958075430227, -1.703530012270459970, 5.372717034856060003 ) ) ;
#7591=CARTESIAN_POINT ( 'NONE',  ( 1.991984774470479946, -3.985782264522710339, 3.446707398186009907 ) ) ;
#7592=CARTESIAN_POINT ( 'NONE',  ( -1.572563554680370679, -4.781424942684484591, 3.380172092915589843 ) ) ;
#7593=CARTESIAN_POINT ( 'NONE',  ( 1.378221871957440170, -0.4201271186440679872, 6.607619368096269596 ) ) ;
#7599=CARTESIAN_POINT ( 'NONE',  ( -1.795861365445549973, -0.2491525423728821742, 3.705232155007899930 ) ) ;
#7600=CARTESIAN_POINT ( 'NONE',  ( -1.465095039565370127, -3.566593075333519991, 2.858195935359880480 ) ) ;
#7609=CARTESIAN_POINT ( 'NONE',  ( -2.601107615185130673, -5.215466101694915757, 5.226397344856384741 ) ) ;
#7617=CARTESIAN_POINT ( 'NONE',  ( 1.058024172752470182, -3.869340823081269587, 2.940600473883339561 ) ) ;
#7618=CARTESIAN_POINT ( 'NONE',  ( 2.230812463554230352, -0.1023305084745770588, 6.137473736419911674 ) ) ;
#7622=CARTESIAN_POINT ( 'NONE',  ( -1.432215783582709401, -0.4868644067796619179, 6.170863372171116801 ) ) ;
#7624=CARTESIAN_POINT ( 'NONE',  ( 0.08231150243515643339, -0.001483050847457899508, 2.050000000000001155 ) ) ;
#7631=CIRCLE ( 'NONE', #17048, 0.1499999999999999667 ) ;
#7632=CARTESIAN_POINT ( 'NONE',  ( 1.370891210199511434, -3.869340823081269587, 2.427606771969341715 ) ) ;
#7635=CARTESIAN_POINT ( 'NONE',  ( -1.687170344131989852, -2.848497014756560475, 6.340793075730589479 ) ) ;
#7638=CARTESIAN_POINT ( 'NONE',  ( 1.491388273269019571, -4.012911429170968880, 6.110908523251506352 ) ) ;
#7641=CARTESIAN_POINT ( 'NONE',  ( -1.971820545011380821, -1.544352870612421880, 4.128313389260230615 ) ) ;
#7644=CARTESIAN_POINT ( 'NONE',  ( 1.526064881623949931, -0.7763906680874419486, 2.903976516638540062 ) ) ;
#7645=CARTESIAN_POINT ( 'NONE',  ( 2.573461662271340877, -0.7525510688106187285, 5.348389362822485893 ) ) ;
#7650=CARTESIAN_POINT ( 'NONE',  ( -1.428515267734880023, -5.268855932203390324, 2.829745655876930055 ) ) ;
#7659=CARTESIAN_POINT ( 'NONE',  ( -0.7137241095604881513, -2.099430913171361102, 2.143887406933340678 ) ) ;
#7663=CARTESIAN_POINT ( 'NONE',  ( -2.023259452208839626, -3.174533050792599731, 3.497849062500260064 ) ) ;
#7665=CARTESIAN_POINT ( 'NONE',  ( 0.009452110982655383825, -5.000192044704546035, 2.050000000000001155 ) ) ;
#7666=CARTESIAN_POINT ( 'NONE',  ( -2.281778813005780115, -4.847448931189379806, 5.276394947932169899 ) ) ;
#7670=CARTESIAN_POINT ( 'NONE',  ( 1.508881462028659692, -4.311818300558746486, 6.092184821126257255 ) ) ;
#7673=CARTESIAN_POINT ( 'NONE',  ( -1.057242234132100167, -5.577754237288139905, 2.597442975781530272 ) ) ;
#7675=CARTESIAN_POINT ( 'NONE',  ( 1.534924416212170017, -5.333856471232000018, 2.911460733964629899 ) ) ;
#7681=CARTESIAN_POINT ( 'NONE',  ( -2.111627294540180166, -1.889836318576769925, 3.660877362176710559 ) ) ;
#7685=DIRECTION ( 'NONE',  ( 1.000000000000000000, -1.762990951820104838E-17, 2.220446049250309876E-16 ) ) ;
#7687=CARTESIAN_POINT ( 'NONE',  ( 2.329383452786330189, -1.028169651910100013, 5.035735636132829818 ) ) ;
#7688=CARTESIAN_POINT ( 'NONE',  ( 2.192143888961729736, -4.218665147405599392, 5.556300681753580051 ) ) ;
#7689=CARTESIAN_POINT ( 'NONE',  ( 1.903446074666960364, -3.919758276017824006, 5.469282057156545029 ) ) ;
#7694=CARTESIAN_POINT ( 'NONE',  ( 1.575321925694149972, -5.277599664614070818, 3.124678074305839992 ) ) ;
#7695=CARTESIAN_POINT ( 'NONE',  ( 1.246151616534670215, -0.3311440677966111523, 3.068501529594759081 ) ) ;
#7696=CARTESIAN_POINT ( 'NONE',  ( -1.816660071039029933, -3.170692174432619748, 6.196159040268240936 ) ) ;
#7703=CARTESIAN_POINT ( 'NONE',  ( -1.000896394980330006, -5.170974576271190948, 6.829956240957379521 ) ) ;
#7711=CARTESIAN_POINT ( 'NONE',  ( 0.7205524543785531977, -4.428259742000194343, 6.622421910798232503 ) ) ;
#7712=CARTESIAN_POINT ( 'NONE',  ( -0.07064654565474801085, -0.4512711864406789841, 7.352897294663512717 ) ) ;
#7713=( BOUNDED_SURFACE ( )  B_SPLINE_SURFACE ( 3, 3, ( 
 ( #9259, #2228, #17850, #9546, #7875, #5095, #10747 ),
 ( #12325, #16394, #13629, #16586, #9345, #12232, #939 ),
 ( #8158, #15016, #5383, #13799, #13716, #18039, #5189 ),
 ( #2334, #10838, #1123, #3978, #16486, #2606, #8255 ),
 ( #3803, #2431, #8076, #4247, #1211, #18119, #9910 ),
 ( #4437, #11301, #14066, #14176, #15566, #16754, #5829 ),
 ( #1388, #16938, #4071, #7054, #7151, #2786, #18209 ) ),
 .UNSPECIFIED., .T., .F., .F. ) 
 B_SPLINE_SURFACE_WITH_KNOTS ( ( 4, 3, 4 ),
 ( 4, 1, 1, 1, 4 ),
 ( 0.000000000000000000, 3.141592653589790007, 6.283185307179590673 ),
 ( 5.497787143782139729, 5.798117950472390092, 5.930336460519450625, 6.055422062302069364, 6.283185307179590673 ),
 .UNSPECIFIED. ) 
 GEOMETRIC_REPRESENTATION_ITEM ( )  RATIONAL_B_SPLINE_SURFACE ( (
 ( 1.000000000000000000, 1.000000000000000000, 1.000000000000000000, 1.000000000000000000, 1.000000000000000000, 1.000000000000000000, 1.000000000000000000),
 ( 0.3333333333333329818, 0.3333333333333329818, 0.3333333333333329818, 0.3333333333333329818, 0.3333333333333329818, 0.3333333333333329818, 0.3333333333333329818),
 ( 0.3333333333333329818, 0.3333333333333329818, 0.3333333333333329818, 0.3333333333333329818, 0.3333333333333329818, 0.3333333333333329818, 0.3333333333333329818),
 ( 1.000000000000000000, 1.000000000000000000, 1.000000000000000000, 1.000000000000000000, 1.000000000000000000, 1.000000000000000000, 1.000000000000000000),
 ( 0.3333333333333329818, 0.3333333333333329818, 0.3333333333333329818, 0.3333333333333329818, 0.3333333333333329818, 0.3333333333333329818, 0.3333333333333329818),
 ( 0.3333333333333329818, 0.3333333333333329818, 0.3333333333333329818, 0.3333333333333329818, 0.3333333333333329818, 0.3333333333333329818, 0.3333333333333329818),
 ( 1.000000000000000000, 1.000000000000000000, 1.000000000000000000, 1.000000000000000000, 1.000000000000000000, 1.000000000000000000, 1.000000000000000000) ) ) 
 REPRESENTATION_ITEM ( '' )  SURFACE ( )  );
#7715=CARTESIAN_POINT ( 'NONE',  ( -1.289141334274979789, -0.4824152542372879826, 6.297747079672432413 ) ) ;
#7716=CARTESIAN_POINT ( 'NONE',  ( 2.484260633728970546, -0.05783898305084796132, 3.766563288620793593 ) ) ;
#7719=CARTESIAN_POINT ( 'NONE',  ( -1.596341326794979976, -5.564406779661021041, 2.970780074643819990 ) ) ;
#7720=CARTESIAN_POINT ( 'NONE',  ( 1.282210379528779809, -0.9388573751169242421, 6.673494927815259103 ) ) ;
#7721=CARTESIAN_POINT ( 'NONE',  ( -0.8147348917079840769, -0.2831443699174389650, 2.488757019513870183 ) ) ;
#7722=CARTESIAN_POINT ( 'NONE',  ( -2.295344368707641358, -3.473439922180372452, 3.367893426919611688 ) ) ;
#7725=CARTESIAN_POINT ( 'NONE',  ( 1.741913176380120110, -3.640298816558360073, 3.117443785062520067 ) ) ;
#7728=CARTESIAN_POINT ( 'NONE',  ( -1.538437905835030595, -3.221109627369172390, 3.340547664492051094 ) ) ;
#7731=CARTESIAN_POINT ( 'NONE',  ( -1.065036425887979421, -1.218316834576379737, 6.455163597548632559 ) ) ;
#7739=CARTESIAN_POINT ( 'NONE',  ( -2.203023580853999963, -5.242161016949149932, 3.872235369154300333 ) ) ;
#7740=ORIENTED_EDGE ( 'NONE', *, *, #17579, .T. ) ;
#7744=CARTESIAN_POINT ( 'NONE',  ( 1.526064881623949931, -0.7763906680874419486, 2.903976516638540062 ) ) ;
#7747=CARTESIAN_POINT ( 'NONE',  ( 0.6187874668174475623, -5.435381355932195291, 6.657494107589526422 ) ) ;
#7748=CARTESIAN_POINT ( 'NONE',  ( -2.146130664537640786, -3.197821339080880065, 3.138834773724098692 ) ) ;
#7750=CARTESIAN_POINT ( 'NONE',  ( -2.644456467089570939, -1.796683165423619055, 4.476474416072687035 ) ) ;
#7754=CARTESIAN_POINT ( 'NONE',  ( 1.710920205120059823, -4.012911429170970656, 6.316012914303540171 ) ) ;
#7757=CARTESIAN_POINT ( 'NONE',  ( -0.8400312909772689185, -3.030962444702889780, 7.217431453521816920 ) ) ;
#7763=CARTESIAN_POINT ( 'NONE',  ( -2.308170020371289599, -1.726818300558750074, 5.159452766389659217 ) ) ;
#7765=CARTESIAN_POINT ( 'NONE',  ( 2.020286629067969297, -5.408686440677975327, 6.420841923842827370 ) ) ;
#7774=CARTESIAN_POINT ( 'NONE',  ( 1.353103843060669886, -2.798079561820010053, 6.625579309552930063 ) ) ;
#7776=CARTESIAN_POINT ( 'NONE',  ( 1.641808337277750107, -5.413135593220339103, 6.386111670537619744 ) ) ;
#7777=CARTESIAN_POINT ( 'NONE',  ( 0.2818998297622880012, -1.354205687946139935, 7.036509827384409554 ) ) ;
#7778=CARTESIAN_POINT ( 'NONE',  ( 1.928470600873580132, -2.472043525783979678, 3.995796205495612874 ) ) ;
#7780=CARTESIAN_POINT ( 'NONE',  ( 0.2189795514005130062, -0.3044491525423729805, 2.356806637999009801 ) ) ;
#7786=CARTESIAN_POINT ( 'NONE',  ( -1.917298190932639868, -3.496728210468659892, 3.335187436117939885 ) ) ;
#7787=VERTEX_POINT ( 'NONE', #7326 ) ;
#7795=CARTESIAN_POINT ( 'NONE',  ( -0.3743405594629430344, -5.157627118644070308, 7.023440622744399953 ) ) ;
#7799=CARTESIAN_POINT ( 'NONE',  ( 0.1526488871098231337, -3.752899381639833720, 2.652660223633551251 ) ) ;
#7800=CARTESIAN_POINT ( 'NONE',  ( 0.4917262214558945632, -0.008898305084746043966, 2.092115739186370948 ) ) ;
#7802=CARTESIAN_POINT ( 'NONE',  ( 0.07299321914061039640, -0.3014830508474579673, 2.350000000000000089 ) ) ;
#7804=CARTESIAN_POINT ( 'NONE',  ( 0.8570167067220200163, -0.01779661016949179997, 2.508190348879349774 ) ) ;
#7809=CARTESIAN_POINT ( 'NONE',  ( 1.477796163681079911, -5.417584745762709986, 6.531563725478140015 ) ) ;
#7810=CARTESIAN_POINT ( 'NONE',  ( -2.328527996529179411, -5.033755237495684653, 3.426787111016392107 ) ) ;
#7814=CARTESIAN_POINT ( 'NONE',  ( -2.347833536521260367, -3.058091609351150097, 4.537447324629909851 ) ) ;
#7815=CARTESIAN_POINT ( 'NONE',  ( 0.2041457401074358857, -4.498124606865046893, 7.346023093209487875 ) ) ;
#7818=CARTESIAN_POINT ( 'NONE',  ( -1.259207372045990869, -3.267686203945749490, 3.078488779929933639 ) ) ;
#7822=CARTESIAN_POINT ( 'NONE',  ( -1.372465729645771182, -1.264893411152960834, 6.226839763556076157 ) ) ;
#7826=CARTESIAN_POINT ( 'NONE',  ( -2.398725280367459245, -3.151244762504313179, 3.564557036955213754 ) ) ;
#7827=ORIENTED_EDGE ( 'NONE', *, *, #6435, .F. ) ;
#7829=CARTESIAN_POINT ( 'NONE',  ( 2.351212046067109984, -0.9815930753335269099, 4.597298481426010497 ) ) ;
#7831=CARTESIAN_POINT ( 'NONE',  ( 2.050059171113549183, -5.077542372881359789, 4.809263467226075228 ) ) ;
#7839=CARTESIAN_POINT ( 'NONE',  ( -1.088937603231280304, -5.573305084745765470, 2.959627624143549074 ) ) ;
#7840=CARTESIAN_POINT ( 'NONE',  ( 1.597383073937500786, -3.593722239981783861, 2.580688553303249755 ) ) ;
#7841=CARTESIAN_POINT ( 'NONE',  ( 1.661700935665417544, -5.037501140877957084, 3.038299064334577082 ) ) ;
#7842=CARTESIAN_POINT ( 'NONE',  ( -2.639965200365840037, -1.750106588847040845, 4.971472712918284742 ) ) ;
#7845=CARTESIAN_POINT ( 'NONE',  ( -0.9170541073686521161, -4.315659176918719808, 6.867431071947200039 ) ) ;
#7848=CARTESIAN_POINT ( 'NONE',  ( -1.700860513939528751, -3.124115597856051085, 6.737200825918551850 ) ) ;
#7852=CARTESIAN_POINT ( 'NONE',  ( 0.7109160811436110450, -1.307629111369560171, 6.943511536198400336 ) ) ;
#7853=CARTESIAN_POINT ( 'NONE',  ( -2.332582362116870200, -0.5313559322033900578, 4.387643303570819775 ) ) ;
#7855=CARTESIAN_POINT ( 'NONE',  ( 1.467041701146838406, -5.422033898305085309, 6.911479965439912831 ) ) ;
#7858=CARTESIAN_POINT ( 'NONE',  ( 0.06264882350516236265, -5.148728813559319661, 7.052569299041217654 ) ) ;
#7865=CARTESIAN_POINT ( 'NONE',  ( 1.902324933209389890, -2.402178660919109809, 3.314393441133530072 ) ) ;
#7866=CARTESIAN_POINT ( 'NONE',  ( -1.978267656359410154, -5.497669491525420504, 5.974740860598790171 ) ) ;
#7869=CARTESIAN_POINT ( 'NONE',  ( 2.276802572547980130, -2.495331814072260013, 4.104251954998760610 ) ) ;
#7871=CARTESIAN_POINT ( 'NONE',  ( 0.05638445020230590382, -1.377493976234431372, 6.752248190741917178 ) ) ;
#7875=CARTESIAN_POINT ( 'NONE',  ( -0.4617942143426889690, -0.5906145504024210569, 2.383143958488499692 ) ) ;
#7877=CARTESIAN_POINT ( 'NONE',  ( 1.600938225939040116, -5.062364510889980629, 3.099061774060949848 ) ) ;
#7879=CARTESIAN_POINT ( 'NONE',  ( 2.190084968185480374, -4.032358841099290103, 3.838447030292440054 ) ) ;
#7885=CARTESIAN_POINT ( 'NONE',  ( -2.353194804772640314, -5.224364406779660186, 4.731327187377240229 ) ) ;
#7891=CARTESIAN_POINT ( 'NONE',  ( 2.281778813005790330, -0.7525510688106179513, 5.276394947932120161 ) ) ;
#7894=CARTESIAN_POINT ( 'NONE',  ( -1.673492459604430938, -3.496728210468663889, 3.510746103527421891 ) ) ;
#7897=CARTESIAN_POINT ( 'NONE',  ( 1.248294325655350034, -0.02669491525423759934, 2.704938983774300088 ) ) ;
#7899=CARTESIAN_POINT ( 'NONE',  ( 2.116444151961470066, -0.3533898305084750002, 3.670839500609349937 ) ) ;
#7902=CARTESIAN_POINT ( 'NONE',  ( -2.630358833876468960, -0.2313559322033900412, 4.347767980622416317 ) ) ;
#7905=CARTESIAN_POINT ( 'NONE',  ( -2.340070819011249803, -5.519915254237290014, 4.950151441910549899 ) ) ;
#7906=CARTESIAN_POINT ( 'NONE',  ( 2.296954468777709923, -0.6361096273691759784, 4.187412587068651604 ) ) ;
#7907=CARTESIAN_POINT ( 'NONE',  ( 1.300961508564179914, -5.422033898305079092, 6.661123742937279602 ) ) ;
#7911=CARTESIAN_POINT ( 'NONE',  ( 2.632587027711251526, -0.6593979156574641953, 4.364441905910536157 ) ) ;
#7914=CARTESIAN_POINT ( 'NONE',  ( -0.7109160811435620841, -4.292370888630429704, 6.943511536198419876 ) ) ;
#7915=CARTESIAN_POINT ( 'NONE',  ( -2.328527996529179411, -5.033755237495684653, 3.426787111016392107 ) ) ;
#7919=CARTESIAN_POINT ( 'NONE',  ( -1.764143222953850065, -3.174533050792599731, 3.649904513135073802 ) ) ;
#7923=CARTESIAN_POINT ( 'NONE',  ( -0.7205524543785096769, -1.171740257999810852, 6.622421910798247602 ) ) ;
#7924=ORIENTED_EDGE ( 'NONE', *, *, #1240, .T. ) ;
#7930=CARTESIAN_POINT ( 'NONE',  ( 0.2254033459420760055, -0.6247245358507570456, 2.348900562125120217 ) ) ;
#7931=CARTESIAN_POINT ( 'NONE',  ( -0.3832714063288900630, -2.685478996738538626, 7.326064873930687504 ) ) ;
#7936=CARTESIAN_POINT ( 'NONE',  ( 2.034805890357269220, -5.068644067796615360, 4.427518626519221456 ) ) ;
#7944=CARTESIAN_POINT ( 'NONE',  ( 0.9150601050661639757, -5.430932203389830626, 6.868218666554230190 ) ) ;
#7947=CARTESIAN_POINT ( 'NONE',  ( 2.612083973477990373, -3.780028546288090041, 4.230818789270793800 ) ) ;
#7951=CARTESIAN_POINT ( 'NONE',  ( 1.003115764947319910, -4.106064582324129297, 6.828967930617570126 ) ) ;
#7956=CARTESIAN_POINT ( 'NONE',  ( 0.9880847989278174204, -2.262448931189378509, 2.236912075639679198 ) ) ;
#7961=CARTESIAN_POINT ( 'NONE',  ( -2.267872052190610166, -1.843259742000189938, 4.071110468860649867 ) ) ;
#7962=CARTESIAN_POINT ( 'NONE',  ( -2.143090896833110381, -0.5046610169491529962, 5.672454929438350391 ) ) ;
#7969=CARTESIAN_POINT ( 'NONE',  ( 0.001589539283866070029, -0.4248071483275199789, 2.499688892524300154 ) ) ;
#7971=CARTESIAN_POINT ( 'NONE',  ( 2.311987889326980294, -4.078935417675859654, 4.260161748947079552 ) ) ;
#7973=CARTESIAN_POINT ( 'NONE',  ( -2.318251751302029984, -5.533262711864409766, 4.294764266798999586 ) ) ;
#7976=CARTESIAN_POINT ( 'NONE',  ( 2.352760675243219968, -2.565196678937129882, 4.757121734156020132 ) ) ;
#7978=CARTESIAN_POINT ( 'NONE',  ( 0.9361665894546294941, -2.285737219477670390, 2.872845392579769452 ) ) ;
#7993=CARTESIAN_POINT ( 'NONE',  ( -1.378221871957430178, -5.179872881355930048, 6.607619368096279366 ) ) ;
#7997=CARTESIAN_POINT ( 'NONE',  ( 2.334748642087659753, -0.6593979156574649725, 4.403867486184820379 ) ) ;
#8000=CARTESIAN_POINT ( 'NONE',  ( -1.741913176380149864, -1.959701183441629802, 3.117443785062560035 ) ) ;
#8001=CARTESIAN_POINT ( 'NONE',  ( -0.5609751937345790473, -0.1601694915254239793, 7.293870047334757523 ) ) ;
#8004=CARTESIAN_POINT ( 'NONE',  ( 2.270487904532159984, -0.06228813559322070315, 4.080813552109670894 ) ) ;
#8007=CARTESIAN_POINT ( 'NONE',  ( -2.192143888961709308, -1.381334852594400031, 5.556300681753639559 ) ) ;
#8009=CARTESIAN_POINT ( 'NONE',  ( -0.7197963925281907205, -0.5829339996946386604, 2.774540890140321014 ) ) ;
#8011=CARTESIAN_POINT ( 'NONE',  ( -2.632587027711260852, -4.940602084342534894, 4.364441905910590336 ) ) ;
#8016=CARTESIAN_POINT ( 'NONE',  ( 1.588913656381999884, -0.5196681859277345605, 3.399901838171224266 ) ) ;
#8020=CARTESIAN_POINT ( 'NONE',  ( 0.2475374578675958726, -1.354205687946139491, 6.738044908627027318 ) ) ;
#8024=CARTESIAN_POINT ( 'NONE',  ( -1.472933559740131626, -2.848497014756559143, 6.130163826706357177 ) ) ;
#8026=CARTESIAN_POINT ( 'NONE',  ( -3.763524982345449879E-15, -5.450000000000000178, 2.350000000000000089 ) ) ;
#8029=CARTESIAN_POINT ( 'NONE',  ( 0.9930264841371569950, -0.4076464065212260235, 2.562902636367419884 ) ) ;
#8030=CARTESIAN_POINT ( 'NONE',  ( -0.2010642693394331104, -1.847100618360169699, 2.053740970238008501 ) ) ;
#8034=CARTESIAN_POINT ( 'NONE',  ( -0.6964468257805866980, -5.166525423728809407, 6.631228347243847132 ) ) ;
#8036=ADVANCED_FACE ( 'NONE', ( #4327 ), #733, .T. ) ;
#8043=CARTESIAN_POINT ( 'NONE',  ( 2.328217775191430139, -5.381991525423729605, 5.043379051721160522 ) ) ;
#8045=CARTESIAN_POINT ( 'NONE',  ( -1.668426559427188982, -4.385524041783587457, 6.763847501343006385 ) ) ;
#8047=CARTESIAN_POINT ( 'NONE',  ( -2.502804106625960756, -3.426863345603793576, 3.817341913956430410 ) ) ;
#8049=CARTESIAN_POINT ( 'NONE',  ( 2.255259958075439997, -3.896469987729530349, 5.372717034855999607 ) ) ;
#8052=CARTESIAN_POINT ( 'NONE',  ( -0.1110902655589390137, -2.961097579838030569, 7.351560417169478612 ) ) ;
#8056=CARTESIAN_POINT ( 'NONE',  ( -1.197297565406129971, -1.517223705964160008, 6.726135293448209929 ) ) ;
#8057=CARTESIAN_POINT ( 'NONE',  ( -1.112838723655040107, -0.4735169491525429986, 6.773667561836210105 ) ) ;
#8059=CARTESIAN_POINT ( 'NONE',  ( 2.630358833876468960, -5.368644067796615182, 4.347767980622404771 ) ) ;
#8063=CARTESIAN_POINT ( 'NONE',  ( 2.350067830300900162, -5.077542372881358901, 4.825253242917691310 ) ) ;
#8068=B_SPLINE_CURVE_WITH_KNOTS ( 'NONE', 3,
 ( #7420, #3244, #461, #6281, #643, #14539, #8888, #17395, #6103, #11768, #10363, #16029, #3329, #3602, #13622, #5179, #9338, #13710, #7776, #10651, #3791, #16580, #6759, #17557, #4889, #12035, #2127, #932, #10537, #17757, #9448, #14911, #16201, #13420, #15110, #735, #2221, #7866, #6571, #13518, #10931, #5281, #6658, #835, #15007, #7973, #3885, #2504, #3509, #6477, #9153, #15196, #6369, #2424, #8070, #12137, #16297, #9250, #1111, #12225, #1021, #5088 ),
 .UNSPECIFIED., .F., .F.,
 ( 4, 1, 1, 1, 1, 1, 1, 1, 1, 1, 1, 1, 1, 1, 1, 1, 1, 1, 1, 1, 1, 1, 1, 1, 1, 1, 1, 1, 1, 1, 1, 1, 1, 1, 1, 1, 1, 1, 1, 1, 1, 1, 1, 1, 1, 1, 1, 1, 1, 1, 1, 1, 1, 1, 1, 1, 1, 1, 1, 4 ),
 ( 0.7853981633974479459, 0.8785809963429079827, 0.9717638292883680196, 1.064946662233830166, 1.158129495179289981, 1.251312328124750017, 1.344495161070210054, 1.437677994015669869, 1.530860826961129906, 1.624043659906589943, 1.717226492852049979, 1.810409325797509794, 1.903592158742969609, 1.996774991688429868, 2.089957824633889683, 2.183140657579349941, 2.276323490524809756, 2.369506323470270015, 2.462689156415730274, 2.555871989361190089, 2.649054822306649903, 2.742237655252109718, 2.835420488197569977, 2.928603321143030236, 3.021786154088490051, 3.114968987033949865, 3.208151819979410124, 3.301334652924869939, 3.394517485870330198, 3.487700318815790013, 3.580883151761249827, 3.674065984706710086, 3.767248817652169901, 3.860431650597620390, 3.953614483543079761, 4.046797316488540019, 4.139980149433999834, 4.233162982379460537, 4.326345815324920352, 4.419528648270380167, 4.512711481215839981, 4.605894314161299796, 4.699077147106760499, 4.792259980052219426, 4.885442812997680129, 4.978625645943139943, 5.071808478888599758, 5.164991311834059573, 5.258174144779520276, 5.351356977724980091, 5.444539810670439905, 5.537722643615899720, 5.630905476561360423, 5.724088309506820238, 5.817271142452280053, 5.910453975397739868, 6.003636808343199682, 6.096819641288659497, 6.190002474234119312, 6.283185307179590673 ),
 .UNSPECIFIED. ) ;
#8069=CARTESIAN_POINT ( 'NONE',  ( 0.3949552299394610277, -3.776187669928119828, 2.379923265530350385 ) ) ;
#8070=CARTESIAN_POINT ( 'NONE',  ( -1.248294325655370018, -5.573305084745760141, 2.704938983774309857 ) ) ;
#8072=CARTESIAN_POINT ( 'NONE',  ( -1.669205944673819886, -3.147403886144329643, 6.359065158982450505 ) ) ;
#8073=CARTESIAN_POINT ( 'NONE',  ( -2.161802606005209793, -5.010466949207389220, 3.769755311421840283 ) ) ;
#8074=CARTESIAN_POINT ( 'NONE',  ( -1.385380178477320312, -1.982989471729918352, 3.184868453331453075 ) ) ;
#8076=CARTESIAN_POINT ( 'NONE',  ( -1.061361729696689515, -0.2742238837839081067, 2.926312958971010847 ) ) ;
#8086=CARTESIAN_POINT ( 'NONE',  ( -1.889104232906369862, -5.255508474576269684, 3.296507079072529933 ) ) ;
#8088=CARTESIAN_POINT ( 'NONE',  ( -2.418933091173281369, -4.501965483225034426, 5.791730916219171021 ) ) ;
#8090=CARTESIAN_POINT ( 'NONE',  ( 2.350542563031990273, -1.004881363621820123, 4.817027120179740329 ) ) ;
#8091=CARTESIAN_POINT ( 'NONE',  ( 2.345900685764729765, -0.07118644067796649211, 4.512231114381330066 ) ) ;
#8093=CARTESIAN_POINT ( 'NONE',  ( -2.286166334984490067, -0.5135593220338989795, 5.258525443163870605 ) ) ;
#8095=CARTESIAN_POINT ( 'NONE',  ( 0.1765068388402390998, -0.1468220338983061424, 7.347961541693647902 ) ) ;
#8096=VERTEX_POINT ( 'NONE', #4693 ) ;
#8099=CARTESIAN_POINT ( 'NONE',  ( 1.820241257191439699, -0.5196681859277350046, 3.208199930689770163 ) ) ;
#8100=CARTESIAN_POINT ( 'NONE',  ( -0.7983658734557950165, -5.466525423728810118, 6.913847129767330735 ) ) ;
#8101=CARTESIAN_POINT ( 'NONE',  ( 2.622715975066190364, -0.7292627805223297344, 5.105554690682975405 ) ) ;
#8103=CARTESIAN_POINT ( 'NONE',  ( -0.4068869028847361125, -5.251463457376924104, 2.679545647941359743 ) ) ;
#8104=CARTESIAN_POINT ( 'NONE',  ( -2.287919158821179799, -4.548542059801599535, 5.251517552016939483 ) ) ;
#8109=CARTESIAN_POINT ( 'NONE',  ( 1.566607907718229553, -1.167899381639830203, 6.026891670824254810 ) ) ;
#8114=CARTESIAN_POINT ( 'NONE',  ( 1.622657008870240762E-16, -0.3000000000000002665, 2.649999999999998579 ) ) ;
#8115=CARTESIAN_POINT ( 'NONE',  ( -0.6890111762203582346, -1.800524041783588824, 2.137115435286770282 ) ) ;
#8118=CARTESIAN_POINT ( 'NONE',  ( 1.940327948426050941, -5.390889830508485581, 5.370677689277660427 ) ) ;
#8122=CARTESIAN_POINT ( 'NONE',  ( 2.328217775191430139, -5.381991525423729605, 5.043379051721160522 ) ) ;
#8125=CARTESIAN_POINT ( 'NONE',  ( 2.058670345754650022, -5.350847457627120107, 3.559656372813920111 ) ) ;
#8126=CARTESIAN_POINT ( 'NONE',  ( 0.9038768003982520227, -4.129352870612409632, 7.195219513931331967 ) ) ;
#8127=B_SPLINE_CURVE_WITH_KNOTS ( 'NONE', 3,
 ( #18166, #4026, #9783, #7109, #14125, #8576, #2936, #4301, #16812, #7001, #5619, #1543, #145, #5432, #12556, #16714, #12831, #13947, #16988, #9963, #15444, #2753, #15628, #5794, #17074, #12650, #1263, #6908, #8396, #14033, #247, #11894, #13012, #1721, #10216, #6234, #3359, #5886, #10320, #3100, #8660, #1630, #3286, #14309, #7275, #3194, #13180, #10056, #12919, #11528, #17160, #15982, #15712, #11614, #8928, #17513, #15881, #17241, #4481, #496, #7373, #11807 ),
 .UNSPECIFIED., .F., .F.,
 ( 4, 1, 1, 1, 1, 1, 1, 1, 1, 1, 1, 1, 1, 1, 1, 1, 1, 1, 1, 1, 1, 1, 1, 1, 1, 1, 1, 1, 1, 1, 1, 1, 1, 1, 1, 1, 1, 1, 1, 1, 1, 1, 1, 1, 1, 1, 1, 1, 1, 1, 1, 1, 1, 1, 1, 1, 1, 1, 1, 4 ),
 ( 0.000000000000000000, 0.09318283294546000906, 0.1863656658909200181, 0.2795484988363799994, 0.3727313317818400362, 0.4659141647272999620, 0.5590969976727599988, 0.6522798306182200356, 0.7454626635636800724, 0.8386454965091399982, 0.9318283294545990358, 1.025011162400059961, 1.118193995345519998, 1.211376828290979812, 1.304559661236440071, 1.397742494181900108, 1.490925327127360145, 1.584108160072819960, 1.677290993018279996, 1.770473825963740033, 1.863656658909199848, 1.956839491854659885, 2.050022324800119922, 2.143205157745580181, 2.236387990691039995, 2.329570823636499810, 2.422753656581960069, 2.515936489527420328, 2.609119322472880143, 2.702302155418339957, 2.795484988363799772, 2.888667821309260031, 2.981850654254720290, 3.075033487200179660, 3.168216320145639919, 3.261399153091099734, 3.354581986036559993, 3.447764818982019808, 3.540947651927480067, 3.634130484872939437, 3.727313317818399696, 3.820496150763859955, 3.913678983709319770, 4.006861816654780029, 4.100044649600239843, 4.193227482545699658, 4.286410315491160361, 4.379593148436620176, 4.472775981382079991, 4.565958814327539805, 4.659141647272999620, 4.752324480218450553, 4.845507313163910368, 4.938690146109370183, 5.031872979054829997, 5.125055812000289812, 5.218238644945749627, 5.311421477891210330, 5.404604310836670145, 5.497787143782139729 ),
 .UNSPECIFIED. ) ;
#8128=CARTESIAN_POINT ( 'NONE',  ( 0.9250303514740658706, -3.822764246504686270, 2.212544966868020602 ) ) ;
#8130=CARTESIAN_POINT ( 'NONE',  ( 1.588913656381999884, -0.5196681859277345605, 3.399901838171224266 ) ) ;
#8137=CARTESIAN_POINT ( 'NONE',  ( 0.5889081234606849957, -0.4379237288135600092, 6.978529000034869867 ) ) ;
#8139=CARTESIAN_POINT ( 'NONE',  ( -1.981271652668300298, -1.633665147405599871, 5.970160748022450115 ) ) ;
#8143=CARTESIAN_POINT ( 'NONE',  ( -0.7322514394120432923, -5.586652542372875452, 2.149183891723918993 ) ) ;
#8149=CARTESIAN_POINT ( 'NONE',  ( -0.4790341583531910197, -3.683034516774959855, 2.395814251711740006 ) ) ;
#8153=CARTESIAN_POINT ( 'NONE',  ( -2.295719155670160383, -3.287133615874060055, 5.218091927917240191 ) ) ;
#8155=CARTESIAN_POINT ( 'NONE',  ( 0.3943683997329633373, -2.215872354612800521, 2.685210827922638543 ) ) ;
#8158=CARTESIAN_POINT ( 'NONE',  ( -1.873832970144350130, -0.2625000000000002331, 2.826167029855650270 ) ) ;
#8162=CARTESIAN_POINT ( 'NONE',  ( -0.6864473529425049181, -4.591277760018209975, 6.951118770549909343 ) ) ;
#8167=CARTESIAN_POINT ( 'NONE',  ( 2.051331987628511211, -5.073093220338980025, 4.618035453557344461 ) ) ;
#8170=CARTESIAN_POINT ( 'NONE',  ( -0.6150581927481590938, -1.148451969711520082, 6.971662190339330323 ) ) ;
#8172=CARTESIAN_POINT ( 'NONE',  ( -2.316639661709700260, -1.819971453711900056, 4.285359956977770501 ) ) ;
#8173=CARTESIAN_POINT ( 'NONE',  ( 0.4360591020457930123, -0.008898305084746040497, 2.387347919655840034 ) ) ;
#8176=CARTESIAN_POINT ( 'NONE',  ( -2.143090896833110381, -0.5046610169491529962, 5.672454929438350391 ) ) ;
#8178=CARTESIAN_POINT ( 'NONE',  ( 1.889104232906359870, -0.04449152542372909747, 3.296507079072520163 ) ) ;
#8182=CARTESIAN_POINT ( 'NONE',  ( 0.2620510901103108581, -1.893677194936739694, 2.361180871966390260 ) ) ;
#8183=CARTESIAN_POINT ( 'NONE',  ( 2.293398556041700065, -5.364194915254239859, 4.171956209133470317 ) ) ;
#8184=CARTESIAN_POINT ( 'NONE',  ( -2.652408070456659051, -4.917313796054240349, 4.611427313555255481 ) ) ;
#8187=CARTESIAN_POINT ( 'NONE',  ( -0.9170541073686521161, -4.315659176918719808, 6.867431071947200039 ) ) ;
#8189=CARTESIAN_POINT ( 'NONE',  ( 2.199635523370541357, -0.5429564742160235546, 3.215170965528963531 ) ) ;
#8193=CARTESIAN_POINT ( 'NONE',  ( -1.203420131881960398, -1.540511994252448780, 6.363334551077827861 ) ) ;
#8201=CARTESIAN_POINT ( 'NONE',  ( -1.994315313497099229, -0.2135593220338991571, 5.187224322759965922 ) ) ;
#8202=CARTESIAN_POINT ( 'NONE',  ( 2.008025181017630167, -2.079983501243050981, 2.964791492240490101 ) ) ;
#8205=CARTESIAN_POINT ( 'NONE',  ( -1.864786684738369837, -4.804713230972779137, 2.817120744449669978 ) ) ;
#8206=CARTESIAN_POINT ( 'NONE',  ( -1.202278654260740876, -5.179872881355935377, 6.364093491318035589 ) ) ;
#8213=CARTESIAN_POINT ( 'NONE',  ( -0.1910247150515231307, -5.595550847457635868, 2.655937705488500722 ) ) ;
#8215=CARTESIAN_POINT ( 'NONE',  ( -2.579602008086729459, -4.548542059801595094, 5.323511966907305215 ) ) ;
#8216=CARTESIAN_POINT ( 'NONE',  ( 2.369027826908510548, -4.009070552811004440, 3.503830760997844518 ) ) ;
#8218=CARTESIAN_POINT ( 'NONE',  ( -1.372465729645771182, -1.264893411152960834, 6.226839763556076157 ) ) ;
#8226=CARTESIAN_POINT ( 'NONE',  ( 2.645377369053839356, -0.3711864406779670222, 4.488260618344900088 ) ) ;
#8227=CARTESIAN_POINT ( 'NONE',  ( 1.724579595320000047, -3.939205687946140344, 3.098572228637889836 ) ) ;
#8232=CARTESIAN_POINT ( 'NONE',  ( -2.180207327701299658, -5.206567796610168664, 5.586116916730199833 ) ) ;
#8238=ORIENTED_EDGE ( 'NONE', *, *, #13786, .T. ) ;
#8240=CARTESIAN_POINT ( 'NONE',  ( -1.282210379528740063, -4.661142624883069630, 6.673494927815290190 ) ) ;
#8249=CARTESIAN_POINT ( 'NONE',  ( -0.8429265834919730249, -2.076142624883080323, 2.502678798553459760 ) ) ;
#8253=CARTESIAN_POINT ( 'NONE',  ( -1.937109463115380903, -3.426863345603793576, 4.019920026366796684 ) ) ;
#8255=CARTESIAN_POINT ( 'NONE',  ( 0.009452110982654818305, -0.3001920447045379747, 2.350000000000000089 ) ) ;
#8259=CARTESIAN_POINT ( 'NONE',  ( -2.334748642087669523, -4.940602084342530453, 4.403867486184871005 ) ) ;
#8266=CARTESIAN_POINT ( 'NONE',  ( -2.012177589105470066, -5.215466101694915757, 5.107213040360599088 ) ) ;
#8267=CARTESIAN_POINT ( 'NONE',  ( -0.2010642693394331104, -1.847100618360169699, 2.053740970238008501 ) ) ;
#8275=CARTESIAN_POINT ( 'NONE',  ( -1.710920205120030069, -1.587088570829020107, 6.316012914303580139 ) ) ;
#8276=CARTESIAN_POINT ( 'NONE',  ( -2.043014502273419186, -0.2580508474576271305, 3.006203457898251052 ) ) ;
#8277=CARTESIAN_POINT ( 'NONE',  ( 0.3743405594629510280, -0.4423728813559330009, 7.023440622744399953 ) ) ;
#8280=CARTESIAN_POINT ( 'NONE',  ( -1.300961508564169922, -0.1779661016949160013, 6.661123742937279602 ) ) ;
#8281=CARTESIAN_POINT ( 'NONE',  ( 1.652654650382400003, -0.7952867690272209522, 3.029252778805629820 ) ) ;
#8284=CARTESIAN_POINT ( 'NONE',  ( 2.326448859701049976, -2.219713230972779616, 4.344498395672271585 ) ) ;
#8285=CARTESIAN_POINT ( 'NONE',  ( 2.578017356471871135, -5.386440677966105817, 5.329826563567761077 ) ) ;
#8288=CARTESIAN_POINT ( 'NONE',  ( 2.351212046067109984, -0.9815930753335269099, 4.597298481426010497 ) ) ;
#8291=CARTESIAN_POINT ( 'NONE',  ( -1.803891155489810050, -4.781424942684489920, 3.188470185434129966 ) ) ;
#8296=CARTESIAN_POINT ( 'NONE',  ( -1.688800633088611836, -4.758136654396205145, 3.532586505616431616 ) ) ;
#8302=CARTESIAN_POINT ( 'NONE',  ( -0.2453710345350140487, -0.1557203389830511819, 6.738252723719333481 ) ) ;
#8303=CARTESIAN_POINT ( 'NONE',  ( -2.174104834890490778, -4.455388906648449776, 6.221966445066275497 ) ) ;
#8306=CARTESIAN_POINT ( 'NONE',  ( -1.385366411767399608, -5.164643153926310681, 2.415423146782709640 ) ) ;
#8307=CARTESIAN_POINT ( 'NONE',  ( -0.3803919826357066158, -5.291101694915254505, 2.682580100125310896 ) ) ;
#8311=CARTESIAN_POINT ( 'NONE',  ( -1.661700935788390066, -0.5625000000000000000, 3.038299064211610112 ) ) ;
#8313=CARTESIAN_POINT ( 'NONE',  ( -0.8570167067220350043, -5.582203389830509899, 2.508190348879359988 ) ) ;
#8314=CARTESIAN_POINT ( 'NONE',  ( 2.556942001999820580, -3.756740257999804378, 3.989253004641562406 ) ) ;
#8315=CARTESIAN_POINT ( 'NONE',  ( -2.649291707874080970, -3.356998480738929924, 4.543900225523854530 ) ) ;
#8318=CARTESIAN_POINT ( 'NONE',  ( -2.044452488559148851, -1.451199717459271454, 4.887392274793804781 ) ) ;
#8321=CARTESIAN_POINT ( 'NONE',  ( 1.752210068153130074, -5.105895474282090341, 2.947789931846859890 ) ) ;
#8323=CARTESIAN_POINT ( 'NONE',  ( -2.234315482767910144, -0.5402542372881360411, 3.960850823455329905 ) ) ;
#8324=CARTESIAN_POINT ( 'NONE',  ( 0.1226612266411070129, -2.937809291549740021, 7.050255286338659388 ) ) ;
#8326=CARTESIAN_POINT ( 'NONE',  ( 2.321479326063749404, -5.050847457627124726, 3.414080590619961608 ) ) ;
#8335=CARTESIAN_POINT ( 'NONE',  ( -0.8986180677147959095, -3.636457940198390304, 2.524860635301629852 ) ) ;
#8337=CARTESIAN_POINT ( 'NONE',  ( 1.104321075428930765, -5.320452325212860600, 2.282937282173381099 ) ) ;
#8340=CARTESIAN_POINT ( 'NONE',  ( -0.03714311608457869507, -4.521412895153340550, 7.053160869216429596 ) ) ;
#8342=CARTESIAN_POINT ( 'NONE',  ( -1.951270856817509003, -3.263845327585779277, 5.338313313320930398 ) ) ;
#8349=CARTESIAN_POINT ( 'NONE',  ( -2.281778813005780115, -4.847448931189379806, 5.276394947932169899 ) ) ;
#8355=CARTESIAN_POINT ( 'NONE',  ( -0.6964468257805866980, -5.166525423728809407, 6.631228347243847132 ) ) ;
#8361=CARTESIAN_POINT ( 'NONE',  ( 0.9170541073686970801, -1.284340823081270067, 6.867431071947180499 ) ) ;
#8362=CARTESIAN_POINT ( 'NONE',  ( 0.6470883152343921418, -2.569037555297099651, 6.648378442427241630 ) ) ;
#8363=CARTESIAN_POINT ( 'NONE',  ( -1.791574935211209807, -0.1913135593220340047, 6.226029630577610163 ) ) ;
#8366=CARTESIAN_POINT ( 'NONE',  ( 1.000896394980339998, -0.4290254237288140260, 6.829956240957369751 ) ) ;
#8367=CARTESIAN_POINT ( 'NONE',  ( -1.994315313497099229, -0.5135593220338985354, 5.187224322759965922 ) ) ;
#8371=CARTESIAN_POINT ( 'NONE',  ( -0.4974685680287780354, -0.1601694915254240070, 7.000224381598740386 ) ) ;
#8372=CARTESIAN_POINT ( 'NONE',  ( 2.145694642186089851, -1.098034516774969882, 5.666819626392539888 ) ) ;
#8377=CARTESIAN_POINT ( 'NONE',  ( -1.397172971746989178, -1.707370888630439731, 2.806153814454940054 ) ) ;
#8378=CARTESIAN_POINT ( 'NONE',  ( 0.7998959936908462964, -5.435381355932195291, 7.230419212249866945 ) ) ;
#8380=CARTESIAN_POINT ( 'NONE',  ( 1.901882987994760965, -0.3934322033898309257, 5.472995608211450147 ) ) ;
#8385=CARTESIAN_POINT ( 'NONE',  ( 0.05638445020230590382, -1.377493976234431372, 6.752248190741917178 ) ) ;
#8390=CARTESIAN_POINT ( 'NONE',  ( 0.06367493584606445656, -0.3014830508474583004, 2.649999999999998579 ) ) ;
#8392=CARTESIAN_POINT ( 'NONE',  ( 1.752195476665078688, -4.036199717459260761, 6.693219682964302031 ) ) ;
#8394=CARTESIAN_POINT ( 'NONE',  ( 0.7982439214406963357, -5.130932203389829915, 6.591424794228156081 ) ) ;
#8396=CARTESIAN_POINT ( 'NONE',  ( 1.378221871957439504, -0.1201271186440679983, 6.607619368096267820 ) ) ;
#8401=CARTESIAN_POINT ( 'NONE',  ( -1.567709126316399804, -1.684082600342149849, 2.944712621036610134 ) ) ;
#8409=CARTESIAN_POINT ( 'NONE',  ( 0.3743405594629510280, -0.4423728813559330009, 7.023440622744399953 ) ) ;
#8410=CARTESIAN_POINT ( 'NONE',  ( 2.337178851518220135, -2.588484967225419986, 4.976298214796759822 ) ) ;
#8413=CARTESIAN_POINT ( 'NONE',  ( 2.508228811380011081, -5.090889830508485758, 5.566973598334535644 ) ) ;
#8420=CARTESIAN_POINT ( 'NONE',  ( -0.009452110982655139229, -5.299807955295460005, 2.350000000000000089 ) ) ;
#8424=CARTESIAN_POINT ( 'NONE',  ( 2.102728310581320148, -4.241953435693879726, 5.757014351541050345 ) ) ;
#8426=CARTESIAN_POINT ( 'NONE',  ( -1.583713126240711588, -3.170692174432623744, 6.006428174987420654 ) ) ;
#8436=PRODUCT_DEFINITION_CONTEXT ( 'detailed design', #4946, 'design' ) ;
#8438=CARTESIAN_POINT ( 'NONE',  ( -0.07299321914061848715, -5.298516949152539901, 2.350000000000000089 ) ) ;
#8439=CARTESIAN_POINT ( 'NONE',  ( 1.011820239713300484, -1.963542059801608897, 2.246566997958089118 ) ) ;
#8441=CARTESIAN_POINT ( 'NONE',  ( 1.732393070546229819, -0.7511144650864829408, 2.954861780286969886 ) ) ;
#8446=CARTESIAN_POINT ( 'NONE',  ( 2.211317922628870392, -2.472043525783979678, 3.894507149290419967 ) ) ;
#8447=CARTESIAN_POINT ( 'NONE',  ( 0.5549238885286489342, -3.500569086828633658, 2.723396519134821059 ) ) ;
#8448=CARTESIAN_POINT ( 'NONE',  ( 0.1565249325564390115, -0.1468220338983060036, 7.048192310558509810 ) ) ;
#8452=CARTESIAN_POINT ( 'NONE',  ( -2.293398556041709835, -0.2358050847457629773, 4.171956209133480975 ) ) ;
#8453=CARTESIAN_POINT ( 'NONE',  ( 2.126557263589630153, -2.448755237495689574, 3.691783806836010040 ) ) ;
#8457=CARTESIAN_POINT ( 'NONE',  ( 0.6918414964981907112, -1.940253771513320125, 2.450533167346752084 ) ) ;
#8459=CARTESIAN_POINT ( 'NONE',  ( -1.596341326794979976, -5.564406779661021041, 2.970780074643819990 ) ) ;
#8462=CARTESIAN_POINT ( 'NONE',  ( 0.4985810152601650724, -1.330917399657850053, 7.000035360316460675 ) ) ;
#8464=CARTESIAN_POINT ( 'NONE',  ( -2.000624272291700034, -0.5358050847457624943, 4.239366054776020576 ) ) ;
#8471=CARTESIAN_POINT ( 'NONE',  ( 1.259207372045950457, -2.332313796054251487, 3.078488779929903441 ) ) ;
#8479=CARTESIAN_POINT ( 'NONE',  ( 0.2453710345350221533, -5.444279661016954819, 6.738252723719333481 ) ) ;
#8487=CARTESIAN_POINT ( 'NONE',  ( 0.6864473529425539899, -1.008722239981789892, 6.951118770549889803 ) ) ;
#8491=CARTESIAN_POINT ( 'NONE',  ( -1.909909196654771213, -1.567641158900710430, 3.946907241329710381 ) ) ;
#8496=CARTESIAN_POINT ( 'NONE',  ( -2.058670345754650022, -0.5491525423728820243, 3.559656372813929881 ) ) ;
#8497=CARTESIAN_POINT ( 'NONE',  ( -2.219956784870669608, -3.426863345603790023, 3.918630970161619764 ) ) ;
#8500=CARTESIAN_POINT ( 'NONE',  ( 0.07064654565475687875, -5.448728813559320372, 7.352897294663512717 ) ) ;
#8510=CARTESIAN_POINT ( 'NONE',  ( -1.558664967382870525, -1.540511994252448780, 6.847947208954447973 ) ) ;
#8513=CARTESIAN_POINT ( 'NONE',  ( -0.009452110982655142699, -0.5998079552954631577, 2.050000000000001155 ) ) ;
#8514=CARTESIAN_POINT ( 'NONE',  ( 0.6536199613480476733, -5.011796459788070202, 2.109674034588110647 ) ) ;
#8516=CARTESIAN_POINT ( 'NONE',  ( -0.8242394280876599311, -1.171740257999809964, 6.904399023015030501 ) ) ;
#8519=CARTESIAN_POINT ( 'NONE',  ( 1.994983296312400123, -4.265241723982169830, 5.948514050749290405 ) ) ;
#8521=CARTESIAN_POINT ( 'NONE',  ( 0.6713553523423281266, -2.867944426684881254, 6.640150466718861999 ) ) ;
#8536=CARTESIAN_POINT ( 'NONE',  ( 1.880631435828169939, -5.055296610169490279, 3.876649216148224220 ) ) ;
#8538=CARTESIAN_POINT ( 'NONE',  ( 1.757131520353529819, -0.5645261550885040114, 2.952711384047340015 ) ) ;
#8546=CARTESIAN_POINT ( 'NONE',  ( -2.219956784870669608, -3.426863345603790023, 3.918630970161619764 ) ) ;
#8547=CARTESIAN_POINT ( 'NONE',  ( 1.520647680314149541, -3.640298816558361406, 3.320676805464615633 ) ) ;
#8548=CARTESIAN_POINT ( 'NONE',  ( 2.052786957354850728, -0.07563559322033948373, 4.727327971967373976 ) ) ;
#8552=CARTESIAN_POINT ( 'NONE',  ( 2.253200202764420013, -0.08898305084745811167, 5.379408587037500133 ) ) ;
#8553=CARTESIAN_POINT ( 'NONE',  ( -0.2023972492402590084, -2.146007489747939978, 2.355265251465770149 ) ) ;
#8558=CARTESIAN_POINT ( 'NONE',  ( -1.962536940652958695, -2.895073591333140683, 5.998920491814799583 ) ) ;
#8560=CARTESIAN_POINT ( 'NONE',  ( -2.230812463554230352, -5.497669491525425833, 6.137473736419926773 ) ) ;
#8562=CARTESIAN_POINT ( 'NONE',  ( -1.197297565406129971, -1.517223705964160008, 6.726135293448209929 ) ) ;
#8563=CARTESIAN_POINT ( 'NONE',  ( -2.030998484741458832, -0.5180084745762725262, 4.999543428097190656 ) ) ;
#8568=CARTESIAN_POINT ( 'NONE',  ( 0.1086361371091010830, -2.937809291549738688, 6.750146344128172160 ) ) ;
#8574=CARTESIAN_POINT ( 'NONE',  ( 1.811729841638690219, -5.341949152542369461, 3.197954009834290012 ) ) ;
#8576=CARTESIAN_POINT ( 'NONE',  ( 0.8570167067220199053, -0.01779661016949179650, 2.508190348879350218 ) ) ;
#8578=CARTESIAN_POINT ( 'NONE',  ( 0.2812789908084389889, -5.444279661016950378, 7.036533610117280624 ) ) ;
#8584=CARTESIAN_POINT ( 'NONE',  ( 1.460675875430079929, -0.9155690868286359141, 6.545310725710029587 ) ) ;
#8586=CARTESIAN_POINT ( 'NONE',  ( 1.992092870331701349, -2.196424942684489956, 4.203544726484164329 ) ) ;
#8592=CARTESIAN_POINT ( 'NONE',  ( 2.268288188848061715, -0.04894067796610205440, 3.322421079292310786 ) ) ;
#8593=CARTESIAN_POINT ( 'NONE',  ( 0.8189529353761060282, -3.822764246504690266, 2.493631540942729874 ) ) ;
#8596=CARTESIAN_POINT ( 'NONE',  ( -2.540842781840720654, -5.211016949152535993, 5.466141598148674952 ) ) ;
#8600=CARTESIAN_POINT ( 'NONE',  ( -2.318251751302029984, -5.233262711864408168, 4.294764266799000474 ) ) ;
#8602=CARTESIAN_POINT ( 'NONE',  ( 1.588044008096809900, -0.7645959921354850142, 3.097578792715899976 ) ) ;
#8604=B_SPLINE_CURVE_WITH_KNOTS ( 'NONE', 3,
 ( #2317, #2584, #12219, #15001, #6750, #12308, #1103, #7969, #17932, #16659, #16574, #9444, #3965, #15106, #16740, #6930 ),
 .UNSPECIFIED., .F., .F.,
 ( 4, 1, 1, 1, 1, 1, 1, 1, 1, 1, 1, 1, 1, 4 ),
 ( 0.4999998212288440103, 0.5105793490764080067, 0.5531463519625079428, 0.5957147871422280305, 0.6382850093032239602, 0.6808567369985039086, 0.7234300338917989404, 0.7660011046592689610, 0.8085801951441730084, 0.8511153557612559650, 0.8935297551199039567, 0.9363130006848809916, 0.9717764100585750686, 1.000000000000000000 ),
 .UNSPECIFIED. ) ;
#8606=CARTESIAN_POINT ( 'NONE',  ( -2.358786130709981332, -1.656953435693890864, 5.916240799583737164 ) ) ;
#8607=CARTESIAN_POINT ( 'NONE',  ( 0.8469861386668179337, -0.7068739681193977331, 2.826929786773349385 ) ) ;
#8609=CARTESIAN_POINT ( 'NONE',  ( 1.661700935788380074, -5.337500000000000355, 3.038299064211610112 ) ) ;
#8611=CARTESIAN_POINT ( 'NONE',  ( 0.5320716618284230259, -2.592325843585389755, 6.992519451207130032 ) ) ;
#8613=CARTESIAN_POINT ( 'NONE',  ( -1.460675875430050175, -4.684430913171359734, 6.545310725710059785 ) ) ;
#8615=CARTESIAN_POINT ( 'NONE',  ( 1.019987577504959608, -2.821367850108300157, 6.481720287913791623 ) ) ;
#8618=CARTESIAN_POINT ( 'NONE',  ( 1.750316316486830059, -0.3400423728813560253, 3.126818518378580158 ) ) ;
#8627=CARTESIAN_POINT ( 'NONE',  ( 1.562863241354470523, -5.408686440677975327, 6.031217337312382298 ) ) ;
#8633=CARTESIAN_POINT ( 'NONE',  ( -0.6343239990445920240, -2.099430913171359769, 2.433641963034089972 ) ) ;
#8634=CARTESIAN_POINT ( 'NONE',  ( -1.181710496343089556, -2.801920438179980710, 6.378827610405741311 ) ) ;
#8635=CARTESIAN_POINT ( 'NONE',  ( -2.350067830300900162, -0.2224576271186440024, 4.825253242917699303 ) ) ;
#8637=CARTESIAN_POINT ( 'NONE',  ( 2.350542563031990273, -1.004881363621820123, 4.817027120179740329 ) ) ;
#8640=CARTESIAN_POINT ( 'NONE',  ( -1.112838723655040107, -0.1735169491525430097, 6.773667561836210105 ) ) ;
#8641=CARTESIAN_POINT ( 'NONE',  ( 0.2365712905368450025, -2.192584066324519743, 2.358466376073659720 ) ) ;
#8644=CARTESIAN_POINT ( 'NONE',  ( 1.552749016687789974, -4.036199717459258984, 6.468535037441731639 ) ) ;
#8646=CARTESIAN_POINT ( 'NONE',  ( -2.130266475405059090, -5.555508474576275724, 3.117337770017961418 ) ) ;
#8649=CARTESIAN_POINT ( 'NONE',  ( -0.2453710345350140487, -0.4557203389830515317, 6.738252723719333481 ) ) ;
#8653=CARTESIAN_POINT ( 'NONE',  ( 0.4874850653660255384, -2.891232714973161144, 6.694306935672937442 ) ) ;
#8658=CARTESIAN_POINT ( 'NONE',  ( 2.043308330018790198, -5.399788135593220240, 5.867646457774659652 ) ) ;
#8660=CARTESIAN_POINT ( 'NONE',  ( -1.112838723655039885, -0.1735169491525430097, 6.773667561836209217 ) ) ;
#8665=CARTESIAN_POINT ( 'NONE',  ( 0.08304008649498713368, -2.638902420161969520, 6.751342532748487280 ) ) ;
#8671=CARTESIAN_POINT ( 'NONE',  ( 2.540842781840729536, -0.3889830508474575455, 5.466141598148674952 ) ) ;
#8672=CARTESIAN_POINT ( 'NONE',  ( -1.661700935788390066, -0.5625000000000000000, 3.038299064211610112 ) ) ;
#8675=CARTESIAN_POINT ( 'NONE',  ( -1.973760952634090238, -5.259957627118655665, 2.925986839873730982 ) ) ;
#8683=CARTESIAN_POINT ( 'NONE',  ( -0.4247583764260595141, -1.424070552811000701, 7.319674410047512403 ) ) ;
#8685=CARTESIAN_POINT ( 'NONE',  ( 1.458615186838411626, -0.4963798976394455664, 3.259477383973563125 ) ) ;
#8687=CARTESIAN_POINT ( 'NONE',  ( 0.6918414964981909332, -1.940253771513320125, 2.450533167346750307 ) ) ;
#8690=CARTESIAN_POINT ( 'NONE',  ( 1.732245706108171746, -5.033893599512585304, 2.684512698446369861 ) ) ;
#8691=CARTESIAN_POINT ( 'NONE',  ( 0.8001094918299610503, -1.307629111369559949, 7.230402832373829192 ) ) ;
#8696=CARTESIAN_POINT ( 'NONE',  ( -1.417606053559450352, -4.707719201459645397, 6.185023541745952258 ) ) ;
#8702=ORIENTED_EDGE ( 'NONE', *, *, #1240, .F. ) ;
#8705=CARTESIAN_POINT ( 'NONE',  ( -0.3803919826357066158, -5.591101694915256104, 2.682580100125310896 ) ) ;
#8707=CARTESIAN_POINT ( 'NONE',  ( -0.8642983280852033490, -2.732055573315119723, 7.209203477813437289 ) ) ;
#8710=CARTESIAN_POINT ( 'NONE',  ( -0.2109711709854041328, -5.280843314568215874, 2.050669023674909663 ) ) ;
#8714=CARTESIAN_POINT ( 'NONE',  ( 1.265407828724300021, -2.309025507765960050, 2.715689360385540319 ) ) ;
#8715=CARTESIAN_POINT ( 'NONE',  ( -1.138568046961029978, -4.362235753495300905, 6.408380708468528475 ) ) ;
#8716=CARTESIAN_POINT ( 'NONE',  ( -1.477796163681079911, -0.1824152542372889929, 6.531563725478150673 ) ) ;
#8720=CARTESIAN_POINT ( 'NONE',  ( -0.3162622016569221484, -4.245794312053864594, 7.334974746141788238 ) ) ;
#8721=CARTESIAN_POINT ( 'NONE',  ( 2.041338374031088865, -0.08008474576271226719, 4.918217215283659627 ) ) ;
#8722=CARTESIAN_POINT ( 'NONE',  ( -2.340959815966380031, -1.750106588847040179, 4.942183458383479611 ) ) ;
#8726=CARTESIAN_POINT ( 'NONE',  ( 0.5902886515193200845, -4.152641158900700624, 6.978224088050040130 ) ) ;
#8728=CARTESIAN_POINT ( 'NONE',  ( -1.347262683220810553, -5.175423728813555613, 6.986424775243341045 ) ) ;
#8731=CARTESIAN_POINT ( 'NONE',  ( 0.1365430262726380628, -0.4468220338983063811, 6.748423079423377047 ) ) ;
#8736=CARTESIAN_POINT ( 'NONE',  ( -0.5549238885286955636, -2.099430913171361102, 2.723396519134838822 ) ) ;
#8738=CARTESIAN_POINT ( 'NONE',  ( 1.192209327851080136, -0.3222457627118649470, 2.329031440774910422 ) ) ;
#8741=CARTESIAN_POINT ( 'NONE',  ( 1.626487163628800081, -5.044101657174960174, 3.073512836371200319 ) ) ;
#8744=CARTESIAN_POINT ( 'NONE',  ( 1.641808337277750107, -5.413135593220339103, 6.386111670537619744 ) ) ;
#8748=CARTESIAN_POINT ( 'NONE',  ( 0.009452110982654814836, -0.3001920447045380858, 2.649999999999998579 ) ) ;
#8751=CARTESIAN_POINT ( 'NONE',  ( -0.1768565782246520057, -1.847100618360170143, 2.353200596935780098 ) ) ;
#8754=CARTESIAN_POINT ( 'NONE',  ( -1.599895119336340876, -2.871785303044851023, 5.986560317183706736 ) ) ;
#8762=CARTESIAN_POINT ( 'NONE',  ( 1.610878918935058524, -0.03114406779661053892, 2.590989782159081933 ) ) ;
#8763=CARTESIAN_POINT ( 'NONE',  ( -1.282210379528740063, -4.661142624883069630, 6.673494927815290190 ) ) ;
#8766=CARTESIAN_POINT ( 'NONE',  ( 1.925796468768800063, -5.104237288135590411, 6.052706598917719560 ) ) ;
#8773=CARTESIAN_POINT ( 'NONE',  ( 2.584100759211419795, -0.9350164987569505870, 4.095403473953104445 ) ) ;
#8776=CARTESIAN_POINT ( 'NONE',  ( -1.567709126316399804, -1.684082600342149849, 2.944712621036610134 ) ) ;
#8779=CARTESIAN_POINT ( 'NONE',  ( 0.06913820924143311564, -1.377493976234431372, 7.352985789827153340 ) ) ;
#8782=CARTESIAN_POINT ( 'NONE',  ( 1.652654650382400003, -0.7952867690272209522, 3.029252778805620050 ) ) ;
#8788=EDGE_LOOP ( 'NONE', ( #3835, #7152, #7924, #3656 ) ) ;
#8797=CARTESIAN_POINT ( 'NONE',  ( 1.432215783582721613, -5.413135593220339992, 6.170863372171116801 ) ) ;
#8799=CARTESIAN_POINT ( 'NONE',  ( -1.094547058713670085, -2.755343861603408939, 7.117660114503937763 ) ) ;
#8804=CARTESIAN_POINT ( 'NONE',  ( 2.331386066015260106, -0.9583047870452390260, 4.378465089518139841 ) ) ;
#8806=CARTESIAN_POINT ( 'NONE',  ( -2.159566522375440112, -3.240557039297490061, 5.635424033751089468 ) ) ;
#8808=CARTESIAN_POINT ( 'NONE',  ( 1.203420131881999477, -4.059488005747546424, 6.363334551077796775 ) ) ;
#8810=CARTESIAN_POINT ( 'NONE',  ( 2.253200202764420013, -0.3889830508474579895, 5.379408587037500133 ) ) ;
#8814=CARTESIAN_POINT ( 'NONE',  ( 0.4247583764261176897, -4.175929447188994281, 7.319674410047496416 ) ) ;
#8816=CARTESIAN_POINT ( 'NONE',  ( 0.1910247150515120007, -0.3044491525423730915, 2.655937705488500722 ) ) ;
#8817=CARTESIAN_POINT ( 'NONE',  ( 0.01716182025089369942, -2.169295778036230082, 2.346608583467340026 ) ) ;
#8824=CARTESIAN_POINT ( 'NONE',  ( 1.586727176531399941, -3.617010528270070413, 2.961885344765600614 ) ) ;
#8827=CARTESIAN_POINT ( 'NONE',  ( -2.638803263991410741, -5.219915254237295521, 4.982085668537435730 ) ) ;
#8831=CARTESIAN_POINT ( 'NONE',  ( 1.851073041990159984, -0.4067796610169499560, 6.153284478378259870 ) ) ;
#8835=CARTESIAN_POINT ( 'NONE',  ( 2.025702773739959106, -2.518620102360551893, 4.366188503657621567 ) ) ;
#8836=CARTESIAN_POINT ( 'NONE',  ( 2.458531667407859889, -0.3934322033898309257, 5.699238225248945966 ) ) ;
#8843=CARTESIAN_POINT ( 'NONE',  ( -0.006659065580995300951, -0.5555405507507519269, 2.241023775284399999 ) ) ;
#8844=CARTESIAN_POINT ( 'NONE',  ( -1.921786527979019166, -5.542161016949150643, 3.977907449687794195 ) ) ;
#8848=CARTESIAN_POINT ( 'NONE',  ( -2.649291707874080970, -3.356998480738929924, 4.543900225523854530 ) ) ;
#8851=CARTESIAN_POINT ( 'NONE',  ( -0.9719602541832299547, -2.755343861603410271, 6.843370931913550059 ) ) ;
#8853=CARTESIAN_POINT ( 'NONE',  ( 2.035869680587130137, -2.289578095837640159, 4.964832940349494628 ) ) ;
#8859=CARTESIAN_POINT ( 'NONE',  ( 2.311987889326980294, -4.078935417675859654, 4.260161748947079552 ) ) ;
#8862=CARTESIAN_POINT ( 'NONE',  ( -2.230812463554230352, -5.197669491525426011, 6.137473736419926773 ) ) ;
#8869=CARTESIAN_POINT ( 'NONE',  ( 0.02098813186351079427, -2.169295778036230526, 2.046196467083000403 ) ) ;
#8870=CARTESIAN_POINT ( 'NONE',  ( 1.526064881623949931, -0.7763906680874419486, 2.903976516638540062 ) ) ;
#8873=CARTESIAN_POINT ( 'NONE',  ( 1.917298190932609891, -2.103271789531340197, 3.335187436117899917 ) ) ;
#8874=CARTESIAN_POINT ( 'NONE',  ( 1.468674196027861756, -1.237764246504700072, 6.910454658870847311 ) ) ;
#8876=CARTESIAN_POINT ( 'NONE',  ( 1.632144308286169965, -4.288530012270460823, 5.945394234592866312 ) ) ;
#8880=ORIENTED_EDGE ( 'NONE', *, *, #4313, .T. ) ;
#8885=CARTESIAN_POINT ( 'NONE',  ( 2.034805890357269220, -5.368644067796615182, 4.427518626519221456 ) ) ;
#8888=CARTESIAN_POINT ( 'NONE',  ( 2.234315482767910144, -5.359745762711869865, 3.960850823455320580 ) ) ;
#8890=CARTESIAN_POINT ( 'NONE',  ( 1.794646911016580137, -1.167899381639829981, 6.222494056560660347 ) ) ;
#8893=CARTESIAN_POINT ( 'NONE',  ( -0.6918414964982418924, -3.659746228486680408, 2.450533167346770291 ) ) ;
#8894=CARTESIAN_POINT ( 'NONE',  ( -1.942813984510721070, -4.525253771513313872, 5.363608065214459764 ) ) ;
#8895=EDGE_CURVE ( 'NONE', #13175, #14300, #8604, .T. ) ;
#8896=CARTESIAN_POINT ( 'NONE',  ( -0.009452173233712278175, -5.299808941921980043, 2.358866582356820008 ) ) ;
#8900=( BOUNDED_SURFACE ( )  B_SPLINE_SURFACE ( 3, 3, ( 
 ( #16348, #15076, #6534, #2387, #14030, #1260, #16808 ),
 ( #6905, #12645, #8306, #5429, #18270, #11066, #18082 ),
 ( #8205, #13852, #9960, #1171, #7106, #6819, #11351 ),
 ( #4023, #10986, #12745, #12374, #2552, #15348, #12464 ),
 ( #60, #5616, #18162, #4298, #16710, #5706, #9677 ),
 ( #2653, #6997, #12553, #13943, #4121, #11260, #11159 ),
 ( #2932, #9780, #16984, #9588, #4209, #15441, #16634 ) ),
 .UNSPECIFIED., .T., .F., .F. ) 
 B_SPLINE_SURFACE_WITH_KNOTS ( ( 4, 3, 4 ),
 ( 4, 1, 1, 1, 4 ),
 ( 0.000000000000000000, 3.141592653589790007, 6.283185307179590673 ),
 ( 18.06415775814129887, 18.36448856483159986, 18.49670707487869947, 18.62179267666130045, 18.84955592153880133 ),
 .UNSPECIFIED. ) 
 GEOMETRIC_REPRESENTATION_ITEM ( )  RATIONAL_B_SPLINE_SURFACE ( (
 ( 1.000000000000000000, 1.000000000000000000, 1.000000000000000000, 1.000000000000000000, 1.000000000000000000, 1.000000000000000000, 1.000000000000000000),
 ( 0.3333333333333329818, 0.3333333333333329818, 0.3333333333333329818, 0.3333333333333329818, 0.3333333333333329818, 0.3333333333333329818, 0.3333333333333329818),
 ( 0.3333333333333329818, 0.3333333333333329818, 0.3333333333333329818, 0.3333333333333329818, 0.3333333333333329818, 0.3333333333333329818, 0.3333333333333329818),
 ( 1.000000000000000000, 1.000000000000000000, 1.000000000000000000, 1.000000000000000000, 1.000000000000000000, 1.000000000000000000, 1.000000000000000000),
 ( 0.3333333333333329818, 0.3333333333333329818, 0.3333333333333329818, 0.3333333333333329818, 0.3333333333333329818, 0.3333333333333329818, 0.3333333333333329818),
 ( 0.3333333333333329818, 0.3333333333333329818, 0.3333333333333329818, 0.3333333333333329818, 0.3333333333333329818, 0.3333333333333329818, 0.3333333333333329818),
 ( 1.000000000000000000, 1.000000000000000000, 1.000000000000000000, 1.000000000000000000, 1.000000000000000000, 1.000000000000000000, 1.000000000000000000) ) ) 
 REPRESENTATION_ITEM ( '' )  SURFACE ( )  );
#8901=CARTESIAN_POINT ( 'NONE',  ( 1.901882987994760965, -0.09343220338983100615, 5.472995608211450147 ) ) ;
#8902=CARTESIAN_POINT ( 'NONE',  ( 1.991984774470479946, -3.985782264522710339, 3.446707398186009907 ) ) ;
#8907=CARTESIAN_POINT ( 'NONE',  ( 2.005512128484128631, -3.686875393134939838, 3.468469736471341491 ) ) ;
#8909=CARTESIAN_POINT ( 'NONE',  ( 2.191755591049679541, -5.046398305084744962, 3.203650300307709475 ) ) ;
#8911=CARTESIAN_POINT ( 'NONE',  ( -2.351526912647309953, -0.5269067796610169552, 4.606040641882809261 ) ) ;
#8917=CARTESIAN_POINT ( 'NONE',  ( -1.934380261529029754, -4.824160642901089702, 5.387804366397155320 ) ) ;
#8919=CARTESIAN_POINT ( 'NONE',  ( -2.431060148753501515, -0.5447033898305090327, 3.635668498923334102 ) ) ;
#8928=CARTESIAN_POINT ( 'NONE',  ( -2.293398556041709835, -0.2358050847457630328, 4.171956209133481863 ) ) ;
#8929=CARTESIAN_POINT ( 'NONE',  ( -0.1926573868394080846, -0.2965485159365558454, 2.049233193116839935 ) ) ;
#8930=CARTESIAN_POINT ( 'NONE',  ( 2.370419177058800120, -4.241953435693877061, 5.893409660608535994 ) ) ;
#8932=CARTESIAN_POINT ( 'NONE',  ( 1.816660071039059909, -2.429307825567370127, 6.196159040268200968 ) ) ;
#8935=CARTESIAN_POINT ( 'NONE',  ( -0.8893259633308450152, -1.753947465207011058, 2.849594321892158888 ) ) ;
#8941=CARTESIAN_POINT ( 'NONE',  ( -0.6919952253609726878, -1.148451969711520082, 7.262080463428013388 ) ) ;
#8947=CARTESIAN_POINT ( 'NONE',  ( 1.791574935211219799, -5.108686440677970175, 6.226029630577610163 ) ) ;
#8954=CARTESIAN_POINT ( 'NONE',  ( 2.282375681463800543, -2.425466949207401690, 3.345793611865401473 ) ) ;
#8958=CARTESIAN_POINT ( 'NONE',  ( 1.286937324407710026, -2.010118636378180224, 2.729584305145179801 ) ) ;
#8959=CARTESIAN_POINT ( 'NONE',  ( -0.009452110982655114943, -5.299807955295455564, 2.050000000000001155 ) ) ;
#8961=CARTESIAN_POINT ( 'NONE',  ( -2.065623031241579977, -5.033755237495680213, 3.572193642975310279 ) ) ;
#8963=CARTESIAN_POINT ( 'NONE',  ( 2.231116159141619981, -0.9117282104686620370, 3.951089877392439664 ) ) ;
#8972=CARTESIAN_POINT ( 'NONE',  ( 1.074829861819710075, -2.285737219477669946, 2.606322265575589991 ) ) ;
#8976=CARTESIAN_POINT ( 'NONE',  ( -1.710920205120030069, -1.587088570829020107, 6.316012914303580139 ) ) ;
#8977=CARTESIAN_POINT ( 'NONE',  ( 1.728413393879709936, -4.311818300558750039, 6.297289212178290185 ) ) ;
#8978=CARTESIAN_POINT ( 'NONE',  ( 1.945780800405119360, -0.9117282104686613708, 4.045142061754263274 ) ) ;
#8982=CARTESIAN_POINT ( 'NONE',  ( -2.050059171113549183, -0.2224576271186441134, 4.809263467226075228 ) ) ;
#8983=CARTESIAN_POINT ( 'NONE',  ( 0.6150581927482109412, -4.451548030288480895, 6.971662190339319665 ) ) ;
#8988=CARTESIAN_POINT ( 'NONE',  ( -2.046174187462379557, -4.478677194936738992, 5.862719605944011647 ) ) ;
#8989=CARTESIAN_POINT ( 'NONE',  ( -0.7322514394120432923, -5.586652542372875452, 2.149183891723918993 ) ) ;
#8995=CARTESIAN_POINT ( 'NONE',  ( -0.9588981328681495109, -3.613169651910099756, 2.884671871696449230 ) ) ;
#8996=CARTESIAN_POINT ( 'NONE',  ( -2.650076489488250697, -0.5224576271186435195, 4.841243018609314497 ) ) ;
#9003=CARTESIAN_POINT ( 'NONE',  ( 2.653886076156968699, -4.125511994252439862, 4.698454755023375284 ) ) ;
#9006=CARTESIAN_POINT ( 'NONE',  ( 0.4201920264139500372, -3.477280798540340001, 2.384360920086630031 ) ) ;
#9010=CARTESIAN_POINT ( 'NONE',  ( 1.385380178477290558, -3.617010528270069525, 3.184868453331423765 ) ) ;
#9012=CARTESIAN_POINT ( 'NONE',  ( 0.5972539422562040956, -1.008722239981790558, 6.664227474374466276 ) ) ;
#9013=ORIENTED_EDGE ( 'NONE', *, *, #5510, .T. ) ;
#9016=CARTESIAN_POINT ( 'NONE',  ( 1.440522616026430391, -0.7952867690272208412, 3.241384813161591438 ) ) ;
#9017=CARTESIAN_POINT ( 'NONE',  ( 2.652408070456659051, -0.6826862039457533005, 4.611427313555195084 ) ) ;
#9018=EDGE_LOOP ( 'NONE', ( #1044, #17607, #13317, #11043 ) ) ;
#9019=CARTESIAN_POINT ( 'NONE',  ( 1.869848057046569867, -4.288530012270459935, 6.129130480762009725 ) ) ;
#9022=CARTESIAN_POINT ( 'NONE',  ( -2.318251751302029984, -5.233262711864409056, 4.294764266798999586 ) ) ;
#9030=CARTESIAN_POINT ( 'NONE',  ( 0.8642983280852605255, -2.867944426684881254, 7.209203477813407979 ) ) ;
#9034=CARTESIAN_POINT ( 'NONE',  ( -1.764807890102220167, -3.221109627369169726, 3.143016121304770039 ) ) ;
#9035=CARTESIAN_POINT ( 'NONE',  ( 0.9788656693287738353, -5.320452325212859712, 2.556357798777459944 ) ) ;
#9036=CARTESIAN_POINT ( 'NONE',  ( 0.5606293434988925961, -1.330917399657850497, 7.293994686233932434 ) ) ;
#9037=CARTESIAN_POINT ( 'NONE',  ( 1.659340743383524552, -5.037500632107527743, 3.040659256616468742 ) ) ;
#9038=CARTESIAN_POINT ( 'NONE',  ( -0.06264882350515391107, -0.4512711864406790396, 7.052569299041220319 ) ) ;
#9040=CARTESIAN_POINT ( 'NONE',  ( 2.578017356471871135, -5.386440677966105817, 5.329826563567761077 ) ) ;
#9051=CARTESIAN_POINT ( 'NONE',  ( 2.169623098572349917, -2.658349832090280529, 5.611855963200990338 ) ) ;
#9056=CARTESIAN_POINT ( 'NONE',  ( 2.151546283159470274, -0.8884399221803740421, 3.746273477677459773 ) ) ;
#9058=CARTESIAN_POINT ( 'NONE',  ( -0.4735094604798580353, -4.567989471729919870, 7.005327412390699671 ) ) ;
#9059=CARTESIAN_POINT ( 'NONE',  ( -1.785776242921159884, -4.478677194936736328, 5.712869711683835838 ) ) ;
#9065=CARTESIAN_POINT ( 'NONE',  ( 2.012177589105479392, -0.08453389830508521718, 5.107213040360584877 ) ) ;
#9066=CARTESIAN_POINT ( 'NONE',  ( -0.2620510901103649815, -3.706322805063249959, 2.361180871966390260 ) ) ;
#9074=CARTESIAN_POINT ( 'NONE',  ( 0.07064654565475687875, -5.148728813559319661, 7.352897294663512717 ) ) ;
#9076=CARTESIAN_POINT ( 'NONE',  ( 2.088297318559229954, -0.3978813559322040283, 5.785136623276629919 ) ) ;
#9081=CARTESIAN_POINT ( 'NONE',  ( 2.043688444617268729, -4.102223705964154199, 4.504451070148833836 ) ) ;
#9082=CARTESIAN_POINT ( 'NONE',  ( 0.2469343877495150108, -0.004449152542373164231, 2.057675570509529539 ) ) ;
#9084=ORIENTED_EDGE ( 'NONE', *, *, #1335, .T. ) ;
#9085=CARTESIAN_POINT ( 'NONE',  ( 2.130266475405040882, -0.04449152542372925012, 3.117337770017949428 ) ) ;
#9088=CARTESIAN_POINT ( 'NONE',  ( -1.378221871957430178, -5.479872881355929870, 6.607619368096279366 ) ) ;
#9092=CARTESIAN_POINT ( 'NONE',  ( -1.661700935788390066, -0.2625000000000000111, 3.038299064211610112 ) ) ;
#9093=CARTESIAN_POINT ( 'NONE',  ( -1.233489123281609645, -4.637854336594775084, 7.049812391606588236 ) ) ;
#9096=CARTESIAN_POINT ( 'NONE',  ( -1.611907055891630192, -3.244397915657459830, 2.985210995296889713 ) ) ;
#9100=CARTESIAN_POINT ( 'NONE',  ( 1.353302556710500371, -4.036199717459260761, 6.243850391919140819 ) ) ;
#9104=CARTESIAN_POINT ( 'NONE',  ( -1.058024172752510594, -1.730659176918718956, 2.940600473883360433 ) ) ;
#9110=CARTESIAN_POINT ( 'NONE',  ( -1.769056124370508964, -1.684082600342149627, 2.721729512470790979 ) ) ;
#9117=CARTESIAN_POINT ( 'NONE',  ( -0.4360591020458099987, -5.291101694915250064, 2.387347919655840034 ) ) ;
#9125=CARTESIAN_POINT ( 'NONE',  ( -1.213493134184840727, -3.314262780522333696, 2.339799138571439396 ) ) ;
#9127=CARTESIAN_POINT ( 'NONE',  ( -2.603140590302631008, -1.726818300558751851, 5.216500493824310247 ) ) ;
#9130=CARTESIAN_POINT ( 'NONE',  ( 2.316639661709690046, -3.780028546288089597, 4.285359956977719875 ) ) ;
#9133=CARTESIAN_POINT ( 'NONE',  ( 2.531332855772549184, -2.635061543801990869, 5.497162258444460825 ) ) ;
#9141=CARTESIAN_POINT ( 'NONE',  ( 2.145694642186089851, -1.098034516774969882, 5.666819626392539888 ) ) ;
#9143=CARTESIAN_POINT ( 'NONE',  ( -1.750316316486840051, -5.559957627118639500, 3.126818518378589928 ) ) ;
#9152=CARTESIAN_POINT ( 'NONE',  ( -1.816660071039029933, -3.170692174432619748, 6.196159040268240936 ) ) ;
#9153=CARTESIAN_POINT ( 'NONE',  ( -1.889104232906369862, -5.555508474576269506, 3.296507079072529933 ) ) ;
#9155=CARTESIAN_POINT ( 'NONE',  ( 2.291237445532070094, -0.9350164987569499209, 4.162434510291790346 ) ) ;
#9156=CARTESIAN_POINT ( 'NONE',  ( -1.630481553867809907, -3.543304787045240101, 3.002862530617889547 ) ) ;
#9157=CARTESIAN_POINT ( 'NONE',  ( -1.750352751699820963, -1.913124606865061139, 3.627075451280493468 ) ) ;
#9158=CARTESIAN_POINT ( 'NONE',  ( 1.042222075699120287, -0.1245762711864410871, 6.468743694056166227 ) ) ;
#9160=CARTESIAN_POINT ( 'NONE',  ( 0.3743405594629510280, -0.4423728813559330009, 7.023440622744399953 ) ) ;
#9163=CARTESIAN_POINT ( 'NONE',  ( -1.580445181003969912, -0.5580508474576266753, 3.389704561770339630 ) ) ;
#9167=CARTESIAN_POINT ( 'NONE',  ( -1.669205944673819886, -3.147403886144329643, 6.359065158982450505 ) ) ;
#9173=CARTESIAN_POINT ( 'NONE',  ( 2.286166334984490067, -5.086440677966099777, 5.258525443163859947 ) ) ;
#9177=CARTESIAN_POINT ( 'NONE',  ( -2.155845792290839835, -0.5447033898305089217, 3.756158857535780271 ) ) ;
#9180=CARTESIAN_POINT ( 'NONE',  ( 0.5302109551885175742, -3.799475958216412153, 2.716624547488259989 ) ) ;
#9181=CARTESIAN_POINT ( 'NONE',  ( 1.128670402850170174, -0.1290254237288140371, 7.101865548313628373 ) ) ;
#9184=CARTESIAN_POINT ( 'NONE',  ( 1.596341326794969984, -0.3355932203389830337, 2.970780074643809776 ) ) ;
#9185=CARTESIAN_POINT ( 'NONE',  ( 2.458531667407859889, -0.3934322033898309257, 5.699238225248945966 ) ) ;
#9188=CARTESIAN_POINT ( 'NONE',  ( -2.318251751302029984, -5.533262711864409766, 4.294764266798999586 ) ) ;
#9190=CARTESIAN_POINT ( 'NONE',  ( 2.143090896833110381, -5.395338983050850246, 5.672454929438339732 ) ) ;
#9191=CARTESIAN_POINT ( 'NONE',  ( 0.2010642693393740188, -3.752899381639833720, 2.053740970237999619 ) ) ;
#9193=CARTESIAN_POINT ( 'NONE',  ( -0.8092638295168710361, -4.911779243796849492, 2.486823565593869745 ) ) ;
#9194=CARTESIAN_POINT ( 'NONE',  ( -2.169623098572329933, -2.941650167909710234, 5.611855963201049846 ) ) ;
#9197=CARTESIAN_POINT ( 'NONE',  ( 0.5133516189064986079, -4.152641158900696183, 6.687805814961351736 ) ) ;
#9200=CARTESIAN_POINT ( 'NONE',  ( 2.029711248330070994, -2.219713230972778728, 4.391497016172514201 ) ) ;
#9203=CARTESIAN_POINT ( 'NONE',  ( 1.097896950867359500, -0.7068739681193977331, 2.280088753565270743 ) ) ;
#9204=CARTESIAN_POINT ( 'NONE',  ( 0.04661003995938393929, -1.870388906648449812, 2.046522810126899294 ) ) ;
#9210=CARTESIAN_POINT ( 'NONE',  ( 2.000624272291700034, -5.064194915254235596, 4.239366054775996595 ) ) ;
#9217=CARTESIAN_POINT ( 'NONE',  ( -0.5137283630188880235, -5.462076271186444565, 6.687652957477222770 ) ) ;
#9218=CARTESIAN_POINT ( 'NONE',  ( 2.589141052314449354, -2.312866384125929820, 5.282633936723466483 ) ) ;
#9220=CARTESIAN_POINT ( 'NONE',  ( 2.567863625471588751, -2.495331814072259569, 4.029783546918046078 ) ) ;
#9225=CARTESIAN_POINT ( 'NONE',  ( -0.2365712905368979879, -3.407415933675480346, 2.358466376073659720 ) ) ;
#9226=CARTESIAN_POINT ( 'NONE',  ( 1.315859850362970151, -5.328211948015590060, 2.737664967889629875 ) ) ;
#9229=CARTESIAN_POINT ( 'NONE',  ( 2.494165244384159763, -2.472043525783979678, 3.793218093085234166 ) ) ;
#9232=CARTESIAN_POINT ( 'NONE',  ( 0.6493550500446280127, -0.3133474576271190193, 2.437955526623099889 ) ) ;
#9233=CARTESIAN_POINT ( 'NONE',  ( 0.6673090596498160165, -2.239160642901090181, 2.443133963569570355 ) ) ;
#9234=CARTESIAN_POINT ( 'NONE',  ( -1.791574935211209807, -0.4913135593220339659, 6.226029630577610163 ) ) ;
#9236=CARTESIAN_POINT ( 'NONE',  ( 1.932035991685901122, -5.338983050847455836, 2.884370051397200818 ) ) ;
#9247=CARTESIAN_POINT ( 'NONE',  ( -1.948278411993560111, -3.193980462720909852, 6.020210936496040333 ) ) ;
#9250=CARTESIAN_POINT ( 'NONE',  ( -0.6493550500446439999, -5.586652542372879005, 2.437955526623099889 ) ) ;
#9254=CARTESIAN_POINT ( 'NONE',  ( -1.741913176380149864, -1.959701183441629802, 3.117443785062560035 ) ) ;
#9256=CARTESIAN_POINT ( 'NONE',  ( 0.1824815401350060040, -4.498124606865050445, 7.046368721022729709 ) ) ;
#9257=CARTESIAN_POINT ( 'NONE',  ( -0.7368491673940088527, -2.076142624883081211, 2.783765372628170809 ) ) ;
#9259=CARTESIAN_POINT ( 'NONE',  ( -1.661700935788390066, -0.5625000000000000000, 3.038299064211610112 ) ) ;
#9261=CARTESIAN_POINT ( 'NONE',  ( 1.656536077435048604, -0.4969333835596383420, 3.061489489342141823 ) ) ;
#9263=CARTESIAN_POINT ( 'NONE',  ( 1.397172971746949877, -3.892629111369559691, 2.806153814454899642 ) ) ;
#9268=CARTESIAN_POINT ( 'NONE',  ( -1.803891155489809606, -4.781424942684489920, 3.188470185434129966 ) ) ;
#9270=CARTESIAN_POINT ( 'NONE',  ( 1.713314936023349944, -5.038983050847460454, 3.089913064446569546 ) ) ;
#9275=CARTESIAN_POINT ( 'NONE',  ( -0.4194839839382230595, -3.683034516774964295, 2.690289814463939777 ) ) ;
#9276=CARTESIAN_POINT ( 'NONE',  ( 2.130266475405040882, -0.04449152542372925012, 3.117337770017949428 ) ) ;
#9278=CARTESIAN_POINT ( 'NONE',  ( 1.057242234132090175, -0.3222457627118650025, 2.597442975781520058 ) ) ;
#9280=CARTESIAN_POINT ( 'NONE',  ( 1.596341326794969984, -0.03559322033898330156, 2.970780074643809776 ) ) ;
#9282=CARTESIAN_POINT ( 'NONE',  ( -2.088297318559229954, -5.502118644067800268, 5.785136623276639689 ) ) ;
#9283=CARTESIAN_POINT ( 'NONE',  ( 0.6864473529425536569, -1.008722239981789892, 6.951118770549889803 ) ) ;
#9284=CARTESIAN_POINT ( 'NONE',  ( -1.661700935788390066, -0.5625000000000000000, 3.038299064211610112 ) ) ;
#9285=CARTESIAN_POINT ( 'NONE',  ( 2.524473153133520054, -0.6128213390808875394, 3.881373716577345867 ) ) ;
#9289=CARTESIAN_POINT ( 'NONE',  ( 2.028464043723889887, -0.7292627805223297344, 5.016599851465070259 ) ) ;
#9290=CARTESIAN_POINT ( 'NONE',  ( -1.447263454062130528, -4.661142624883069630, 6.924531903016462486 ) ) ;
#9294=CARTESIAN_POINT ( 'NONE',  ( 1.279347147864559275, -2.033406924666469884, 3.094331068408280760 ) ) ;
#9298=CARTESIAN_POINT ( 'NONE',  ( 0.2554393686801398333, -0.6247245358507580448, 2.048880876762550596 ) ) ;
#9299=CARTESIAN_POINT ( 'NONE',  ( 0.1110902655589990351, -2.638902420161969520, 7.351560417169478612 ) ) ;
#9302=CARTESIAN_POINT ( 'NONE',  ( 2.231116159141619981, -0.9117282104686620370, 3.951089877392439664 ) ) ;
#9304=CARTESIAN_POINT ( 'NONE',  ( -2.011500846714319835, -5.251059322033900578, 3.478373409938470218 ) ) ;
#9311=CARTESIAN_POINT ( 'NONE',  ( 2.332582362116870200, -5.368644067796609853, 4.387643303570810005 ) ) ;
#9312=CARTESIAN_POINT ( 'NONE',  ( 1.963178672446078687, -3.640298816558361406, 2.914210764660420061 ) ) ;
#9316=CARTESIAN_POINT ( 'NONE',  ( 1.741913176380120110, -3.640298816558360073, 3.117443785062520067 ) ) ;
#9320=CARTESIAN_POINT ( 'NONE',  ( -1.597383073937548970, -2.006277760018210898, 2.580688553303291943 ) ) ;
#9324=CARTESIAN_POINT ( 'NONE',  ( -0.5902886515192680150, -1.447358841099289917, 6.978224088050050788 ) ) ;
#9326=CARTESIAN_POINT ( 'NONE',  ( 1.670747152266691016, -0.4963810343603142217, 3.047345280935851441 ) ) ;
#9327=CARTESIAN_POINT ( 'NONE',  ( -1.549742865090599997, -5.484322033898309634, 6.471102547561460305 ) ) ;
#9331=CARTESIAN_POINT ( 'NONE',  ( 1.641808337277749663, -5.113135593220338393, 6.386111670537620633 ) ) ;
#9336=CARTESIAN_POINT ( 'NONE',  ( 2.075124426334590044, -2.681638120378570189, 5.810227140144509583 ) ) ;
#9338=CARTESIAN_POINT ( 'NONE',  ( 1.925796468768800063, -5.404237288135590234, 6.052706598917719560 ) ) ;
#9340=CARTESIAN_POINT ( 'NONE',  ( 1.167621112247380077, -2.821367850108300157, 6.743381174846749815 ) ) ;
#9342=CARTESIAN_POINT ( 'NONE',  ( -2.021195349941399044, -1.819971453711898945, 4.339901124684693912 ) ) ;
#9345=CARTESIAN_POINT ( 'NONE',  ( -0.5198535559317755128, -0.5906145504024216120, 2.087183161631441131 ) ) ;
#9358=CARTESIAN_POINT ( 'NONE',  ( -2.088297318559229954, -5.202118644067800446, 5.785136623276639689 ) ) ;
#9364=CARTESIAN_POINT ( 'NONE',  ( -2.650521604678268694, -4.595118636378185073, 4.833599835830360014 ) ) ;
#9366=CARTESIAN_POINT ( 'NONE',  ( -1.881914957835490121, -1.936412895153350133, 3.286797332666350435 ) ) ;
#9368=CARTESIAN_POINT ( 'NONE',  ( -2.519547246525518425, -0.2402542372881359412, 3.866491354109200529 ) ) ;
#9371=CARTESIAN_POINT ( 'NONE',  ( -1.869504824896970119, -0.5046610169491535514, 5.548311746956866131 ) ) ;
#9375=CARTESIAN_POINT ( 'NONE',  ( 1.428515267734870031, -0.03114406779661050076, 2.829745655876919841 ) ) ;
#9379=CARTESIAN_POINT ( 'NONE',  ( 1.713314936023349722, -5.038983050847458678, 3.089913064446569546 ) ) ;
#9383=CARTESIAN_POINT ( 'NONE',  ( -0.5889081234606770021, -5.462076271186440124, 6.978529000034869867 ) ) ;
#9387=CARTESIAN_POINT ( 'NONE',  ( 1.447263454062181598, -0.9388573751169233539, 6.924531903016430512 ) ) ;
#9391=CARTESIAN_POINT ( 'NONE',  ( 2.091095264232530226, -3.943046564306110113, 5.779845490516200002 ) ) ;
#9392=CARTESIAN_POINT ( 'NONE',  ( -1.940935473245981147, -5.095857339597785973, 2.893832807158200016 ) ) ;
#9396=CARTESIAN_POINT ( 'NONE',  ( -0.6217226704572171858, -4.292370888630430592, 6.656620240022991908 ) ) ;
#9399=CARTESIAN_POINT ( 'NONE',  ( 1.951270856817530319, -2.336154672414218592, 5.338313313320885989 ) ) ;
#9406=CARTESIAN_POINT ( 'NONE',  ( 1.118481890237429610, -0.4076464065212261345, 2.289482119763390333 ) ) ;
#9407=CARTESIAN_POINT ( 'NONE',  ( -2.635341251434490495, -3.011515032774579215, 5.013193520829514860 ) ) ;
#9411=CARTESIAN_POINT ( 'NONE',  ( -3.421358338620380043E-15, -5.299999999999999822, 2.350000000000000089 ) ) ;
#9419=CARTESIAN_POINT ( 'NONE',  ( 1.791574935211219799, -5.408686440677969998, 6.226029630577610163 ) ) ;
#9420=AXIS2_PLACEMENT_3D ( 'NONE', #16826, #13871, #2847 ) ;
#9422=CARTESIAN_POINT ( 'NONE',  ( -0.06913820924137326074, -4.222506023765566496, 7.352985789827153340 ) ) ;
#9426=CARTESIAN_POINT ( 'NONE',  ( 1.586727176531399941, -3.617010528270069969, 2.961885344765599726 ) ) ;
#9430=CARTESIAN_POINT ( 'NONE',  ( 2.445954350973281510, -2.658349832090279197, 5.729767452368150771 ) ) ;
#9436=CARTESIAN_POINT ( 'NONE',  ( -2.199335452462570117, -1.866548030288480042, 3.862342996790939953 ) ) ;
#9437=CARTESIAN_POINT ( 'NONE',  ( -0.006659065580996091117, -5.255540550750799511, 2.241023775284449737 ) ) ;
#9439=CARTESIAN_POINT ( 'NONE',  ( -2.116444151961480280, -5.546610169491529518, 3.670839500609359707 ) ) ;
#9442=CARTESIAN_POINT ( 'NONE',  ( -0.5889081234606770021, -5.162076271186438525, 6.978529000034869867 ) ) ;
#9444=CARTESIAN_POINT ( 'NONE',  ( -0.007508403481306110717, -0.5690018372754820364, 2.444053578789350034 ) ) ;
#9446=CARTESIAN_POINT ( 'NONE',  ( -2.351999299633229956, -3.333710192450639820, 4.782734406438290620 ) ) ;
#9448=CARTESIAN_POINT ( 'NONE',  ( -0.7983658734557950165, -5.466525423728810118, 6.913847129767330735 ) ) ;
#9451=CARTESIAN_POINT ( 'NONE',  ( -1.507201387235980183, -3.124115597856050197, 6.507509243627219497 ) ) ;
#9453=CARTESIAN_POINT ( 'NONE',  ( -1.951437470830620136, -5.057043525783970317, 3.384463041838880137 ) ) ;
#9454=CARTESIAN_POINT ( 'NONE',  ( 2.025702773739959106, -2.518620102360551893, 4.366188503657621567 ) ) ;
#9459=CARTESIAN_POINT ( 'NONE',  ( -1.282210379528740063, -4.661142624883069630, 6.673494927815290190 ) ) ;
#9463=CARTESIAN_POINT ( 'NONE',  ( -2.331386066015260106, -4.641695212954759953, 4.378465089518192244 ) ) ;
#9464=CARTESIAN_POINT ( 'NONE',  ( 1.477796163681079911, -5.117584745762710163, 6.531563725478140015 ) ) ;
#9467=CARTESIAN_POINT ( 'NONE',  ( -0.1824815401349519917, -1.101875393134939873, 7.046368721022739479 ) ) ;
#9471=CARTESIAN_POINT ( 'NONE',  ( -1.802718065953990978, -5.033755237495684653, 3.717600174934233781 ) ) ;
#9472=CARTESIAN_POINT ( 'NONE',  ( -2.431060148753501515, -0.2447033898305090438, 3.635668498923334102 ) ) ;
#9474=CARTESIAN_POINT ( 'NONE',  ( -1.254903241568450900, -0.1735169491525429541, 7.038391080368498365 ) ) ;
#9480=( LENGTH_UNIT ( ) NAMED_UNIT ( * ) SI_UNIT ( .MILLI., .METRE. ) );
#9481=CARTESIAN_POINT ( 'NONE',  ( -2.253200202764409799, -5.511016949152540256, 5.379408587037509903 ) ) ;
#9482=CARTESIAN_POINT ( 'NONE',  ( -2.107551805806941125, -1.311469987729540376, 6.312866726931216199 ) ) ;
#9486=CARTESIAN_POINT ( 'NONE',  ( -1.936998685628559924, -4.758136654396199816, 3.363294429306559863 ) ) ;
#9488=CARTESIAN_POINT ( 'NONE',  ( 2.471388659209138972, -4.218665147405589622, 5.667135868497455320 ) ) ;
#9493=CARTESIAN_POINT ( 'NONE',  ( 2.032257487115179728, -1.028169651910100679, 4.991258216523873692 ) ) ;
#9501=CARTESIAN_POINT ( 'NONE',  ( 1.647941990407678636, -0.3444915254237289615, 3.475676388127089123 ) ) ;
#9503=CARTESIAN_POINT ( 'NONE',  ( -2.619177996481920179, -3.081379897639443310, 4.272191262657214494 ) ) ;
#9506=CARTESIAN_POINT ( 'NONE',  ( 1.949083719010301197, -5.359745762711870753, 4.055210292801453953 ) ) ;
#9512=CARTESIAN_POINT ( 'NONE',  ( -2.318251751302029984, -5.533262711864409766, 4.294764266798999586 ) ) ;
#9513=CARTESIAN_POINT ( 'NONE',  ( 0.6672256841321406728, -4.152641158900696183, 7.268642361138727637 ) ) ;
#9514=CARTESIAN_POINT ( 'NONE',  ( 0.009452039534068971960, -5.000193177104105047, 2.350000000173209536 ) ) ;
#9515=CARTESIAN_POINT ( 'NONE',  ( -2.161103922260861232, -3.496728210468663889, 3.159628768708461877 ) ) ;
#9518=CARTESIAN_POINT ( 'NONE',  ( 1.886482464143609095, -0.5895330507926000996, 3.890008792968652429 ) ) ;
#9519=CARTESIAN_POINT ( 'NONE',  ( 1.534924416212170017, -5.333856471232000018, 2.911460733964629899 ) ) ;
#9523=CARTESIAN_POINT ( 'NONE',  ( 2.353194804772640314, -0.3756355932203400139, 4.731327187377229571 ) ) ;
#9524=CARTESIAN_POINT ( 'NONE',  ( 1.480680413335799805, -1.214475958216410190, 6.529298007719799735 ) ) ;
#9525=CARTESIAN_POINT ( 'NONE',  ( -2.234315482767910144, -0.5402542372881360411, 3.960850823455329905 ) ) ;
#9531=CARTESIAN_POINT ( 'NONE',  ( 1.943632316591229481, -5.046398305084738745, 3.373048379518160722 ) ) ;
#9535=CARTESIAN_POINT ( 'NONE',  ( -0.6864473529425049181, -4.591277760018209975, 6.951118770549909343 ) ) ;
#9542=CARTESIAN_POINT ( 'NONE',  ( -2.159566522375440112, -3.240557039297490061, 5.635424033751089468 ) ) ;
#9544=CARTESIAN_POINT ( 'NONE',  ( -2.041954431566909367, -1.750106588847040845, 4.912894203848660268 ) ) ;
#9546=CARTESIAN_POINT ( 'NONE',  ( -0.8244235255442939891, -0.5829339996946389935, 2.492493020344019872 ) ) ;
#9554=CARTESIAN_POINT ( 'NONE',  ( 2.351526912647309953, -5.073093220338979137, 4.606040641882800379 ) ) ;
#9558=CARTESIAN_POINT ( 'NONE',  ( -1.728413393879669968, -1.288181699441249828, 6.297289212178331042 ) ) ;
#9560=CARTESIAN_POINT ( 'NONE',  ( 1.803891155489780074, -0.8185750573155089471, 3.188470185434109982 ) ) ;
#9561=CARTESIAN_POINT ( 'NONE',  ( 2.353194804772640314, -0.07563559322033940047, 4.731327187377229571 ) ) ;
#9563=CARTESIAN_POINT ( 'NONE',  ( 2.180207327701309872, -0.3934322033898309812, 5.586116916730190063 ) ) ;
#9564=CARTESIAN_POINT ( 'NONE',  ( -2.050059171113549183, -0.5224576271186435195, 4.809263467226075228 ) ) ;
#9566=CARTESIAN_POINT ( 'NONE',  ( -2.431060148753501515, -0.2447033898305090438, 3.635668498923334102 ) ) ;
#9570=CARTESIAN_POINT ( 'NONE',  ( -0.3949552299395130417, -1.823812330071880261, 2.379923265530350385 ) ) ;
#9571=CARTESIAN_POINT ( 'NONE',  ( -0.1641805561540918557, -0.5962015548080631389, 2.650681144176719961 ) ) ;
#9572=CARTESIAN_POINT ( 'NONE',  ( -2.293791554891330353, -4.777584066324515710, 6.034778631725542297 ) ) ;
#9574=CARTESIAN_POINT ( 'NONE',  ( -0.009452110982656879157, -5.299807955295460005, 2.350000000000000089 ) ) ;
#9575=CARTESIAN_POINT ( 'NONE',  ( 0.5902886515193200845, -4.152641158900699736, 6.978224088050040130 ) ) ;
#9576=CARTESIAN_POINT ( 'NONE',  ( 1.940935473245969156, -0.5041426604022095637, 2.893832807158179143 ) ) ;
#9580=CARTESIAN_POINT ( 'NONE',  ( 1.945780800405119360, -0.9117282104686613708, 4.045142061754263274 ) ) ;
#9586=CARTESIAN_POINT ( 'NONE',  ( 2.589141052314449354, -2.312866384125929820, 5.282633936723466483 ) ) ;
#9588=CARTESIAN_POINT ( 'NONE',  ( -0.8298945877350979439, -5.211074464177370302, 2.494426474263899962 ) ) ;
#9589=CARTESIAN_POINT ( 'NONE',  ( 1.432215783582721613, -5.413135593220339992, 6.170863372171116801 ) ) ;
#9598=CARTESIAN_POINT ( 'NONE',  ( 2.043308330018790198, -5.399788135593220240, 5.867646457774659652 ) ) ;
#9599=CARTESIAN_POINT ( 'NONE',  ( -2.022685914314908739, -4.432100618360157007, 6.418096442297106741 ) ) ;
#9600=CARTESIAN_POINT ( 'NONE',  ( -1.650842931266140790, -3.566593075333521767, 2.622060802311461547 ) ) ;
#9602=CARTESIAN_POINT ( 'NONE',  ( -0.7205524543785096769, -1.171740257999810852, 6.622421910798247602 ) ) ;
#9607=CARTESIAN_POINT ( 'NONE',  ( 0.1565249325564390115, -0.4468220338983060480, 7.048192310558509810 ) ) ;
#9608=CARTESIAN_POINT ( 'NONE',  ( -2.137408332595969629, -3.450151633892079683, 3.714996798363980002 ) ) ;
#9611=CARTESIAN_POINT ( 'NONE',  ( 1.031876288691629506, -5.430932203389830626, 7.145012538880298081 ) ) ;
#9616=CARTESIAN_POINT ( 'NONE',  ( 0.7093417302541467073, -5.135381355932199021, 6.943956659919690466 ) ) ;
#9620=CARTESIAN_POINT ( 'NONE',  ( -2.036228139452650243, -3.473439922180369788, 3.519948877554409883 ) ) ;
#9622=CARTESIAN_POINT ( 'NONE',  ( 1.319613955262860072, -5.028306595106929677, 2.740497729816110173 ) ) ;
#9625=CARTESIAN_POINT ( 'NONE',  ( 1.353103843060669886, -2.798079561820010053, 6.625579309552930063 ) ) ;
#9627=CARTESIAN_POINT ( 'NONE',  ( -1.883235269974520287, -3.240557039297494057, 5.517512544583926370 ) ) ;
#9636=CARTESIAN_POINT ( 'NONE',  ( 0.05465110135556765225, -5.148728813559319661, 6.752241303418941243 ) ) ;
#9638=CARTESIAN_POINT ( 'NONE',  ( -1.152986057740030379, -1.753947465207011058, 2.309657588616440549 ) ) ;
#9647=CARTESIAN_POINT ( 'NONE',  ( -0.1569242594330230167, -1.400782264522720144, 7.048216443236290374 ) ) ;
#9648=CARTESIAN_POINT ( 'NONE',  ( 1.707817112497189926, -0.1112288135593230004, 6.319218296629480314 ) ) ;
#9650=CARTESIAN_POINT ( 'NONE',  ( -2.332582362116870200, -0.5313559322033900578, 4.387643303570819775 ) ) ;
#9652=CARTESIAN_POINT ( 'NONE',  ( -2.304156201936080617, -0.2002118644067801267, 6.016707707703351282 ) ) ;
#9656=CARTESIAN_POINT ( 'NONE',  ( 0.09706517602699295255, -2.638902420161969076, 7.051451474958978061 ) ) ;
#9658=CARTESIAN_POINT ( 'NONE',  ( 1.851400890972779045, -5.413135593220339992, 6.601359968904126241 ) ) ;
#9661=CARTESIAN_POINT ( 'NONE',  ( -0.4985810152601130585, -4.269082600342140488, 7.000035360316470445 ) ) ;
#9663=CARTESIAN_POINT ( 'NONE',  ( 0.4500319419456214609, -4.474836318576761229, 7.315451193241913508 ) ) ;
#9667=CARTESIAN_POINT ( 'NONE',  ( -2.052909741356249373, -1.773394877135329839, 4.721527574705180363 ) ) ;
#9674=CARTESIAN_POINT ( 'NONE',  ( -2.051331987628511211, -0.2269067796610169385, 4.618035453557344461 ) ) ;
#9675=CARTESIAN_POINT ( 'NONE',  ( -1.428323476796611535, -3.290974492234041815, 2.463260019887531627 ) ) ;
#9677=CARTESIAN_POINT ( 'NONE',  ( 0.009452110982653675123, -5.000192044704546035, 2.649999999999998579 ) ) ;
#9678=CARTESIAN_POINT ( 'NONE',  ( -0.9222751404131093178, -5.277754237288146300, 2.865854510788139908 ) ) ;
#9681=FACE_OUTER_BOUND ( 'NONE', #10885, .T. ) ;
#9685=CARTESIAN_POINT ( 'NONE',  ( -2.116444151961480280, -5.546610169491529518, 3.670839500609359707 ) ) ;
#9687=CARTESIAN_POINT ( 'NONE',  ( 2.161802606005190253, -0.5895330507925999886, 3.769755311421790545 ) ) ;
#9688=CARTESIAN_POINT ( 'NONE',  ( -2.409576349373780513, -3.450151633892079239, 3.587770028483140194 ) ) ;
#9690=CARTESIAN_POINT ( 'NONE',  ( -1.704669856830349994, -4.796950468210010143, 3.080704711052660194 ) ) ;
#9700=CARTESIAN_POINT ( 'NONE',  ( -1.943632316591239917, -0.5536016949152539057, 3.373048379518170048 ) ) ;
#9701=CARTESIAN_POINT ( 'NONE',  ( -1.286937324407759986, -3.589881363621809651, 2.729584305145209999 ) ) ;
#9704=CARTESIAN_POINT ( 'NONE',  ( -0.9664230948142090716, -5.582203389830510787, 2.228384861502259895 ) ) ;
#9713=CARTESIAN_POINT ( 'NONE',  ( -1.777964140657649850, -4.731007489747940831, 6.241943319976260618 ) ) ;
#9716=CARTESIAN_POINT ( 'NONE',  ( 0.2270348434643680025, -5.304612347394249916, 2.348896311281980065 ) ) ;
#9720=CARTESIAN_POINT ( 'NONE',  ( 2.353452300571019506, -4.125511994252439862, 4.697179287168359529 ) ) ;
#9723=CARTESIAN_POINT ( 'NONE',  ( -1.652654650382402668, -4.804713230972782689, 3.029252778805632484 ) ) ;
#9725=CARTESIAN_POINT ( 'NONE',  ( 0.1526488871098231337, -3.752899381639833720, 2.652660223633551251 ) ) ;
#9726=CARTESIAN_POINT ( 'NONE',  ( -0.2812789908084309953, -0.4557203389830509765, 7.036533610117280624 ) ) ;
#9740=CARTESIAN_POINT ( 'NONE',  ( -0.1365430262726299304, -5.153177966101685215, 6.748423079423377047 ) ) ;
#9741=CARTESIAN_POINT ( 'NONE',  ( -2.607432201095288615, -1.521064582324129777, 4.205620581240213873 ) ) ;
#9747=CARTESIAN_POINT ( 'NONE',  ( 2.231116159141619981, -0.9117282104686620370, 3.951089877392439664 ) ) ;
#9748=CARTESIAN_POINT ( 'NONE',  ( -0.2993653819235400082, -2.685478996738538626, 6.731079075450757898 ) ) ;
#9749=CARTESIAN_POINT ( 'NONE',  ( 0.9222751404130974384, -0.02224576271186471527, 2.865854510788131027 ) ) ;
#9750=CARTESIAN_POINT ( 'NONE',  ( -1.112838723655040107, -0.4735169491525429986, 6.773667561836210105 ) ) ;
#9753=CARTESIAN_POINT ( 'NONE',  ( 0.7983658734558030101, -0.1334745762711870010, 6.913847129767330735 ) ) ;
#9754=CARTESIAN_POINT ( 'NONE',  ( 1.644832646965660006, -1.191187669928119863, 6.383232381746459794 ) ) ;
#9759=CARTESIAN_POINT ( 'NONE',  ( -1.567709126316399804, -1.684082600342149627, 2.944712621036611022 ) ) ;
#9760=CARTESIAN_POINT ( 'NONE',  ( -2.601107615185130673, -5.515466101694915579, 5.226397344856384741 ) ) ;
#9763=CARTESIAN_POINT ( 'NONE',  ( -2.182690844914350059, -1.680241723982170088, 5.580117243900479806 ) ) ;
#9766=CARTESIAN_POINT ( 'NONE',  ( 2.052786957354850728, -0.3756355932203404024, 4.727327971967373976 ) ) ;
#9771=CARTESIAN_POINT ( 'NONE',  ( -2.013199450439951299, -1.726818300558751851, 5.102405038955014405 ) ) ;
#9776=CARTESIAN_POINT ( 'NONE',  ( 2.012177589105479392, -0.3845338983050847759, 5.107213040360584877 ) ) ;
#9777=CARTESIAN_POINT ( 'NONE',  ( -0.7540633504678314614, -3.360839357098899693, 2.155495695330209127 ) ) ;
#9780=CARTESIAN_POINT ( 'NONE',  ( -1.505092429369619955, -5.128627060139309357, 2.879659483602799774 ) ) ;
#9781=CARTESIAN_POINT ( 'NONE',  ( 1.795861365445541091, -5.350847457627126325, 3.705232155007893713 ) ) ;
#9783=CARTESIAN_POINT ( 'NONE',  ( 0.2189795514005130062, -0.004449152542373159026, 2.356806637999009801 ) ) ;
#9788=CARTESIAN_POINT ( 'NONE',  ( -2.516451517878150135, -4.688271789531334832, 3.857037693030694214 ) ) ;
#9791=CARTESIAN_POINT ( 'NONE',  ( -1.974086094277271108, -1.404623140882690580, 5.263813741415750869 ) ) ;
#9796=CARTESIAN_POINT ( 'NONE',  ( 1.610878918935058524, -0.3311440677966099311, 2.590989782159081933 ) ) ;
#9797=CARTESIAN_POINT ( 'NONE',  ( -0.3159454637156809409, -2.984385868126319785, 7.032150113402090064 ) ) ;
#9800=CARTESIAN_POINT ( 'NONE',  ( -0.4917262214559124933, -5.591101694915256104, 2.092115739186370948 ) ) ;
#9809=CARTESIAN_POINT ( 'NONE',  ( 2.426866425021050766, -0.8884399221803740421, 3.626019996130599665 ) ) ;
#9810=CARTESIAN_POINT ( 'NONE',  ( 0.5637478356992829953, -0.6606104644819250638, 2.398845082743519708 ) ) ;
#9811=CARTESIAN_POINT ( 'NONE',  ( 0.2570708662023959423, -5.304612347394245475, 2.048876625919409111 ) ) ;
#9814=CARTESIAN_POINT ( 'NONE',  ( -2.135041058613629694, -4.800872354612799597, 5.690123914223820023 ) ) ;
#9816=CARTESIAN_POINT ( 'NONE',  ( 1.333132471082870918, -2.774791273531719060, 6.261300629978916454 ) ) ;
#9817=CARTESIAN_POINT ( 'NONE',  ( -1.477796163681079911, -0.4824152542372879826, 6.531563725478150673 ) ) ;
#9830=EDGE_CURVE ( 'NONE', #13175, #11001, #648, .T. ) ;
#9831=CARTESIAN_POINT ( 'NONE',  ( 1.795861365445541091, -5.050847457627124726, 3.705232155007893713 ) ) ;
#9832=EDGE_CURVE ( 'NONE', #10555, #12628, #18080, .T. ) ;
#9838=CARTESIAN_POINT ( 'NONE',  ( 2.023259452208809872, -2.425466949207399914, 3.497849062500220096 ) ) ;
#9839=CARTESIAN_POINT ( 'NONE',  ( -2.025702773739959106, -3.081379897639443310, 4.366188503657674858 ) ) ;
#9840=CARTESIAN_POINT ( 'NONE',  ( 1.392553072310509510, -0.03559322033898333626, 3.191531554476519261 ) ) ;
#9843=CARTESIAN_POINT ( 'NONE',  ( 1.549742865090599997, -0.4156779661016959948, 6.471102547561449647 ) ) ;
#9846=CARTESIAN_POINT ( 'NONE',  ( 1.707817112497189926, -0.1112288135593230004, 6.319218296629480314 ) ) ;
#9847=CARTESIAN_POINT ( 'NONE',  ( 1.704669856830330010, -0.8030495317899829510, 3.080704711052640210 ) ) ;
#9852=CARTESIAN_POINT ( 'NONE',  ( 2.159566522375459652, -2.359442960702510028, 5.635424033751040618 ) ) ;
#9853=CARTESIAN_POINT ( 'NONE',  ( -1.057242234132100167, -5.577754237288139905, 2.597442975781530272 ) ) ;
#9856=CARTESIAN_POINT ( 'NONE',  ( 1.704669856830330010, -0.8030495317899829510, 3.080704711052640210 ) ) ;
#9857=CARTESIAN_POINT ( 'NONE',  ( -1.679950111053631900, -0.4957627118644069575, 5.880020650119711867 ) ) ;
#9862=CARTESIAN_POINT ( 'NONE',  ( -2.041954431566909367, -1.750106588847040845, 4.912894203848660268 ) ) ;
#9864=CARTESIAN_POINT ( 'NONE',  ( 2.230812463554230352, -0.4023305084745772420, 6.137473736419911674 ) ) ;
#9868=CARTESIAN_POINT ( 'NONE',  ( 2.052786957354850728, -0.3756355932203404024, 4.727327971967373976 ) ) ;
#9871=CARTESIAN_POINT ( 'NONE',  ( -2.046424002475610404, -5.228813559322024851, 4.536201610417774255 ) ) ;
#9875=CARTESIAN_POINT ( 'NONE',  ( 2.351526912647309953, -5.373093220338979847, 4.606040641882800379 ) ) ;
#9879=CARTESIAN_POINT ( 'NONE',  ( 0.4735094604799090501, -1.032010528270079996, 7.005327412390689901 ) ) ;
#9881=CARTESIAN_POINT ( 'NONE',  ( 1.503462833636809881, -0.5041426604022095637, 3.304888304972889657 ) ) ;
#9886=CARTESIAN_POINT ( 'NONE',  ( -2.224278379903029901, -0.5091101694915259879, 5.468825643806110470 ) ) ;
#9887=CARTESIAN_POINT ( 'NONE',  ( -0.7435598031058080482, -3.030962444702889780, 6.932904947974540377 ) ) ;
#9890=CARTESIAN_POINT ( 'NONE',  ( -0.9002849211310044453, -5.466525423728811006, 7.196465912290821443 ) ) ;
#9893=CARTESIAN_POINT ( 'NONE',  ( -1.596341326794980198, -5.264406779661019442, 2.970780074643820878 ) ) ;
#9897=B_SPLINE_CURVE_WITH_KNOTS ( 'NONE', 3,
 ( #8281, #9847, #6882, #4952, #13921, #2186, #9302, #1238, #4098, #7829, #792, #5488, #12099, #2280, #8372, #13476, #17719, #15503, #9754, #5051, #6968, #15419, #2725, #16880, #12616, #5591, #6430, #11236, #4188, #3561, #2812, #10704, #16347, #2908, #123, #1520, #5860, #10118, #11506, #17136, #7079, #4275, #8722, #7172, #5771, #10031, #1788, #14367, #392, #5947, #213, #1692, #15690, #12810, #11414, #3000, #9934, #15591, #11678, #8553, #8817, #8641, #11328, #7252, #11586, #308, #1421, #15771, #14468, #1607, #4539, #12723, #8453, #7345, #7432, #14288, #13074, #17302, #6031, #17046, #4630, #12894, #3079, #17217, #10191, #4461, #4370, #12987, #15855, #10290, #3161, #15957, #14200, #14088, #39, #5683, #16965, #16119, #3521, #16039, #13251, #11782, #9167, #7696, #849, #17670, #14922, #17405, #14828, #14630, #570, #4809, #2233, #2141, #13531, #746, #13342, #7786, #10458, #1945, #7600, #13433, #3258, #3417, #6380, #10751, #9066, #14726, #6118, #2041, #12049, #5008, #14548, #10553, #9263, #655, #10662, #1864, #8902, #16307, #7879, #6213, #3613, #3338, #6293, #11870, #6488, #11953, #17567, #4901, #12148, #4725, #17768, #5100, #16214, #7512, #10375, #13157, #8983, #474, #17489, #2434, #12420, #3980, #8162, #12507, #6582, #9459, #2609, #15396, #2514, #3701, #15206, #17949, #16758, #8349, #15021, #5193, #6945, #8259, #2697, #12236, #13898, #17854, #13720, #1034, #18042, #6672 ),
 .UNSPECIFIED., .F., .F.,
 ( 4, 1, 1, 1, 1, 1, 1, 1, 1, 1, 1, 1, 1, 1, 1, 1, 1, 1, 1, 1, 1, 1, 1, 1, 1, 1, 1, 1, 1, 1, 1, 1, 1, 1, 1, 1, 1, 1, 1, 1, 1, 1, 1, 1, 1, 1, 1, 1, 1, 1, 1, 1, 1, 1, 1, 1, 1, 1, 1, 1, 1, 1, 1, 1, 1, 1, 1, 1, 1, 1, 1, 1, 1, 1, 1, 1, 1, 1, 1, 1, 1, 1, 1, 1, 1, 1, 1, 1, 1, 1, 1, 1, 1, 1, 1, 1, 1, 1, 1, 1, 1, 1, 1, 1, 1, 1, 1, 1, 1, 1, 1, 1, 1, 1, 1, 1, 1, 1, 1, 1, 1, 1, 1, 1, 1, 1, 1, 1, 1, 1, 1, 1, 1, 1, 1, 1, 1, 1, 1, 1, 1, 1, 1, 1, 1, 1, 1, 1, 1, 1, 1, 1, 1, 1, 1, 1, 1, 1, 1, 1, 1, 1, 1, 1, 1, 1, 1, 1, 1, 1, 1, 1, 1, 1, 1, 1, 1, 1, 1, 1, 1, 1, 1, 1, 1, 4 ),
 ( 0.7853981633974479459, 0.8787968639095770085, 0.9721955644217059600, 1.065594264933839908, 1.158992965445959866, 1.252391665958090039, 1.345790366470219990, 1.439189066982349940, 1.532587767494480113, 1.625986468006610064, 1.719385168518740015, 1.812783869030869965, 1.906182569543000138, 1.999581270055129867, 2.092979970567249826, 2.186378671079379998, 2.279777371591510171, 2.373176072103639900, 2.466574772615769628, 2.559973473127900245, 2.653372173640029974, 2.746770874152160147, 2.840169574664289875, 2.933568275176409834, 3.026966975688540007, 3.120365676200670180, 3.213764376712799908, 3.307163077224930081, 3.400561777737059810, 3.493960478249190427, 3.587359178761320155, 3.680757879273439670, 3.774156579785570287, 3.867555280297700016, 3.960953980809830188, 4.054352681321960361, 4.147751381834090090, 4.241150082346219818, 4.334548782858350435, 4.427947483370480164, 4.521346183882600123, 4.614744884394729851, 4.708143584906859580, 4.801542285418989309, 4.894940985931119926, 4.988339686443250542, 5.081738386955380271, 5.175137087467510000, 5.268535787979639728, 5.361934488491760575, 5.455333189003890304, 5.548731889516020033, 5.642130590028149761, 5.735529290540279490, 5.828927991052410107, 5.922326691564539836, 6.015725392076670452, 6.109124092588789523, 6.202522793100920140, 6.295921493613049869, 6.389320194125180485, 6.482718894637310214, 6.576117595149439943, 6.669516295661569671, 6.762914996173699400, 6.856313696685830017, 6.949712397197949976, 7.043111097710079704, 7.136509798222209433, 7.229908498734340050, 7.323307199246470667, 7.416705899758600395, 7.510104600270730124, 7.603503300782859853, 7.696902001294989581, 7.790300701807110428, 7.883699402319240157, 7.977098102831369886, 8.070496803343500503, 8.163895503855631119, 8.257294204367759960, 8.350692904879890577, 8.444091605392019417, 8.537490305904137600, 8.630889006416269993, 8.724287706928398833, 8.817686407440529450, 8.911085107952660067, 9.004483808464788908, 9.097882508976921301, 9.191281209489050141, 9.284679910001178982, 9.378078610513298941, 9.471477311025429557, 9.564876011537560174, 9.658274712049690791, 9.751673412561819632, 9.845072113073950248, 9.938470813586080865, 10.03186951409819905, 10.12526821461029947, 10.21866691512249936, 10.31206561563459978, 10.40546431614669842, 10.49886301665890009, 10.59226171717100051, 10.68566041768310093, 10.77905911819519957, 10.87245781870739947, 10.96585651921949989, 11.05925521973160031, 11.15265392024380020, 11.24605262075590062, 11.33945132126800104, 11.43285002178009968, 11.52624872229229958, 11.61964742280439999, 11.71304612331650041, 11.80644482382869853, 11.89984352434079895, 11.99324222485290115, 12.08664092536500156, 12.18003962587719968, 12.27343832638930010, 12.36683702690140052, 12.46023572741360042, 12.55363442792569906, 12.64703312843779948, 12.74043182894989990, 12.83383052946209979, 12.92722922997419843, 13.02062793048630063, 13.11402663099850052, 13.20742533151059916, 13.30082403202269958, 13.39422273253480000, 13.48762143304700167, 13.58102013355910032, 13.67441883407120073, 13.76781753458340063, 13.86121623509549927, 13.95461493560759969, 14.04801363611970011, 14.14141233663190000, 14.23481103714399865, 14.32820973765609907, 14.42160843816829896, 14.51500713868040116, 14.60840583919249980, 14.70180453970460022, 14.79520324021680011, 14.88860194072889875, 14.98200064124100095, 15.07539934175320084, 15.16879804226530126, 15.26219674277739990, 15.35559544328959980, 15.44899414380170022, 15.54239284431380064, 15.63579154482589928, 15.72919024533809740, 15.82258894585020137, 15.91598764636230001, 16.00938634687449991, 16.10278504738660033, 16.19618374789870074, 16.28958244841080116, 16.38298114892299751, 16.47637984943510148, 16.56977854994720545, 16.66317725045940179, 16.75657595097149866, 16.84997465148359908, 16.94337335199570305, 17.03677205250789939, 17.13017075301999981, 17.22356945353210023, 17.31696815404430012, 17.41036685455640054, 17.50376555506850096, 17.59716425558059782, 17.69056295609280127, 17.78396165660489814, 17.87736035711699856, 17.97075905762920200, 18.06415775814129887 ),
 .UNSPECIFIED. ) ;
#9898=CARTESIAN_POINT ( 'NONE',  ( 2.316126390218360420, -0.8651516338920848259, 3.404364157709320438 ) ) ;
#9900=CARTESIAN_POINT ( 'NONE',  ( 0.2735655355027601376, -5.004947479095214646, 2.050775599341920330 ) ) ;
#9902=CARTESIAN_POINT ( 'NONE',  ( -2.353452300571019506, -1.474488005747550012, 4.697179287168410156 ) ) ;
#9904=CARTESIAN_POINT ( 'NONE',  ( 1.869848057046569867, -4.288530012270459935, 6.129130480762009725 ) ) ;
#9906=CARTESIAN_POINT ( 'NONE',  ( 1.181710496343130190, -2.798079561820010941, 6.378827610405712001 ) ) ;
#9910=CARTESIAN_POINT ( 'NONE',  ( 0.009452110982654814836, -0.3001920447045380858, 2.649999999999998579 ) ) ;
#9916=CARTESIAN_POINT ( 'NONE',  ( -1.202278654260740876, -5.179872881355935377, 6.364093491318035589 ) ) ;
#9923=CARTESIAN_POINT ( 'NONE',  ( 0.2365712905368450025, -2.192584066324519743, 2.358466376073659720 ) ) ;
#9924=CARTESIAN_POINT ( 'NONE',  ( -0.9361665894546699063, -3.314262780522333696, 2.872845392579789880 ) ) ;
#9927=CARTESIAN_POINT ( 'NONE',  ( 1.489797906646480596, -0.1112288135593229726, 6.112509577910826941 ) ) ;
#9932=CARTESIAN_POINT ( 'NONE',  ( 2.287919158821199783, -1.051457940198389895, 5.251517552016890633 ) ) ;
#9934=CARTESIAN_POINT ( 'NONE',  ( -0.8429265834919730249, -2.076142624883080323, 2.502678798553459760 ) ) ;
#9937=CARTESIAN_POINT ( 'NONE',  ( 1.917298190932609003, -2.103271789531340641, 3.335187436117900805 ) ) ;
#9939=CARTESIAN_POINT ( 'NONE',  ( 1.467041701146838406, -5.422033898305085309, 6.911479965439912831 ) ) ;
#9943=CARTESIAN_POINT ( 'NONE',  ( -1.994315313497099229, -0.5135593220338985354, 5.187224322759965922 ) ) ;
#9949=CARTESIAN_POINT ( 'NONE',  ( 1.712910428781929006, -2.704926408666860738, 5.831741890007691609 ) ) ;
#9960=CARTESIAN_POINT ( 'NONE',  ( -1.364983921886200546, -4.865515740159335856, 2.403349116468209257 ) ) ;
#9961=CARTESIAN_POINT ( 'NONE',  ( -0.5137283630188880235, -5.462076271186444565, 6.687652957477222770 ) ) ;
#9963=CARTESIAN_POINT ( 'NONE',  ( 2.340070819011249803, -0.08008474576271228107, 4.950151441910538352 ) ) ;
#9964=CARTESIAN_POINT ( 'NONE',  ( 1.300961508564179914, -5.422033898305079092, 6.661123742937279602 ) ) ;
#9970=CARTESIAN_POINT ( 'NONE',  ( -1.869848057046539891, -1.311469987729539932, 6.129130480762059463 ) ) ;
#9974=CARTESIAN_POINT ( 'NONE',  ( -2.048006021857541548, -3.058091609351150986, 4.556566471620694614 ) ) ;
#9979=CARTESIAN_POINT ( 'NONE',  ( 1.733739193136930146, -5.074965191738780135, 2.966260806863060040 ) ) ;
#9980=CARTESIAN_POINT ( 'NONE',  ( 0.4917262214558945632, -0.008898305084746043966, 2.092115739186370948 ) ) ;
#9984=CARTESIAN_POINT ( 'NONE',  ( 1.661700935788380074, -5.037500000000000533, 3.038299064211610112 ) ) ;
#9988=CARTESIAN_POINT ( 'NONE',  ( -2.011500846714318502, -5.251059322033899690, 3.478373409938471550 ) ) ;
#9992=CARTESIAN_POINT ( 'NONE',  ( -2.296954468777729463, -4.963890372630819670, 4.187412587068699565 ) ) ;
#9995=CARTESIAN_POINT ( 'NONE',  ( 1.732245706108171746, -5.033893599512585304, 2.684512698446369861 ) ) ;
#9996=CARTESIAN_POINT ( 'NONE',  ( 1.630481553867769939, -2.056695212954759988, 3.002862530617850023 ) ) ;
#10000=CARTESIAN_POINT ( 'NONE',  ( 0.6096110657044089276, -3.799475958216410376, 2.426869991387509806 ) ) ;
#10002=CARTESIAN_POINT ( 'NONE',  ( 1.909909196654749897, -4.032358841099289215, 3.946907241329673521 ) ) ;
#10016=CARTESIAN_POINT ( 'NONE',  ( -3.421358338620380043E-15, -5.299999999999999822, 2.350000000000000089 ) ) ;
#10024=CARTESIAN_POINT ( 'NONE',  ( 0.8748826269292639957, -2.262448931189380286, 2.515205712983200392 ) ) ;
#10025=CARTESIAN_POINT ( 'NONE',  ( 1.842787987253230897, -3.710163681423226389, 3.794994874786191907 ) ) ;
#10026=CARTESIAN_POINT ( 'NONE',  ( 1.549742865090599997, -0.4156779661016959948, 6.471102547561449647 ) ) ;
#10030=CARTESIAN_POINT ( 'NONE',  ( 1.088937603231269646, -0.02669491525423760975, 2.959627624143540192 ) ) ;
#10031=CARTESIAN_POINT ( 'NONE',  ( -2.316639661709700260, -1.819971453711900056, 4.285359956977770501 ) ) ;
#10036=CARTESIAN_POINT ( 'NONE',  ( 0.6343239990445398435, -3.500569086828631438, 2.433641963034071765 ) ) ;
#10038=CARTESIAN_POINT ( 'NONE',  ( -2.386628511786350160, -5.546610169491530407, 3.539457309197792778 ) ) ;
#10040=CARTESIAN_POINT ( 'NONE',  ( -1.630481553867809907, -3.543304787045240101, 3.002862530617889547 ) ) ;
#10042=CARTESIAN_POINT ( 'NONE',  ( -0.7982439214406890082, -0.4690677966101705065, 6.591424794228156081 ) ) ;
#10047=CARTESIAN_POINT ( 'NONE',  ( -1.642659730162759901, -1.936412895153350133, 3.468508687188699646 ) ) ;
#10054=CARTESIAN_POINT ( 'NONE',  ( 2.234315482767910144, -5.359745762711869865, 3.960850823455320580 ) ) ;
#10056=CARTESIAN_POINT ( 'NONE',  ( -2.143090896833109493, -0.2046610169491529518, 5.672454929438351279 ) ) ;
#10064=CARTESIAN_POINT ( 'NONE',  ( -2.262450597846770162, -1.404623140882689913, 5.348122657979730299 ) ) ;
#10068=CARTESIAN_POINT ( 'NONE',  ( 1.798783563193339985, -2.382731248990799244, 5.689585537188965425 ) ) ;
#10073=CARTESIAN_POINT ( 'NONE',  ( -1.943632316591239917, -0.5536016949152539057, 3.373048379518170048 ) ) ;
#10074=CARTESIAN_POINT ( 'NONE',  ( -0.7998959936908373036, -0.4646186440677965712, 7.230419212249866945 ) ) ;
#10075=CARTESIAN_POINT ( 'NONE',  ( 0.8242394280877100021, -4.428259742000189902, 6.904399023015010073 ) ) ;
#10078=CARTESIAN_POINT ( 'NONE',  ( 2.293398556041700065, -5.064194915254240037, 4.171956209133470317 ) ) ;
#10086=CARTESIAN_POINT ( 'NONE',  ( 2.306572132003631648, -1.121322805063259542, 6.012569500204132389 ) ) ;
#10087=CARTESIAN_POINT ( 'NONE',  ( 1.307725206348619995, -0.7471169921413569615, 2.732408283416570161 ) ) ;
#10089=CARTESIAN_POINT ( 'NONE',  ( 2.237394498046680003, -2.336154672414219924, 5.429939413646329704 ) ) ;
#10091=CARTESIAN_POINT ( 'NONE',  ( 1.571912189623089873, -4.335106588847041031, 6.451524409078630562 ) ) ;
#10093=CARTESIAN_POINT ( 'NONE',  ( -0.03076623656502111559, -4.521412895153344103, 6.752792069673816400 ) ) ;
#10095=CARTESIAN_POINT ( 'NONE',  ( -1.641808337277740115, -0.4868644067796619734, 6.386111670537629514 ) ) ;
#10103=ORIENTED_EDGE ( 'NONE', *, *, #6297, .T. ) ;
#10104=CARTESIAN_POINT ( 'NONE',  ( 1.869504824896970119, -5.395338983050850246, 5.548311746956850143 ) ) ;
#10105=CARTESIAN_POINT ( 'NONE',  ( 2.121170185508189476, -3.663587104846653730, 3.105085978143951486 ) ) ;
#10108=CARTESIAN_POINT ( 'NONE',  ( -1.485788269501200132, -4.829629811528119099, 2.863981322975839738 ) ) ;
#10111=CARTESIAN_POINT ( 'NONE',  ( 1.832842064134690085, -2.728214696955149954, 6.176291182464479945 ) ) ;
#10112=CARTESIAN_POINT ( 'NONE',  ( -1.764143222953850065, -3.174533050792599731, 3.649904513135073802 ) ) ;
#10113=CARTESIAN_POINT ( 'NONE',  ( 2.041338374031088865, -0.08008474576271226719, 4.918217215283659627 ) ) ;
#10116=CARTESIAN_POINT ( 'NONE',  ( -1.630703155447540631, -3.267686203945749490, 2.606218513833090000 ) ) ;
#10117=CARTESIAN_POINT ( 'NONE',  ( -1.811729841638700211, -0.2580508474576269640, 3.197954009834299782 ) ) ;
#10118=CARTESIAN_POINT ( 'NONE',  ( -1.981271652668300298, -1.633665147405599871, 5.970160748022450115 ) ) ;
#10121=CARTESIAN_POINT ( 'NONE',  ( 1.417709711196429412, -3.593722239981790523, 2.821478011237760430 ) ) ;
#10123=CARTESIAN_POINT ( 'NONE',  ( 2.508228811380011081, -5.090889830508485758, 5.566973598334535644 ) ) ;
#10125=CARTESIAN_POINT ( 'NONE',  ( -2.050059171113549183, -0.5224576271186435195, 4.809263467226075228 ) ) ;
#10128=CARTESIAN_POINT ( 'NONE',  ( 2.039016451601951108, -2.588484967225421762, 4.939402908764060740 ) ) ;
#10134=CARTESIAN_POINT ( 'NONE',  ( -1.614765845140348821, -5.493220338983046069, 5.967758800287426446 ) ) ;
#10140=CARTESIAN_POINT ( 'NONE',  ( -1.214457691476030110, -1.730659176918720066, 2.684103622926369948 ) ) ;
#10142=CARTESIAN_POINT ( 'NONE',  ( -1.181710496343089556, -2.801920438179980710, 6.378827610405741311 ) ) ;
#10148=CARTESIAN_POINT ( 'NONE',  ( -2.043014502273419186, -0.5580508474576266753, 3.006203457898251052 ) ) ;
#10150=CARTESIAN_POINT ( 'NONE',  ( 2.262450597846779932, -4.195376859117310175, 5.348122657979680561 ) ) ;
#10154=CARTESIAN_POINT ( 'NONE',  ( -0.1765068388402301069, -5.153177966101685215, 7.347961541693647902 ) ) ;
#10162=CARTESIAN_POINT ( 'NONE',  ( 0.2620510901103109691, -1.893677194936739916, 2.361180871966390260 ) ) ;
#10163=CARTESIAN_POINT ( 'NONE',  ( -0.009452110982655139229, -5.299807955295460005, 2.350000000000000089 ) ) ;
#10164=CARTESIAN_POINT ( 'NONE',  ( 1.668426559427239608, -1.214475958216409746, 6.763847501342977075 ) ) ;
#10167=CARTESIAN_POINT ( 'NONE',  ( -1.934380261529029754, -4.824160642901089702, 5.387804366397155320 ) ) ;
#10176=CARTESIAN_POINT ( 'NONE',  ( -0.1910247150515231307, -5.295550847457634269, 2.655937705488500722 ) ) ;
#10178=CARTESIAN_POINT ( 'NONE',  ( 1.700860513939579599, -2.475884402143949892, 6.737200825918507441 ) ) ;
#10183=CARTESIAN_POINT ( 'NONE',  ( -0.7435598031058080482, -3.030962444702889780, 6.932904947974540377 ) ) ;
#10184=CARTESIAN_POINT ( 'NONE',  ( 0.3257255101953561716, -4.175929447188994281, 6.727018681373227338 ) ) ;
#10189=CARTESIAN_POINT ( 'NONE',  ( -0.8001094918299070935, -4.292370888630430592, 7.230402832373842514 ) ) ;
#10190=CARTESIAN_POINT ( 'NONE',  ( 1.489797906646480596, -0.1112288135593229726, 6.112509577910826941 ) ) ;
#10191=CARTESIAN_POINT ( 'NONE',  ( 1.832842064134690085, -2.728214696955149954, 6.176291182464479945 ) ) ;
#10195=CARTESIAN_POINT ( 'NONE',  ( 1.881914957835459701, -3.663587104846650178, 3.286797332666310467 ) ) ;
#10197=CARTESIAN_POINT ( 'NONE',  ( 1.851400890972779045, -5.113135593220339281, 6.601359968904126241 ) ) ;
#10204=CARTESIAN_POINT ( 'NONE',  ( 0.2993653819235879698, -2.914521003261450360, 6.731079075450741911 ) ) ;
#10205=CARTESIAN_POINT ( 'NONE',  ( 2.601107615185130673, -0.3845338983050847759, 5.226397344856369642 ) ) ;
#10210=CARTESIAN_POINT ( 'NONE',  ( 1.202278654260740876, -0.4201271186440683758, 6.364093491318035589 ) ) ;
#10216=CARTESIAN_POINT ( 'NONE',  ( 0.1565249325564389560, -0.1468220338983060036, 7.048192310558507145 ) ) ;
#10217=CARTESIAN_POINT ( 'NONE',  ( 0.009452110982654818305, -0.3001920447045379747, 2.350000000000000089 ) ) ;
#10218=CARTESIAN_POINT ( 'NONE',  ( -1.011820239713360658, -3.636457940198391636, 2.246566997958110434 ) ) ;
#10220=CARTESIAN_POINT ( 'NONE',  ( -0.6673090596498669758, -3.360839357098900138, 2.443133963569589895 ) ) ;
#10223=CARTESIAN_POINT ( 'NONE',  ( 0.9976707306414894783, -2.522460978720530989, 6.494311833503137343 ) ) ;
#10229=CARTESIAN_POINT ( 'NONE',  ( 0.2908063684825958894, -1.055298816558370101, 7.337905485238597869 ) ) ;
#10233=CARTESIAN_POINT ( 'NONE',  ( -1.128670402850159737, -5.170974576271189171, 7.101865548313641696 ) ) ;
#10242=CARTESIAN_POINT ( 'NONE',  ( -2.197904923864619331, -3.193980462720909408, 6.187389538303117220 ) ) ;
#10248=CARTESIAN_POINT ( 'NONE',  ( -1.526791597786389953, -2.825208726468269926, 6.490992212270280781 ) ) ;
#10251=CARTESIAN_POINT ( 'NONE',  ( -1.930452136971070987, -1.587088570829020551, 6.521117305355617511 ) ) ;
#10253=CARTESIAN_POINT ( 'NONE',  ( 1.224086244040949900, -4.358394877135324030, 6.348185277745746369 ) ) ;
#10268=CARTESIAN_POINT ( 'NONE',  ( -0.06367493584607197832, -5.298516949152545230, 2.649999999999998579 ) ) ;
#10269=CARTESIAN_POINT ( 'NONE',  ( -0.3752419433106839453, -1.424070552810999812, 7.023346545710370314 ) ) ;
#10270=CARTESIAN_POINT ( 'NONE',  ( -2.065789008932981119, -2.871785303044851023, 6.366022047745341084 ) ) ;
#10278=CARTESIAN_POINT ( 'NONE',  ( 1.704669856830330010, -0.8030495317899829510, 3.080704711052640210 ) ) ;
#10280=CARTESIAN_POINT ( 'NONE',  ( -2.325590009395030133, -4.870737219477670799, 5.061077271074069905 ) ) ;
#10282=CARTESIAN_POINT ( 'NONE',  ( 1.043047520545210105, -4.082776294035843634, 6.468319459971126228 ) ) ;
#10289=CARTESIAN_POINT ( 'NONE',  ( -0.4339619423229766348, -0.1601694915254239793, 6.706578715862737461 ) ) ;
#10290=CARTESIAN_POINT ( 'NONE',  ( 0.9719602541832789155, -2.844656138396589817, 6.843370931913530519 ) ) ;
#10296=CARTESIAN_POINT ( 'NONE',  ( -1.115198193348239997, -4.338947465207011689, 6.772457159276568994 ) ) ;
#10299=CARTESIAN_POINT ( 'NONE',  ( -0.2469343877495291661, -5.595550847457635868, 2.057675570509529539 ) ) ;
#10304=CARTESIAN_POINT ( 'NONE',  ( -0.7093417302541390468, -0.4646186440677970153, 6.943956659919700236 ) ) ;
#10309=CARTESIAN_POINT ( 'NONE',  ( -1.668733558229350766, -4.754295778036219389, 5.895922302771936074 ) ) ;
#10310=CARTESIAN_POINT ( 'NONE',  ( 0.1765068388402390998, -0.4468220338983063811, 7.347961541693647902 ) ) ;
#10311=ORIENTED_EDGE ( 'NONE', *, *, #11047, .T. ) ;
#10317=CARTESIAN_POINT ( 'NONE',  ( -0.009452110982655708218, -0.5998079552954630467, 2.350000000000000089 ) ) ;
#10318=CARTESIAN_POINT ( 'NONE',  ( -0.1910247150515231307, -5.595550847457635868, 2.655937705488500722 ) ) ;
#10320=CARTESIAN_POINT ( 'NONE',  ( -0.7093417302541388247, -0.1646186440677969709, 6.943956659919700236 ) ) ;
#10321=CARTESIAN_POINT ( 'NONE',  ( 2.248786803694151182, -4.265241723982168942, 6.109280527266637506 ) ) ;
#10325=CARTESIAN_POINT ( 'NONE',  ( -2.211317922628890376, -3.127956474216019966, 3.894507149290469705 ) ) ;
#10328=CARTESIAN_POINT ( 'NONE',  ( 2.051695471449629160, -2.266289807549351387, 4.773807418740724451 ) ) ;
#10332=CARTESIAN_POINT ( 'NONE',  ( 2.622715975066190364, -0.7292627805223297344, 5.105554690682975405 ) ) ;
#10335=CARTESIAN_POINT ( 'NONE',  ( 0.4005155088302400634, -4.474836318576759453, 7.019123328904770531 ) ) ;
#10344=CARTESIAN_POINT ( 'NONE',  ( 0.9880847989278174204, -2.262448931189378509, 2.236912075639679198 ) ) ;
#10345=CARTESIAN_POINT ( 'NONE',  ( 1.545075033357670158, -0.4774152569121719591, 2.920238509828300355 ) ) ;
#10348=CARTESIAN_POINT ( 'NONE',  ( -1.832842064134660109, -2.871785303044850135, 6.176291182464519913 ) ) ;
#10349=CARTESIAN_POINT ( 'NONE',  ( 1.661700935788380074, -5.337500000000000355, 3.038299064211610112 ) ) ;
#10350=CARTESIAN_POINT ( 'NONE',  ( -0.9038768003981948462, -1.470647129387581575, 7.195219513931347954 ) ) ;
#10352=CARTESIAN_POINT ( 'NONE',  ( -1.668733558229350766, -4.754295778036219389, 5.895922302771936074 ) ) ;
#10362=CARTESIAN_POINT ( 'NONE',  ( 2.352760675243219968, -2.565196678937129882, 4.757121734156020132 ) ) ;
#10363=CARTESIAN_POINT ( 'NONE',  ( 2.350067830300900162, -5.377542372881360500, 4.825253242917690422 ) ) ;
#10364=CARTESIAN_POINT ( 'NONE',  ( -3.763524982345449879E-15, -5.450000000000000178, 2.350000000000000089 ) ) ;
#10365=CARTESIAN_POINT ( 'NONE',  ( -2.182690844914350059, -1.680241723982170088, 5.580117243900479806 ) ) ;
#10367=CARTESIAN_POINT ( 'NONE',  ( 2.313035575219750228, -4.172088570829020071, 5.134294963419709923 ) ) ;
#10368=CARTESIAN_POINT ( 'NONE',  ( 2.033547680391670998, -0.9583047870452394701, 4.417890669792418734 ) ) ;
#10374=CARTESIAN_POINT ( 'NONE',  ( 1.846259792136599076, -0.3533898305084745561, 3.802221692020924415 ) ) ;
#10375=CARTESIAN_POINT ( 'NONE',  ( 1.026235786675480099, -4.404971453711899798, 6.817920158464540137 ) ) ;
#10382=CARTESIAN_POINT ( 'NONE',  ( -2.276802572547989456, -3.104668185927729862, 4.104251954998811236 ) ) ;
#10384=CARTESIAN_POINT ( 'NONE',  ( -0.9664230948142090716, -5.582203389830510787, 2.228384861502259895 ) ) ;
#10390=CARTESIAN_POINT ( 'NONE',  ( 1.909909196654749897, -4.032358841099289215, 3.946907241329673521 ) ) ;
#10392=CARTESIAN_POINT ( 'NONE',  ( 2.458531667407859889, -0.09343220338983100615, 5.699238225248945966 ) ) ;
#10394=CARTESIAN_POINT ( 'NONE',  ( 0.6493550500446280127, -0.3133474576271190193, 2.437955526623099889 ) ) ;
#10402=CARTESIAN_POINT ( 'NONE',  ( -2.049607015837349167, -3.170692174432623744, 6.385889905549041679 ) ) ;
#10404=CARTESIAN_POINT ( 'NONE',  ( -0.01716182025094739952, -3.430704221963770006, 2.346608583467349796 ) ) ;
#10407=CARTESIAN_POINT ( 'NONE',  ( -1.785776242921159884, -4.478677194936736328, 5.712869711683835838 ) ) ;
#10409=CARTESIAN_POINT ( 'NONE',  ( -2.043688444617268729, -1.497776294035840561, 4.504451070148879133 ) ) ;
#10414=CARTESIAN_POINT ( 'NONE',  ( -2.369027826908540302, -1.590929447188999646, 3.503830760997904470 ) ) ;
#10417=CARTESIAN_POINT ( 'NONE',  ( 1.571912189623089873, -4.335106588847041031, 6.451524409078630562 ) ) ;
#10420=CARTESIAN_POINT ( 'NONE',  ( -2.180207327701300102, -5.206567796610169552, 5.586116916730199833 ) ) ;
#10427=CARTESIAN_POINT ( 'NONE',  ( -2.260671505268489145, -1.913124606865061139, 3.309864021662289435 ) ) ;
#10428=CARTESIAN_POINT ( 'NONE',  ( 1.118481890237429610, -0.4076464065212261345, 2.289482119763390333 ) ) ;
#10431=CARTESIAN_POINT ( 'NONE',  ( 0.1569242594330760021, -4.199217735477280833, 7.048216443236290374 ) ) ;
#10432=CARTESIAN_POINT ( 'NONE',  ( 1.340185291429730974, -5.033893599512585304, 3.140995886557053307 ) ) ;
#10433=CARTESIAN_POINT ( 'NONE',  ( 2.626509418457480649, -1.028169651910100679, 5.080213055741780614 ) ) ;
#10436=CARTESIAN_POINT ( 'NONE',  ( 2.306642602145299925, -0.3845338983050849979, 5.166805192608480368 ) ) ;
#10438=CARTESIAN_POINT ( 'NONE',  ( -1.707817112497179934, -5.488771186440679628, 6.319218296629480314 ) ) ;
#10446=CARTESIAN_POINT ( 'NONE',  ( -2.005512128484160161, -1.913124606865060029, 3.468469736471389897 ) ) ;
#10451=CARTESIAN_POINT ( 'NONE',  ( 1.214457691475989920, -3.869340823081270031, 2.684103622926340194 ) ) ;
#10452=CARTESIAN_POINT ( 'NONE',  ( 1.292934267244360447, -1.214475958216409746, 6.294748514096617065 ) ) ;
#10457=CARTESIAN_POINT ( 'NONE',  ( 1.526871680339569659, -0.3400423728813561364, 3.327650196883443101 ) ) ;
#10458=CARTESIAN_POINT ( 'NONE',  ( -1.781655196750479897, -3.520016498756949996, 3.162323035427820450 ) ) ;
#10466=CARTESIAN_POINT ( 'NONE',  ( -2.268288188848061715, -5.251059322033895249, 3.322421079292323665 ) ) ;
#10474=CARTESIAN_POINT ( 'NONE',  ( 1.835037444103841286, -4.241953435693877061, 5.620619042473564697 ) ) ;
#10476=CARTESIAN_POINT ( 'NONE',  ( 2.601107615185130673, -0.08453389830508521718, 5.226397344856369642 ) ) ;
#10478=CARTESIAN_POINT ( 'NONE',  ( 1.428515267734870031, -0.3311440677966109858, 2.829745655876919841 ) ) ;
#10480=CARTESIAN_POINT ( 'NONE',  ( -1.932035991685910004, -0.5610169491525425212, 2.884370051397200818 ) ) ;
#10484=CARTESIAN_POINT ( 'NONE',  ( -0.1698804968610999888, -0.2965485159365569556, 2.349238660949160007 ) ) ;
#10485=CARTESIAN_POINT ( 'NONE',  ( -2.197904923864619331, -3.193980462720909408, 6.187389538303117220 ) ) ;
#10488=CARTESIAN_POINT ( 'NONE',  ( -2.126557263589650137, -3.151244762504310071, 3.691783806836059778 ) ) ;
#10491=ADVANCED_FACE ( 'NONE', ( #2510 ), #7713, .T. ) ;
#10492=CARTESIAN_POINT ( 'NONE',  ( 1.978802102381368888, -3.756740257999804378, 4.152967933079626306 ) ) ;
#10495=CARTESIAN_POINT ( 'NONE',  ( -0.5302109551885640926, -1.800524041783588824, 2.716624547488271979 ) ) ;
#10499=CARTESIAN_POINT ( 'NONE',  ( 0.5355577887186364627, -1.032010528270079330, 7.299286738308158107 ) ) ;
#10504=CARTESIAN_POINT ( 'NONE',  ( -0.2189795514005259958, -5.295550847457629828, 2.356806637999020015 ) ) ;
#10512=CARTESIAN_POINT ( 'NONE',  ( 2.445954350973281510, -2.658349832090279197, 5.729767452368150771 ) ) ;
#10517=CARTESIAN_POINT ( 'NONE',  ( 1.981271652668330052, -3.966334852594400662, 5.970160748022399488 ) ) ;
#10518=CARTESIAN_POINT ( 'NONE',  ( 0.9788656693287738353, -5.320452325212859712, 2.556357798777459944 ) ) ;
#10519=CARTESIAN_POINT ( 'NONE',  ( 1.923406176634910203, -0.8030495317899833951, 2.875176962145290727 ) ) ;
#10522=FACE_OUTER_BOUND ( 'NONE', #16086, .T. ) ;
#10523=CARTESIAN_POINT ( 'NONE',  ( 2.180207327701309872, -0.3934322033898309812, 5.586116916730190063 ) ) ;
#10535=CARTESIAN_POINT ( 'NONE',  ( -0.6343239990445920240, -2.099430913171359769, 2.433641963034089972 ) ) ;
#10537=CARTESIAN_POINT ( 'NONE',  ( -0.3743405594629430344, -5.457627118644070130, 7.023440622744399953 ) ) ;
#10542=CARTESIAN_POINT ( 'NONE',  ( 1.021156010535390068, -3.846052534792979927, 2.579625955254269964 ) ) ;
#10544=CARTESIAN_POINT ( 'NONE',  ( 1.538437905834991515, -2.378890372630820149, 3.340547664492009350 ) ) ;
#10551=CARTESIAN_POINT ( 'NONE',  ( 1.585619829032530070, -0.5482184015263239507, 3.126197263413850180 ) ) ;
#10553=CARTESIAN_POINT ( 'NONE',  ( 1.214457691475989920, -3.869340823081270031, 2.684103622926340194 ) ) ;
#10555=VERTEX_POINT ( 'NONE', #5660 ) ;
#10560=CARTESIAN_POINT ( 'NONE',  ( -2.329383452786330189, -4.571830348089889640, 5.035735636132877779 ) ) ;
#10562=CARTESIAN_POINT ( 'NONE',  ( -2.340070819011249803, -5.219915254237290192, 4.950151441910549899 ) ) ;
#10564=CARTESIAN_POINT ( 'NONE',  ( 2.180207327701309872, -0.3934322033898309812, 5.586116916730190063 ) ) ;
#10569=CARTESIAN_POINT ( 'NONE',  ( -1.124021676335500208, -3.589881363621813648, 2.982013645643241340 ) ) ;
#10571=CARTESIAN_POINT ( 'NONE',  ( 2.614198783383141045, -0.06673728813559372253, 4.243032045539284702 ) ) ;
#10575=CARTESIAN_POINT ( 'NONE',  ( 1.248294325655350034, -0.3266949152542379942, 2.704938983774300088 ) ) ;
#10577=CARTESIAN_POINT ( 'NONE',  ( 0.7322514394120266390, -0.01334745762711889508, 2.149183891723918993 ) ) ;
#10579=CARTESIAN_POINT ( 'NONE',  ( -1.248294325655370018, -5.573305084745760141, 2.704938983774309857 ) ) ;
#10582=CARTESIAN_POINT ( 'NONE',  ( -1.571912189623050127, -1.264893411152959501, 6.451524409078660760 ) ) ;
#10584=CARTESIAN_POINT ( 'NONE',  ( 1.925796468768800063, -5.404237288135590234, 6.052706598917719560 ) ) ;
#10585=CARTESIAN_POINT ( 'NONE',  ( 1.373536515609961484, -4.381683165423609694, 6.970795264502707589 ) ) ;
#10587=CARTESIAN_POINT ( 'NONE',  ( -0.1654173910288039839, -5.280843314568230085, 2.650679959339568459 ) ) ;
#10588=CARTESIAN_POINT ( 'NONE',  ( 1.236334101859160040, -3.570433951693499974, 2.697445712080689617 ) ) ;
#10592=CARTESIAN_POINT ( 'NONE',  ( 1.616473591439308688, -3.989623140882693875, 5.965667796385536903 ) ) ;
#10596=CARTESIAN_POINT ( 'NONE',  ( 1.423520578776751533, -2.056695212954759100, 3.220645071516909930 ) ) ;
#10601=CARTESIAN_POINT ( 'NONE',  ( 1.475946938622679783, -0.7471169921413568504, 2.482078242844649729 ) ) ;
#10602=CARTESIAN_POINT ( 'NONE',  ( -2.550815101416269659, -1.404623140882690580, 5.432431574543720387 ) ) ;
#10608=CARTESIAN_POINT ( 'NONE',  ( -1.750316316486840051, -5.259957627118650336, 3.126818518378589928 ) ) ;
#10618=CARTESIAN_POINT ( 'NONE',  ( -1.980638384804660257, -5.537711864406785978, 4.159858630563765480 ) ) ;
#10620=CARTESIAN_POINT ( 'NONE',  ( -1.428323476796611535, -3.290974492234041815, 2.463260019887531627 ) ) ;
#10621=CARTESIAN_POINT ( 'NONE',  ( 0.5843165771433389555, -0.3612150962701970447, 2.403837883145311327 ) ) ;
#10622=CARTESIAN_POINT ( 'NONE',  ( 2.398725280367429047, -2.448755237495690462, 3.564557036955152913 ) ) ;
#10626=CARTESIAN_POINT ( 'NONE',  ( 0.5902886515193200845, -4.152641158900699736, 6.978224088050040130 ) ) ;
#10629=CARTESIAN_POINT ( 'NONE',  ( 1.720450724489989813, -2.774791273531719060, 6.720683794561567836 ) ) ;
#10633=CARTESIAN_POINT ( 'NONE',  ( 0.2189795514005130062, -0.3044491525423729805, 2.356806637999009801 ) ) ;
#10634=CARTESIAN_POINT ( 'NONE',  ( -1.381042549632419902, -1.540511994252449890, 6.605640880016140137 ) ) ;
#10635=CARTESIAN_POINT ( 'NONE',  ( -2.155845792290839835, -0.5447033898305089217, 3.756158857535780271 ) ) ;
#10636=CARTESIAN_POINT ( 'NONE',  ( -1.494590226124049792, -0.2673043920988010802, 2.870965838437660622 ) ) ;
#10637=CARTESIAN_POINT ( 'NONE',  ( 2.519547246525509543, -5.359745762711870753, 3.866491354109194756 ) ) ;
#10641=ORIENTED_EDGE ( 'NONE', *, *, #12721, .T. ) ;
#10642=CARTESIAN_POINT ( 'NONE',  ( 2.286166334984490067, -5.086440677966098889, 5.258525443163859059 ) ) ;
#10649=CARTESIAN_POINT ( 'NONE',  ( -0.4201920264140019956, -2.122719201459649874, 2.384360920086639801 ) ) ;
#10651=CARTESIAN_POINT ( 'NONE',  ( 1.477796163681079911, -5.417584745762709986, 6.531563725478140015 ) ) ;
#10652=CARTESIAN_POINT ( 'NONE',  ( 0.7678268402137939930, -2.867944426684879922, 6.924676972266129660 ) ) ;
#10653=CARTESIAN_POINT ( 'NONE',  ( -1.286937324407759986, -3.589881363621809651, 2.729584305145209999 ) ) ;
#10654=CARTESIAN_POINT ( 'NONE',  ( 2.048006021857541548, -2.541908390648840665, 4.556566471620634218 ) ) ;
#10657=CARTESIAN_POINT ( 'NONE',  ( 0.07299321914061039640, -0.3014830508474579673, 2.350000000000000089 ) ) ;
#10662=CARTESIAN_POINT ( 'NONE',  ( 1.724579595320000047, -3.939205687946140344, 3.098572228637889836 ) ) ;
#10669=CARTESIAN_POINT ( 'NONE',  ( -0.4917262214559124933, -5.291101694915254505, 2.092115739186370948 ) ) ;
#10675=CARTESIAN_POINT ( 'NONE',  ( 1.831349212334668852, -4.009070552811004440, 3.772065786216904026 ) ) ;
#10676=CARTESIAN_POINT ( 'NONE',  ( -1.873832970144350130, -0.5625000000000005551, 2.826167029855650270 ) ) ;
#10678=CARTESIAN_POINT ( 'NONE',  ( 2.270487904532159984, -0.3622881355932209835, 4.080813552109670894 ) ) ;
#10679=CARTESIAN_POINT ( 'NONE',  ( 0.07299321914061039640, -0.001483050847457899942, 2.350000000000000089 ) ) ;
#10682=CARTESIAN_POINT ( 'NONE',  ( -0.7983658734557950165, -5.466525423728810118, 6.913847129767330735 ) ) ;
#10685=CARTESIAN_POINT ( 'NONE',  ( 2.286166334984490067, -5.386440677966100488, 5.258525443163859947 ) ) ;
#10686=CARTESIAN_POINT ( 'NONE',  ( -1.447263454062130528, -4.661142624883069630, 6.924531903016462486 ) ) ;
#10688=CARTESIAN_POINT ( 'NONE',  ( -0.1881942810071039751, -5.280843314568230085, 2.350674491507239949 ) ) ;
#10689=CARTESIAN_POINT ( 'NONE',  ( 2.353343516942209668, -3.826605122864669806, 4.722803042560139275 ) ) ;
#10690=CARTESIAN_POINT ( 'NONE',  ( -2.006003143955999324, -4.731007489747939054, 6.437545705712661714 ) ) ;
#10693=CARTESIAN_POINT ( 'NONE',  ( 0.1781895581254300809, -3.453992510252061887, 2.654724878163539969 ) ) ;
#10696=CARTESIAN_POINT ( 'NONE',  ( -2.016543577558690625, -1.521064582324129777, 4.314702916654059806 ) ) ;
#10700=CARTESIAN_POINT ( 'NONE',  ( 0.6575972843460591299, -0.3612150962701959900, 2.110392115010549130 ) ) ;
#10701=CARTESIAN_POINT ( 'NONE',  ( 2.574214976178930137, -2.196424942684489956, 4.054607910322744146 ) ) ;
#10704=CARTESIAN_POINT ( 'NONE',  ( -1.003115764947269950, -1.493935417675869903, 6.828967930617589666 ) ) ;
#10705=CARTESIAN_POINT ( 'NONE',  ( -2.116444151961480280, -5.246610169491529696, 3.670839500609359707 ) ) ;
#10711=CARTESIAN_POINT ( 'NONE',  ( -1.549742865090599997, -5.484322033898309634, 6.471102547561460305 ) ) ;
#10712=CARTESIAN_POINT ( 'NONE',  ( 2.623186471072028514, -2.219713230972778728, 4.297499775172036962 ) ) ;
#10716=CARTESIAN_POINT ( 'NONE',  ( -0.4539185741479770386, -3.384127645387189798, 2.390735265170449875 ) ) ;
#10720=CARTESIAN_POINT ( 'NONE',  ( 1.818868030982612183, -2.355602084342530933, 2.767428454397789839 ) ) ;
#10726=CARTESIAN_POINT ( 'NONE',  ( -0.8001898266890440370, -1.470647129387580021, 6.913242401714570384 ) ) ;
#10729=CARTESIAN_POINT ( 'NONE',  ( 2.650076489488250697, -5.377542372881360500, 4.841243018609314497 ) ) ;
#10736=CARTESIAN_POINT ( 'NONE',  ( -0.7435598031058080482, -3.030962444702889780, 6.932904947974540377 ) ) ;
#10742=CARTESIAN_POINT ( 'NONE',  ( 2.337178851518220135, -2.588484967225419986, 4.976298214796759822 ) ) ;
#10744=CARTESIAN_POINT ( 'NONE',  ( -0.5549238885286955636, -2.099430913171361102, 2.723396519134838822 ) ) ;
#10746=CARTESIAN_POINT ( 'NONE',  ( 1.057242234132090175, -0.3222457627118650025, 2.597442975781520058 ) ) ;
#10747=CARTESIAN_POINT ( 'NONE',  ( -0.009452110982655708218, -0.5998079552954630467, 2.350000000000000089 ) ) ;
#10751=CARTESIAN_POINT ( 'NONE',  ( -0.4790341583531910197, -3.683034516774959855, 2.395814251711740006 ) ) ;
#10756=CARTESIAN_POINT ( 'NONE',  ( -2.231116159141639521, -4.688271789531330391, 3.951089877392499616 ) ) ;
#10759=CARTESIAN_POINT ( 'NONE',  ( -2.180207327701300102, -5.206567796610169552, 5.586116916730199833 ) ) ;
#10762=ORIENTED_EDGE ( 'NONE', *, *, #11912, .T. ) ;
#10763=CARTESIAN_POINT ( 'NONE',  ( -2.342931736853879787, -1.497776294035840117, 4.477701633099189671 ) ) ;
#10766=CARTESIAN_POINT ( 'NONE',  ( 0.7109160811436110450, -1.307629111369560171, 6.943511536198400336 ) ) ;
#10767=CARTESIAN_POINT ( 'NONE',  ( 1.428515267734870031, -0.03114406779661050076, 2.829745655876919841 ) ) ;
#10770=CARTESIAN_POINT ( 'NONE',  ( 1.128670402850170174, -0.1290254237288140371, 7.101865548313628373 ) ) ;
#10774=CARTESIAN_POINT ( 'NONE',  ( 2.058670345754650022, -5.350847457627120107, 3.559656372813920111 ) ) ;
#10775=CARTESIAN_POINT ( 'NONE',  ( 0.5355577887186364627, -1.032010528270079330, 7.299286738308158107 ) ) ;
#10777=CARTESIAN_POINT ( 'NONE',  ( -0.1458667720079689645, -4.981295943764795453, 2.649245313618650677 ) ) ;
#10778=CARTESIAN_POINT ( 'NONE',  ( -2.226511124464849889, -4.525253771513310319, 5.462491901673850236 ) ) ;
#10779=CARTESIAN_POINT ( 'NONE',  ( -2.622715975066178817, -4.870737219477664581, 5.105554690683034913 ) ) ;
#10783=CARTESIAN_POINT ( 'NONE',  ( 0.5549238885286489342, -3.500569086828633658, 2.723396519134821059 ) ) ;
#10786=CARTESIAN_POINT ( 'NONE',  ( 0.6050872056802326648, -1.940253771513320125, 2.738171435586128410 ) ) ;
#10790=CARTESIAN_POINT ( 'NONE',  ( 0.9724415447670879953, -0.7068739681193980662, 2.553509270169310064 ) ) ;
#10791=CARTESIAN_POINT ( 'NONE',  ( -2.494165244384181079, -3.127956474216021299, 3.793218093085275910 ) ) ;
#10795=CARTESIAN_POINT ( 'NONE',  ( 1.562863241354470523, -5.108686440677975504, 6.031217337312382298 ) ) ;
#10800=EDGE_LOOP ( 'NONE', ( #10311, #17055, #7370, #17550 ) ) ;
#10801=CARTESIAN_POINT ( 'NONE',  ( -1.851073041990159984, -5.493220338983049622, 6.153284478378270528 ) ) ;
#10802=CARTESIAN_POINT ( 'NONE',  ( 2.218077401483169897, -0.7758393570989060573, 5.486688202856499608 ) ) ;
#10804=CARTESIAN_POINT ( 'NONE',  ( -2.523518139275819916, -3.263845327585779277, 5.521565513971835593 ) ) ;
#10807=CARTESIAN_POINT ( 'NONE',  ( -2.322440385110939864, -3.081379897639439758, 4.319189883157439347 ) ) ;
#10810=CARTESIAN_POINT ( 'NONE',  ( -0.9490039995899379743, -2.076142624883081211, 2.221592224478750488 ) ) ;
#10813=CARTESIAN_POINT ( 'NONE',  ( 1.750316316486830059, -0.3400423728813560253, 3.126818518378580158 ) ) ;
#10814=CARTESIAN_POINT ( 'NONE',  ( -2.340959815966380031, -1.750106588847040179, 4.942183458383479611 ) ) ;
#10815=CARTESIAN_POINT ( 'NONE',  ( 0.005141112625543309625, -5.068517718233539249, 2.221989741495029591 ) ) ;
#10821=CARTESIAN_POINT ( 'NONE',  ( -0.3743405594629429789, -5.157627118644069419, 7.023440622744399953 ) ) ;
#10829=CARTESIAN_POINT ( 'NONE',  ( -1.630481553867809907, -3.543304787045240101, 3.002862530617889547 ) ) ;
#10833=CARTESIAN_POINT ( 'NONE',  ( -1.332058588847369940, -3.100827309567760537, 6.640197310420220767 ) ) ;
#10835=CARTESIAN_POINT ( 'NONE',  ( 0.2047443300700049207, -2.192584066324520187, 2.657212296411530783 ) ) ;
#10838=CARTESIAN_POINT ( 'NONE',  ( -1.494590226124050014, -0.2673043920988010247, 2.870965838437660178 ) ) ;
#10843=FILL_AREA_STYLE ('',( #13633 ) ) ;
#10852=CARTESIAN_POINT ( 'NONE',  ( 1.641808337277750107, -5.113135593220339281, 6.386111670537619744 ) ) ;
#10858=CARTESIAN_POINT ( 'NONE',  ( 0.8934014991060330590, -0.9854339516935011201, 6.877287176483390496 ) ) ;
#10859=CARTESIAN_POINT ( 'NONE',  ( -1.661700935788390066, -4.954166666666670160, 3.038299064211620326 ) ) ;
#10860=CARTESIAN_POINT ( 'NONE',  ( -0.8001898266890440370, -1.470647129387580021, 6.913242401714570384 ) ) ;
#10863=CARTESIAN_POINT ( 'NONE',  ( -2.650076489488250697, -0.2224576271186441134, 4.841243018609314497 ) ) ;
#10864=CARTESIAN_POINT ( 'NONE',  ( -2.234315482767910144, -0.5402542372881360411, 3.960850823455329905 ) ) ;
#10868=EDGE_CURVE ( 'NONE', #12508, #13175, #11666, .T. ) ;
#10870=CARTESIAN_POINT ( 'NONE',  ( -1.221947981261169991, -0.5741044150835520332, 2.670403636935529956 ) ) ;
#10874=CARTESIAN_POINT ( 'NONE',  ( 2.573461662271340877, -0.7525510688106187285, 5.348389362822485893 ) ) ;
#10877=CARTESIAN_POINT ( 'NONE',  ( 1.197297565406180153, -4.082776294035840969, 6.726135293448179731 ) ) ;
#10880=CARTESIAN_POINT ( 'NONE',  ( -1.942813984510721070, -4.525253771513313872, 5.363608065214459764 ) ) ;
#10884=CARTESIAN_POINT ( 'NONE',  ( -0.2047443300700520219, -3.407415933675483899, 2.657212296411530783 ) ) ;
#10885=EDGE_LOOP ( 'NONE', ( #17195, #10103, #5315, #16345 ) ) ;
#10889=CARTESIAN_POINT ( 'NONE',  ( -1.880631435828179265, -0.2447033898305090438, 3.876649216148230437 ) ) ;
#10892=CARTESIAN_POINT ( 'NONE',  ( 0.6370285429020036139, -0.6606104644819236205, 2.105399314608770833 ) ) ;
#10893=CARTESIAN_POINT ( 'NONE',  ( 1.837442528958791010, -2.056695212954759100, 2.785079989718789673 ) ) ;
#10896=CARTESIAN_POINT ( 'NONE',  ( 1.134881315981519645, -5.122033898305085486, 6.410767520434657918 ) ) ;
#10905=CARTESIAN_POINT ( 'NONE',  ( -2.345900685764729765, -5.528813559322030002, 4.512231114381339836 ) ) ;
#10908=CARTESIAN_POINT ( 'NONE',  ( 2.653777292528160192, -3.826605122864674247, 4.724078510415155030 ) ) ;
#10909=CARTESIAN_POINT ( 'NONE',  ( 1.670747152266691016, -0.4963810343603142217, 3.047345280935851441 ) ) ;
#10910=CARTESIAN_POINT ( 'NONE',  ( -1.011820239713360658, -3.636457940198391636, 2.246566997958110434 ) ) ;
#10912=CARTESIAN_POINT ( 'NONE',  ( -0.1608173401625278554, -1.101875393134940984, 6.746714348835997299 ) ) ;
#10915=CARTESIAN_POINT ( 'NONE',  ( -0.7137241095604881513, -2.099430913171361102, 2.143887406933340678 ) ) ;
#10918=CARTESIAN_POINT ( 'NONE',  ( -1.300961508564169922, -0.4779661016949160457, 6.661123742937279602 ) ) ;
#10920=CARTESIAN_POINT ( 'NONE',  ( 1.074829861819710075, -2.285737219477669946, 2.606322265575589991 ) ) ;
#10921=CARTESIAN_POINT ( 'NONE',  ( -1.713314936023349944, -0.5610169491525430763, 3.089913064446579760 ) ) ;
#10923=CARTESIAN_POINT ( 'NONE',  ( -2.458531667407850563, -5.506567796610171150, 5.699238225248945966 ) ) ;
#10926=CARTESIAN_POINT ( 'NONE',  ( 1.300961508564179692, -5.122033898305089039, 6.661123742937278713 ) ) ;
#10930=CARTESIAN_POINT ( 'NONE',  ( -0.4735094604798580353, -4.567989471729919870, 7.005327412390699671 ) ) ;
#10931=CARTESIAN_POINT ( 'NONE',  ( -2.253200202764409799, -5.511016949152540256, 5.379408587037509903 ) ) ;
#10935=CARTESIAN_POINT ( 'NONE',  ( -0.9485663501270049647, -3.054250732991179440, 6.853826262002260528 ) ) ;
#10937=CARTESIAN_POINT ( 'NONE',  ( -1.919159680931840084, -1.866548030288480042, 3.970803207828165426 ) ) ;
#10938=CARTESIAN_POINT ( 'NONE',  ( -0.7093417302541390468, -0.4646186440677970153, 6.943956659919700236 ) ) ;
#10944=( LENGTH_UNIT ( ) NAMED_UNIT ( * ) SI_UNIT ( .MILLI., .METRE. ) );
#10947=EDGE_LOOP ( 'NONE', ( #8238, #7429, #4392, #5705 ) ) ;
#10950=CARTESIAN_POINT ( 'NONE',  ( 2.155845792290829621, -5.055296610169490279, 3.756158857535770057 ) ) ;
#10952=CARTESIAN_POINT ( 'NONE',  ( 1.951437470830589938, -0.5429564742160228885, 3.384463041838829955 ) ) ;
#10954=DIRECTION ( 'NONE',  ( 0.7045302523384989746, -0.08528919673497019349, -0.7045302523385029714 ) ) ;
#10956=CARTESIAN_POINT ( 'NONE',  ( -2.091095264232510242, -1.656953435693890198, 5.779845490516250628 ) ) ;
#10958=CARTESIAN_POINT ( 'NONE',  ( 0.6640878839024751956, -0.1379237288135599648, 7.269405042592523181 ) ) ;
#10960=CARTESIAN_POINT ( 'NONE',  ( -1.943632316591239917, -0.5536016949152539057, 3.373048379518170048 ) ) ;
#10964=CARTESIAN_POINT ( 'NONE',  ( -2.519547246525518425, -0.2402542372881359412, 3.866491354109200529 ) ) ;
#10967=CARTESIAN_POINT ( 'NONE',  ( -2.075124426334558958, -2.918361879621430344, 5.810227140144560209 ) ) ;
#10969=CARTESIAN_POINT ( 'NONE',  ( 2.043308330018790198, -5.399788135593220240, 5.867646457774659652 ) ) ;
#10970=CARTESIAN_POINT ( 'NONE',  ( 2.328527996529149657, -0.5662447625043111055, 3.426787111016343701 ) ) ;
#10973=CARTESIAN_POINT ( 'NONE',  ( -2.053221424930790295, -4.734848366107910600, 3.549770689668290125 ) ) ;
#10974=CARTESIAN_POINT ( 'NONE',  ( -2.437122747866789840, -5.010466949207390108, 3.649501829874993941 ) ) ;
#10978=CARTESIAN_POINT ( 'NONE',  ( 0.6217226704572607066, -1.307629111369559949, 6.656620240022977697 ) ) ;
#10985=CARTESIAN_POINT ( 'NONE',  ( 2.523518139275831462, -2.336154672414218592, 5.521565513971776085 ) ) ;
#10986=CARTESIAN_POINT ( 'NONE',  ( -1.485788269501200132, -4.829629811528119099, 2.863981322975839738 ) ) ;
#10987=CARTESIAN_POINT ( 'NONE',  ( 1.994315313497110997, -5.386440677966105817, 5.187224322759965922 ) ) ;
#10993=CARTESIAN_POINT ( 'NONE',  ( 1.661700935788380074, -5.337500000000000355, 3.038299064211610112 ) ) ;
#10994=CARTESIAN_POINT ( 'NONE',  ( 1.951437470830589938, -0.5429564742160228885, 3.384463041838829955 ) ) ;
#10995=CARTESIAN_POINT ( 'NONE',  ( 1.769056124370469885, -3.915917399657852904, 2.721729512470748791 ) ) ;
#10997=CARTESIAN_POINT ( 'NONE',  ( -0.3509990757148119811, -1.125163681423229756, 6.722795464567655976 ) ) ;
#11001=VERTEX_POINT ( 'NONE', #9326 ) ;
#11003=CARTESIAN_POINT ( 'NONE',  ( 1.407651048079441525, -0.3266949152542383272, 2.450250343405061759 ) ) ;
#11004=CARTESIAN_POINT ( 'NONE',  ( 0.0003104168811309170268, -5.145080155286260393, 2.198280450787269746 ) ) ;
#11006=CARTESIAN_POINT ( 'NONE',  ( -1.128670402850159737, -5.470974576271190770, 7.101865548313641696 ) ) ;
#11009=CARTESIAN_POINT ( 'NONE',  ( -1.851073041990159540, -5.193220338983048912, 6.153284478378270528 ) ) ;
#11013=CARTESIAN_POINT ( 'NONE',  ( -1.092567884283820012, -4.637854336594780413, 6.784476218553590066 ) ) ;
#11014=CARTESIAN_POINT ( 'NONE',  ( 0.6370285429020036139, -0.6606104644819236205, 2.105399314608770833 ) ) ;
#11015=FACE_OUTER_BOUND ( 'NONE', #3305, .T. ) ;
#11018=CARTESIAN_POINT ( 'NONE',  ( 2.211317922628870392, -2.472043525783979678, 3.894507149290419967 ) ) ;
#11020=CARTESIAN_POINT ( 'NONE',  ( -1.673492459604430938, -3.496728210468663889, 3.510746103527421891 ) ) ;
#11028=ORIENTED_EDGE ( 'NONE', *, *, #2132, .T. ) ;
#11031=CARTESIAN_POINT ( 'NONE',  ( 0.7982439214406963357, -5.130932203389829915, 6.591424794228156081 ) ) ;
#11037=CARTESIAN_POINT ( 'NONE',  ( -2.036910256464079971, -4.940602084342534894, 4.443293066459140128 ) ) ;
#11038=CARTESIAN_POINT ( 'NONE',  ( -0.07064654565474801085, -0.1512711864406789675, 7.352897294663512717 ) ) ;
#11041=CARTESIAN_POINT ( 'NONE',  ( -1.666450993087168930, -0.1824152542372889096, 6.765380371283871597 ) ) ;
#11043=ORIENTED_EDGE ( 'NONE', *, *, #13307, .F. ) ;
#11045=CARTESIAN_POINT ( 'NONE',  ( 2.283153923255319739, -2.196424942684490400, 4.129076318403450685 ) ) ;
#11046=CARTESIAN_POINT ( 'NONE',  ( 2.650076489488250697, -5.377542372881360500, 4.841243018609314497 ) ) ;
#11047=EDGE_CURVE ( 'NONE', #4345, #12508, #1186, .T. ) ;
#11048=CARTESIAN_POINT ( 'NONE',  ( -2.573461662271331551, -4.847448931189385135, 5.348389362822530302 ) ) ;
#11052=CARTESIAN_POINT ( 'NONE',  ( 2.340959815966380031, -3.849893411152960354, 4.942183458383420103 ) ) ;
#11053=CARTESIAN_POINT ( 'NONE',  ( -0.5355577887185811736, -4.567989471729919870, 7.299286738308172318 ) ) ;
#11058=CARTESIAN_POINT ( 'NONE',  ( -1.727468145286550127, -1.633665147405598761, 5.809394271505101237 ) ) ;
#11063=CARTESIAN_POINT ( 'NONE',  ( -0.9707742057416274273, -0.1735169491525429541, 6.508944043303927174 ) ) ;
#11064=CARTESIAN_POINT ( 'NONE',  ( 1.650842931266089497, -2.033406924666469884, 2.622060802311419803 ) ) ;
#11066=CARTESIAN_POINT ( 'NONE',  ( -0.2109711709854041328, -5.280843314568215874, 2.050669023674909663 ) ) ;
#11067=CARTESIAN_POINT ( 'NONE',  ( -1.965557623688110933, -5.211016949152535993, 5.292675575926340414 ) ) ;
#11076=CARTESIAN_POINT ( 'NONE',  ( -2.011500846714319835, -5.551059322033900401, 3.478373409938470218 ) ) ;
#11078=CARTESIAN_POINT ( 'NONE',  ( -2.316126390218390618, -4.734848366107908824, 3.404364157709380390 ) ) ;
#11079=CARTESIAN_POINT ( 'NONE',  ( 0.6890111762202997259, -3.799475958216412153, 2.137115435286760956 ) ) ;
#11081=CARTESIAN_POINT ( 'NONE',  ( 2.049150047780149642, -0.7059744922340407403, 4.826039376028505856 ) ) ;
#11086=CARTESIAN_POINT ( 'NONE',  ( -2.293398556041709835, -0.5358050847457630494, 4.171956209133480975 ) ) ;
#11087=CARTESIAN_POINT ( 'NONE',  ( 2.340070819011249803, -0.3800847457627120063, 4.950151441910540129 ) ) ;
#11088=CARTESIAN_POINT ( 'NONE',  ( 1.962536940652990003, -2.704926408666860294, 5.998920491814760503 ) ) ;
#11090=CARTESIAN_POINT ( 'NONE',  ( -1.800129581279449775, -5.564406779661021041, 2.750028594811118943 ) ) ;
#11098=CARTESIAN_POINT ( 'NONE',  ( 1.026235786675480099, -4.404971453711899798, 6.817920158464540137 ) ) ;
#11099=CARTESIAN_POINT ( 'NONE',  ( 0.009452110982655418520, -5.000192044704539818, 2.350000000000000089 ) ) ;
#11102=CARTESIAN_POINT ( 'NONE',  ( -2.283153923255329953, -3.403575057315510133, 4.129076318403500423 ) ) ;
#11104=CARTESIAN_POINT ( 'NONE',  ( -2.035869680587120811, -3.310421904162345719, 4.964832940349540813 ) ) ;
#11116=CARTESIAN_POINT ( 'NONE',  ( -1.754713504580578842, -5.251059322033895249, 3.634325740584633646 ) ) ;
#11117=CARTESIAN_POINT ( 'NONE',  ( -0.4469859058769716786, -1.823812330071880705, 2.084026511420800976 ) ) ;
#11125=CARTESIAN_POINT ( 'NONE',  ( 1.928817277882869829, -1.144611093351550091, 6.048484184565929844 ) ) ;
#11126=CARTESIAN_POINT ( 'NONE',  ( -2.651721837666119796, -0.2269067796610169385, 4.594045830208265180 ) ) ;
#11127=CARTESIAN_POINT ( 'NONE',  ( -1.811729841638700211, -0.5580508474576270084, 3.197954009834299782 ) ) ;
#11129=CARTESIAN_POINT ( 'NONE',  ( 1.647941990407678636, -0.04449152542372906277, 3.475676388127089123 ) ) ;
#11134=CARTESIAN_POINT ( 'NONE',  ( -1.353103843060629918, -2.801920438179980266, 6.625579309552958485 ) ) ;
#11136=CARTESIAN_POINT ( 'NONE',  ( -2.458531667407850563, -5.506567796610171150, 5.699238225248945966 ) ) ;
#11138=CARTESIAN_POINT ( 'NONE',  ( 0.2818998297622880012, -1.354205687946139935, 7.036509827384409554 ) ) ;
#11140=CARTESIAN_POINT ( 'NONE',  ( -2.034805890357269220, -0.5313559322033900578, 4.427518626519226785 ) ) ;
#11146=CARTESIAN_POINT ( 'NONE',  ( -1.491388273268980491, -1.587088570829020551, 6.110908523251552538 ) ) ;
#11155=CARTESIAN_POINT ( 'NONE',  ( 1.392767620582681332, -3.570433951693503527, 2.440948861123688474 ) ) ;
#11159=CARTESIAN_POINT ( 'NONE',  ( -0.009452110982656853136, -5.299807955295470663, 2.649999999999998579 ) ) ;
#11160=CARTESIAN_POINT ( 'NONE',  ( 1.679950111053631900, -5.404237288135596451, 5.880020650119711867 ) ) ;
#11165=CARTESIAN_POINT ( 'NONE',  ( -1.496290472746829803, -0.5672554343907050267, 2.872674968141029961 ) ) ;
#11169=CARTESIAN_POINT ( 'NONE',  ( 2.296954468777709923, -0.6361096273691760894, 4.187412587068650716 ) ) ;
#11171=CARTESIAN_POINT ( 'NONE',  ( 1.861802609626429961, -0.7991276453871953844, 5.565212624397201324 ) ) ;
#11180=CARTESIAN_POINT ( 'NONE',  ( 1.661700935788380074, -5.337500000000000355, 3.038299064211610112 ) ) ;
#11182=CARTESIAN_POINT ( 'NONE',  ( -2.350067830300900162, -0.5224576271186440746, 4.825253242917699303 ) ) ;
#11184=CARTESIAN_POINT ( 'NONE',  ( -1.332058588847369940, -3.100827309567760537, 6.640197310420220767 ) ) ;
#11190=CARTESIAN_POINT ( 'NONE',  ( -1.428515267734879579, -5.268855932203389436, 2.829745655876930499 ) ) ;
#11191=CARTESIAN_POINT ( 'NONE',  ( 0.000000000000000000, 0.000000000000000000, 0.000000000000000000 ) ) ;
#11196=CARTESIAN_POINT ( 'NONE',  ( 0.1824815401350060040, -4.498124606865050445, 7.046368721022729709 ) ) ;
#11199=CARTESIAN_POINT ( 'NONE',  ( -0.009452110982655139229, -5.299807955295460005, 2.350000000000000089 ) ) ;
#11202=CARTESIAN_POINT ( 'NONE',  ( -1.777964140657649850, -4.731007489747940831, 6.241943319976260618 ) ) ;
#11206=CARTESIAN_POINT ( 'NONE',  ( -0.2302241296435190154, -3.706322805063249959, 2.659926792304259990 ) ) ;
#11209=ORIENTED_EDGE ( 'NONE', *, *, #3364, .T. ) ;
#11219=CARTESIAN_POINT ( 'NONE',  ( -1.088937603231280304, -5.273305084745764759, 2.959627624143549074 ) ) ;
#11226=CARTESIAN_POINT ( 'NONE',  ( 1.687170344132030042, -2.751502985243429844, 6.340793075730549511 ) ) ;
#11227=CARTESIAN_POINT ( 'NONE',  ( 1.313542260532459149, -2.475884402143949892, 6.277817661335856059 ) ) ;
#11228=CARTESIAN_POINT ( 'NONE',  ( -1.713314936023349944, -0.2610169491525429764, 3.089913064446579760 ) ) ;
#11235=CARTESIAN_POINT ( 'NONE',  ( -1.477796163681079911, -0.1824152542372889929, 6.531563725478150673 ) ) ;
#11236=CARTESIAN_POINT ( 'NONE',  ( -0.1569242594330230167, -1.400782264522720144, 7.048216443236290374 ) ) ;
#11240=CARTESIAN_POINT ( 'NONE',  ( -0.3413183941262150078, -2.685478996738541291, 7.028571974690709823 ) ) ;
#11242=CARTESIAN_POINT ( 'NONE',  ( 2.304156201936080617, -5.399788135593215799, 6.016707707703351282 ) ) ;
#11244=CARTESIAN_POINT ( 'NONE',  ( 0.9170541073686970801, -1.284340823081270067, 6.867431071947180499 ) ) ;
#11246=CARTESIAN_POINT ( 'NONE',  ( 1.614765845140360589, -0.4067796610169500116, 5.967758800287426446 ) ) ;
#11251=CARTESIAN_POINT ( 'NONE',  ( -0.5133516189064535329, -1.447358841099289251, 6.687805814961367723 ) ) ;
#11256=CARTESIAN_POINT ( 'NONE',  ( 0.3803919826356921829, -0.3088983050847459166, 2.682580100125298461 ) ) ;
#11257=CARTESIAN_POINT ( 'NONE',  ( 1.963178672446078687, -3.640298816558361406, 2.914210764660420061 ) ) ;
#11260=CARTESIAN_POINT ( 'NONE',  ( -0.1654173910288039839, -5.280843314568230085, 2.650679959339568459 ) ) ;
#11261=CARTESIAN_POINT ( 'NONE',  ( -1.489797906646480596, -5.188771186440680694, 6.112509577910826941 ) ) ;
#11264=CARTESIAN_POINT ( 'NONE',  ( 2.234315482767910144, -5.359745762711869865, 3.960850823455320580 ) ) ;
#11265=CARTESIAN_POINT ( 'NONE',  ( -0.009452110982655708218, -0.5998079552954630467, 2.350000000000000089 ) ) ;
#11268=CARTESIAN_POINT ( 'NONE',  ( 0.2620510901103109691, -1.893677194936739916, 2.361180871966390260 ) ) ;
#11271=CARTESIAN_POINT ( 'NONE',  ( -1.508881462028629716, -1.288181699441250050, 6.092184821126286565 ) ) ;
#11275=CARTESIAN_POINT ( 'NONE',  ( -2.155845792290839835, -0.5447033898305089217, 3.756158857535780271 ) ) ;
#11276=CARTESIAN_POINT ( 'NONE',  ( -1.791574935211209807, -0.4913135593220339659, 6.226029630577610163 ) ) ;
#11277=CARTESIAN_POINT ( 'NONE',  ( -2.326448859701059746, -3.380286769027220029, 4.344498395672320434 ) ) ;
#11280=CARTESIAN_POINT ( 'NONE',  ( -2.540842781840720654, -5.511016949152534927, 5.466141598148674952 ) ) ;
#11283=CARTESIAN_POINT ( 'NONE',  ( -0.8570167067220348933, -5.282203389830509188, 2.508190348879360432 ) ) ;
#11287=CARTESIAN_POINT ( 'NONE',  ( -0.9038768003981948462, -1.470647129387581575, 7.195219513931347954 ) ) ;
#11289=CARTESIAN_POINT ( 'NONE',  ( 0.9724415447670879953, -0.7068739681193980662, 2.553509270169310064 ) ) ;
#11290=CARTESIAN_POINT ( 'NONE',  ( 1.661700935788380074, -5.337500000000000355, 3.038299064211610112 ) ) ;
#11293=CARTESIAN_POINT ( 'NONE',  ( 2.239137794397009884, -0.6128213390808879835, 3.975425900939169921 ) ) ;
#11296=CARTESIAN_POINT ( 'NONE',  ( 0.4005155088302400634, -4.474836318576759453, 7.019123328904770531 ) ) ;
#11298=CARTESIAN_POINT ( 'NONE',  ( -1.124021676335500208, -3.589881363621813648, 2.982013645643241340 ) ) ;
#11301=CARTESIAN_POINT ( 'NONE',  ( -1.305383194095490307, -0.5672554343907051377, 3.106059597508353143 ) ) ;
#11310=CARTESIAN_POINT ( 'NONE',  ( 1.134881315981519645, -5.122033898305085486, 6.410767520434657918 ) ) ;
#11311=CARTESIAN_POINT ( 'NONE',  ( 2.295344368707611160, -2.126560077819629413, 3.367893426919545519 ) ) ;
#11314=CARTESIAN_POINT ( 'NONE',  ( 1.763960074743270212, -0.6810390010611521161, 2.931777988865699847 ) ) ;
#11320=CARTESIAN_POINT ( 'NONE',  ( -1.417709711196470046, -2.006277760018209566, 2.821478011237799954 ) ) ;
#11321=CARTESIAN_POINT ( 'NONE',  ( 1.160665242129880426, -2.499172690432241772, 6.393445611272976947 ) ) ;
#11322=CARTESIAN_POINT ( 'NONE',  ( -2.286166334984490067, -0.2135593220338989906, 5.258525443163870605 ) ) ;
#11327=CARTESIAN_POINT ( 'NONE',  ( 1.622657008870240762E-16, -3.053113317719175556E-16, 2.649999999999998579 ) ) ;
#11328=CARTESIAN_POINT ( 'NONE',  ( 0.4539185741479240255, -2.215872354612800521, 2.390735265170440105 ) ) ;
#11333=CARTESIAN_POINT ( 'NONE',  ( -2.100188519621618788, -1.590929447189000090, 3.637948273607420457 ) ) ;
#11334=CARTESIAN_POINT ( 'NONE',  ( 2.431060148753489081, -5.355296610169490101, 3.635668498923322112 ) ) ;
#11337=CARTESIAN_POINT ( 'NONE',  ( 2.331386066015260106, -0.9583047870452390260, 4.378465089518139841 ) ) ;
#11338=CARTESIAN_POINT ( 'NONE',  ( 1.965557623688110933, -0.3889830508474575455, 5.292675575926325315 ) ) ;
#11343=CARTESIAN_POINT ( 'NONE',  ( 0.9361665894546294941, -2.285737219477670390, 2.872845392579769452 ) ) ;
#11345=CARTESIAN_POINT ( 'NONE',  ( 2.386628511786341722, -0.3533898305084745561, 3.539457309197775459 ) ) ;
#11351=CARTESIAN_POINT ( 'NONE',  ( 0.009452110982653675123, -5.000192044704546035, 2.050000000000001155 ) ) ;
#11352=CARTESIAN_POINT ( 'NONE',  ( 2.351526912647309953, -5.373093220338979847, 4.606040641882800379 ) ) ;
#11355=CARTESIAN_POINT ( 'NONE',  ( 1.112838723655040107, -5.426483050847459744, 6.773667561836210105 ) ) ;
#11360=CARTESIAN_POINT ( 'NONE',  ( 1.630481553867769939, -2.056695212954759988, 3.002862530617850023 ) ) ;
#11362=CARTESIAN_POINT ( 'NONE',  ( 0.7854158957161911925, -1.963542059801608897, 2.803154272645130618 ) ) ;
#11366=CARTESIAN_POINT ( 'NONE',  ( 2.645377369053839356, -0.07118644067796667252, 4.488260618344900088 ) ) ;
#11367=CARTESIAN_POINT ( 'NONE',  ( 1.167621112247380077, -2.821367850108300157, 6.743381174846749815 ) ) ;
#11370=CARTESIAN_POINT ( 'NONE',  ( -0.4917262214559124933, -5.291101694915254505, 2.092115739186370948 ) ) ;
#11380=CARTESIAN_POINT ( 'NONE',  ( -1.864786684738369837, -4.804713230972779137, 2.817120744449669978 ) ) ;
#11383=CARTESIAN_POINT ( 'NONE',  ( -1.282210379528740063, -4.661142624883069630, 6.673494927815290190 ) ) ;
#11385=CARTESIAN_POINT ( 'NONE',  ( 1.217499609005879613, -3.892629111369556139, 3.046943272389411206 ) ) ;
#11396=CARTESIAN_POINT ( 'NONE',  ( -1.821706171509118954, -5.202118644067803999, 5.646608543709410455 ) ) ;
#11397=B_SPLINE_CURVE_WITH_KNOTS ( 'NONE', 3,
 ( #26, #194, #15489, #2797, #8441, #14075, #11314, #4259, #2891, #8538, #13061, #4797, #6202, #11859, #4447 ),
 .UNSPECIFIED., .F., .F.,
 ( 4, 1, 1, 1, 1, 1, 1, 1, 1, 1, 1, 1, 4 ),
 ( 0.000000000000000000, 0.04238993203366740042, 0.08487769703127090448, 0.1274691104750300119, 0.1700369147469420195, 0.2126104510727770125, 0.2551841450616499918, 0.2977574123561499975, 0.3403308656859569958, 0.3829042603268439926, 0.4254776701664709782, 0.4680510765564160347, 0.4999998211434338868 ),
 .UNSPECIFIED. ) ;
#11404=CARTESIAN_POINT ( 'NONE',  ( 1.167621112247380077, -2.821367850108300157, 6.743381174846749815 ) ) ;
#11405=CARTESIAN_POINT ( 'NONE',  ( 0.9976707306414894783, -2.522460978720530989, 6.494311833503137343 ) ) ;
#11406=CARTESIAN_POINT ( 'NONE',  ( -1.300961508564169922, -0.1779661016949160013, 6.661123742937279602 ) ) ;
#11408=CARTESIAN_POINT ( 'NONE',  ( 1.707817112497189926, -0.4112288135593229477, 6.319218296629480314 ) ) ;
#11414=CARTESIAN_POINT ( 'NONE',  ( -1.236334101859210000, -2.029566048306499670, 2.697445712080720259 ) ) ;
#11418=CARTESIAN_POINT ( 'NONE',  ( -1.074829861819749821, -3.314262780522329255, 2.606322265575610864 ) ) ;
#11420=CARTESIAN_POINT ( 'NONE',  ( 0.07064654565475687875, -5.448728813559320372, 7.352897294663512717 ) ) ;
#11422=ORIENTED_EDGE ( 'NONE', *, *, #2983, .F. ) ;
#11423=CARTESIAN_POINT ( 'NONE',  ( 2.012177589105479392, -0.3845338983050847759, 5.107213040360584877 ) ) ;
#11426=CARTESIAN_POINT ( 'NONE',  ( 2.052456847059610734, -2.565196678937129438, 4.748194746458525017 ) ) ;
#11427=CARTESIAN_POINT ( 'NONE',  ( 1.347262683220810553, -0.4245762711864407013, 6.986424775243341045 ) ) ;
#11430=CARTESIAN_POINT ( 'NONE',  ( 0.1365430262726380628, -0.4468220338983063811, 6.748423079423377047 ) ) ;
#11435=CARTESIAN_POINT ( 'NONE',  ( -1.392553072310521278, -5.564406779661021041, 3.191531554476531252 ) ) ;
#11441=CARTESIAN_POINT ( 'NONE',  ( 1.465095039565329937, -2.033406924666469884, 2.858195935359850282 ) ) ;
#11446=CARTESIAN_POINT ( 'NONE',  ( -1.627161714697918704, -1.637506023765568530, 3.448102801005849649 ) ) ;
#11453=CARTESIAN_POINT ( 'NONE',  ( -2.304156201936080617, -0.5002118644067795605, 6.016707707703351282 ) ) ;
#11454=CARTESIAN_POINT ( 'NONE',  ( -0.6864473529425049181, -4.591277760018209975, 6.951118770549909343 ) ) ;
#11457=CARTESIAN_POINT ( 'NONE',  ( -0.9002849211310044453, -5.166525423728809407, 7.196465912290821443 ) ) ;
#11466=CARTESIAN_POINT ( 'NONE',  ( 1.468674196027861756, -1.237764246504700072, 6.910454658870847311 ) ) ;
#11470=CARTESIAN_POINT ( 'NONE',  ( -0.1768565782246520057, -1.847100618360170143, 2.353200596935780098 ) ) ;
#11473=CARTESIAN_POINT ( 'NONE',  ( 2.190084968185480374, -4.032358841099290103, 3.838447030292440054 ) ) ;
#11475=CARTESIAN_POINT ( 'NONE',  ( 0.3509990757148593321, -4.474836318576761229, 6.722795464567642654 ) ) ;
#11477=CARTESIAN_POINT ( 'NONE',  ( 2.116444151961470066, -0.3533898305084750002, 3.670839500609349937 ) ) ;
#11488=CARTESIAN_POINT ( 'NONE',  ( 0.4339619423229844619, -5.439830508474575943, 6.706578715862737461 ) ) ;
#11489=CARTESIAN_POINT ( 'NONE',  ( -1.818868030982659700, -3.244397915657463827, 2.767428454397828919 ) ) ;
#11494=CARTESIAN_POINT ( 'NONE',  ( -1.364983921886200546, -4.865515740159335856, 2.403349116468209257 ) ) ;
#11497=CARTESIAN_POINT ( 'NONE',  ( -1.332058588847369940, -3.100827309567760537, 6.640197310420220767 ) ) ;
#11498=CARTESIAN_POINT ( 'NONE',  ( 2.021195349941390162, -3.780028546288090041, 4.339901124684640621 ) ) ;
#11499=CARTESIAN_POINT ( 'NONE',  ( 1.526871680339569659, -0.04004237288135625850, 3.327650196883443101 ) ) ;
#11501=CARTESIAN_POINT ( 'NONE',  ( -0.008736317425858650815, -5.288463233533899910, 2.411138844410889881 ) ) ;
#11504=( BOUNDED_SURFACE ( )  B_SPLINE_SURFACE ( 3, 3, ( 
 ( #13913, #2620, #7161, #1227, #4177, #7241, #12798 ),
 ( #5759, #6871, #17032, #16683, #14355, #8710, #1677 ),
 ( #15759, #5843, #11494, #17125, #12882, #3067, #196 ),
 ( #4449, #10108, #3546, #9193, #16240, #12263, #11982 ),
 ( #17881, #1156, #17790, #13563, #14855, #10777, #15145 ),
 ( #4932, #967, #17981, #5127, #8103, #10587, #17595 ),
 ( #5326, #12173, #16618, #15232, #3918, #10688, #9574 ) ),
 .UNSPECIFIED., .T., .F., .F. ) 
 B_SPLINE_SURFACE_WITH_KNOTS ( ( 4, 3, 4 ),
 ( 4, 1, 1, 1, 4 ),
 ( 0.000000000000000000, 3.141592653589790007, 6.283185307179590673 ),
 ( 18.06415775814129887, 18.36448856483159986, 18.49670707487869947, 18.62179267666130045, 18.84955592153880133 ),
 .UNSPECIFIED. ) 
 GEOMETRIC_REPRESENTATION_ITEM ( )  RATIONAL_B_SPLINE_SURFACE ( (
 ( 1.000000000000000000, 1.000000000000000000, 1.000000000000000000, 1.000000000000000000, 1.000000000000000000, 1.000000000000000000, 1.000000000000000000),
 ( 0.3333333333333329818, 0.3333333333333329818, 0.3333333333333329818, 0.3333333333333329818, 0.3333333333333329818, 0.3333333333333329818, 0.3333333333333329818),
 ( 0.3333333333333329818, 0.3333333333333329818, 0.3333333333333329818, 0.3333333333333329818, 0.3333333333333329818, 0.3333333333333329818, 0.3333333333333329818),
 ( 1.000000000000000000, 1.000000000000000000, 1.000000000000000000, 1.000000000000000000, 1.000000000000000000, 1.000000000000000000, 1.000000000000000000),
 ( 0.3333333333333329818, 0.3333333333333329818, 0.3333333333333329818, 0.3333333333333329818, 0.3333333333333329818, 0.3333333333333329818, 0.3333333333333329818),
 ( 0.3333333333333329818, 0.3333333333333329818, 0.3333333333333329818, 0.3333333333333329818, 0.3333333333333329818, 0.3333333333333329818, 0.3333333333333329818),
 ( 1.000000000000000000, 1.000000000000000000, 1.000000000000000000, 1.000000000000000000, 1.000000000000000000, 1.000000000000000000, 1.000000000000000000) ) ) 
 REPRESENTATION_ITEM ( '' )  SURFACE ( )  );
#11505=CARTESIAN_POINT ( 'NONE',  ( -2.286166334984490067, -0.2135593220338989906, 5.258525443163870605 ) ) ;
#11506=CARTESIAN_POINT ( 'NONE',  ( -2.091095264232510242, -1.656953435693890198, 5.779845490516250628 ) ) ;
#11510=CARTESIAN_POINT ( 'NONE',  ( 2.267872052190589738, -3.756740257999800825, 4.071110468860601017 ) ) ;
#11511=CARTESIAN_POINT ( 'NONE',  ( 2.431060148753489081, -5.055296610169490279, 3.635668498923322112 ) ) ;
#11514=CARTESIAN_POINT ( 'NONE',  ( -1.449568901432419343, -0.5625000000000005551, 3.250431098567584165 ) ) ;
#11521=CARTESIAN_POINT ( 'NONE',  ( 1.928470600873580132, -2.472043525783979678, 3.995796205495612874 ) ) ;
#11526=CARTESIAN_POINT ( 'NONE',  ( -0.009452017499193299602, -0.5998064736617420012, 2.336684903355690235 ) ) ;
#11527=CARTESIAN_POINT ( 'NONE',  ( 0.7982439214406963357, -5.430932203389830626, 6.591424794228156081 ) ) ;
#11528=CARTESIAN_POINT ( 'NONE',  ( -2.286166334984490067, -0.2135593220338989628, 5.258525443163869717 ) ) ;
#11533=CARTESIAN_POINT ( 'NONE',  ( -2.100188519621619676, -1.590929447189000090, 3.637948273607420013 ) ) ;
#11536=CARTESIAN_POINT ( 'NONE',  ( -0.8493734496527890476, -2.755343861603408939, 6.569081749323187225 ) ) ;
#11541=CARTESIAN_POINT ( 'NONE',  ( 1.255262969126039558E-16, -2.775557561562890858E-16, 2.050000000000001155 ) ) ;
#11542=CARTESIAN_POINT ( 'NONE',  ( -1.777964140657649850, -4.731007489747940831, 6.241943319976260618 ) ) ;
#11545=CARTESIAN_POINT ( 'NONE',  ( -1.192209327851089240, -5.277754237288146300, 2.329031440774910422 ) ) ;
#11549=DIRECTION ( 'NONE',  ( -6.123233995736769734E-17, 0.000000000000000000, -1.000000000000000000 ) ) ;
#11552=CARTESIAN_POINT ( 'NONE',  ( -2.235075160050040921, -1.633665147405598761, 6.130927224539796327 ) ) ;
#11557=CARTESIAN_POINT ( 'NONE',  ( 0.4790341583531380065, -1.916965483225030242, 2.395814251711720022 ) ) ;
#11558=CARTESIAN_POINT ( 'NONE',  ( 1.104321075428930765, -5.320452325212860600, 2.282937282173381099 ) ) ;
#11559=CARTESIAN_POINT ( 'NONE',  ( -2.603140590302631008, -1.726818300558751851, 5.216500493824310247 ) ) ;
#11561=CARTESIAN_POINT ( 'NONE',  ( -1.990095963740230900, -4.847448931189385135, 5.204400533041805943 ) ) ;
#11570=CARTESIAN_POINT ( 'NONE',  ( -0.3265524029357583236, -5.457627118644064801, 6.726831181542982208 ) ) ;
#11571=CARTESIAN_POINT ( 'NONE',  ( -1.991177874369409961, -3.221109627369172390, 2.945484578117480989 ) ) ;
#11576=CARTESIAN_POINT ( 'NONE',  ( 1.353103843060669886, -2.798079561820010053, 6.625579309552930063 ) ) ;
#11577=CARTESIAN_POINT ( 'NONE',  ( 1.823404397755048700, -3.943046564306109669, 5.643450181448720571 ) ) ;
#11579=CARTESIAN_POINT ( 'NONE',  ( -2.328217775191430139, -0.2180084745762720100, 5.043379051721170292 ) ) ;
#11581=CARTESIAN_POINT ( 'NONE',  ( -2.034805890357269220, -0.5313559322033900578, 4.427518626519226785 ) ) ;
#11584=CARTESIAN_POINT ( 'NONE',  ( 2.461935615161780611, -3.919758276017824006, 5.690952430644305338 ) ) ;
#11585=CARTESIAN_POINT ( 'NONE',  ( 2.022304719220918479, -0.06673728813559356987, 4.346496488058688712 ) ) ;
#11586=CARTESIAN_POINT ( 'NONE',  ( 0.8748826269292639957, -2.262448931189380286, 2.515205712983200392 ) ) ;
#11590=CARTESIAN_POINT ( 'NONE',  ( 1.044181395669779633, -3.547145663405210314, 2.590869634085890993 ) ) ;
#11592=PRODUCT_CONTEXT ( 'NONE', #5912, 'mechanical' ) ;
#11593=CARTESIAN_POINT ( 'NONE',  ( 1.873832970144350130, -5.037500000000000533, 2.826167029855650270 ) ) ;
#11601=CARTESIAN_POINT ( 'NONE',  ( -0.4625564304287554940, -3.007674156414608557, 6.700235833919871986 ) ) ;
#11603=CARTESIAN_POINT ( 'NONE',  ( -1.661700935788390066, -0.5625000000000000000, 3.038299064211610112 ) ) ;
#11610=CARTESIAN_POINT ( 'NONE',  ( -0.8731223871104993872, -5.470974576271190770, 6.558046933601121786 ) ) ;
#11614=CARTESIAN_POINT ( 'NONE',  ( -2.332582362116870200, -0.2313559322033900412, 4.387643303570821551 ) ) ;
#11616=CARTESIAN_POINT ( 'NONE',  ( -0.2908063684825371031, -4.544701183441625325, 7.337905485238597869 ) ) ;
#11618=CARTESIAN_POINT ( 'NONE',  ( 2.219956784870649624, -2.173136654396199852, 3.918630970161570026 ) ) ;
#11620=CARTESIAN_POINT ( 'NONE',  ( 1.883235269974540937, -2.359442960702510472, 5.517512544583896172 ) ) ;
#11626=CARTESIAN_POINT ( 'NONE',  ( 2.632587027711251526, -0.6593979156574641953, 4.364441905910536157 ) ) ;
#11627=CARTESIAN_POINT ( 'NONE',  ( -2.161802606005209793, -5.010466949207389220, 3.769755311421840283 ) ) ;
#11630=CARTESIAN_POINT ( 'NONE',  ( -0.2469343877495291661, -5.295550847457634269, 2.057675570509529539 ) ) ;
#11631=ORIENTED_EDGE ( 'NONE', *, *, #2132, .F. ) ;
#11638=ADVANCED_FACE ( 'NONE', ( #17720 ), #8900, .T. ) ;
#11640=CARTESIAN_POINT ( 'NONE',  ( -2.033393610350109793, -4.777584066324510381, 5.884928737465370041 ) ) ;
#11643=CARTESIAN_POINT ( 'NONE',  ( -1.353103843060629918, -2.801920438179979822, 6.625579309552960261 ) ) ;
#11644=CARTESIAN_POINT ( 'NONE',  ( -0.009452110982655139229, -5.299807955295460005, 2.350000000000000089 ) ) ;
#11645=CARTESIAN_POINT ( 'NONE',  ( -2.334748642087669523, -4.940602084342530453, 4.403867486184871005 ) ) ;
#11647=DIRECTION ( 'NONE',  ( -1.762990951819940286E-17, -1.000000000000000000, -2.891205793294679017E-15 ) ) ;
#11648=CARTESIAN_POINT ( 'NONE',  ( 1.803891155489780074, -0.8185750573155089471, 3.188470185434109982 ) ) ;
#11649=CARTESIAN_POINT ( 'NONE',  ( -2.286166334984490067, -0.5135593220338989795, 5.258525443163870605 ) ) ;
#11657=B_SPLINE_CURVE_WITH_KNOTS ( 'NONE', 3,
 ( #6462, #3589, #2575, #15184, #9437, #13875, #921, #11004, #5076, #10815, #6559, #16566, #16463, #17830, #5268 ),
 .UNSPECIFIED., .F., .F.,
 ( 4, 1, 1, 1, 1, 1, 1, 1, 1, 1, 1, 1, 4 ),
 ( 0.000000000000000000, 0.04238384222883789798, 0.08486641011426379611, 0.1274541364341190142, 0.1700199979528400074, 0.2125927824332390081, 0.2551660849076620163, 0.2977383825899770353, 0.3403095086483710063, 0.3828788202030369847, 0.4254464832354110104, 0.4680130360807339684, 0.4999998212288473409 ),
 .UNSPECIFIED. ) ;
#11660=CARTESIAN_POINT ( 'NONE',  ( -0.1365430262726299304, -5.453177966101685037, 6.748423079423377047 ) ) ;
#11662=CARTESIAN_POINT ( 'NONE',  ( -2.619177996481920179, -3.081379897639443310, 4.272191262657214494 ) ) ;
#11666=B_SPLINE_CURVE_WITH_KNOTS ( 'NONE', 3,
 ( #14697, #10636, #6647, #5364, #16374, #13776, #12022 ),
 .UNSPECIFIED., .F., .F.,
 ( 4, 1, 1, 1, 4 ),
 ( 5.497787143782139729, 5.798117950472390092, 5.930336460519450625, 6.055422062302069364, 6.283185307179590673 ),
 .UNSPECIFIED. ) ;
#11668=CARTESIAN_POINT ( 'NONE',  ( -0.5902886515192680150, -1.447358841099289917, 6.978224088050050788 ) ) ;
#11670=CARTESIAN_POINT ( 'NONE',  ( -2.033393610350109793, -4.777584066324510381, 5.884928737465370041 ) ) ;
#11671=CARTESIAN_POINT ( 'NONE',  ( -2.050994839075679366, -4.618406924666464519, 4.608774933727191048 ) ) ;
#11672=CARTESIAN_POINT ( 'NONE',  ( 0.006176317641843490427, -5.052110595307439667, 2.465914288053609571 ) ) ;
#11675=CARTESIAN_POINT ( 'NONE',  ( -0.06913820924137326074, -4.222506023765566496, 7.352985789827153340 ) ) ;
#11677=CARTESIAN_POINT ( 'NONE',  ( 1.622657008870240762E-16, -0.3000000000000002665, 2.649999999999998579 ) ) ;
#11678=CARTESIAN_POINT ( 'NONE',  ( -0.4201920264140019956, -2.122719201459649874, 2.384360920086639801 ) ) ;
#11683=CARTESIAN_POINT ( 'NONE',  ( -2.347833536521260367, -3.058091609351149653, 4.537447324629908962 ) ) ;
#11685=CARTESIAN_POINT ( 'NONE',  ( -1.747582379783008788, -5.184322033898315141, 6.697200745122486865 ) ) ;
#11688=CARTESIAN_POINT ( 'NONE',  ( 1.549742865090599997, -0.4156779661016959948, 6.471102547561449647 ) ) ;
#11693=CARTESIAN_POINT ( 'NONE',  ( 2.007801995112640903, -2.611773255513701653, 5.128524201241654978 ) ) ;
#11694=CARTESIAN_POINT ( 'NONE',  ( 2.560337424259670591, -0.06228813559322075172, 4.001768473655590519 ) ) ;
#11700=CARTESIAN_POINT ( 'NONE',  ( 1.477796163681079911, -5.417584745762709986, 6.531563725478140015 ) ) ;
#11704=CARTESIAN_POINT ( 'NONE',  ( -2.409576349373780513, -3.450151633892079239, 3.587770028483140194 ) ) ;
#11706=CARTESIAN_POINT ( 'NONE',  ( -2.301223891756910334, -2.988226744486289999, 5.193066210047999398 ) ) ;
#11709=CARTESIAN_POINT ( 'NONE',  ( 1.865240315818150973, -2.149848366107909303, 3.842223568244794496 ) ) ;
#11713=ORIENTED_EDGE ( 'NONE', *, *, #8895, .T. ) ;
#11716=CARTESIAN_POINT ( 'NONE',  ( 0.2254033459420760055, -0.6247245358507570456, 2.348900562125120217 ) ) ;
#11717=CARTESIAN_POINT ( 'NONE',  ( -2.247144151254851341, -1.614217735477279536, 3.288101683376949413 ) ) ;
#11719=CARTESIAN_POINT ( 'NONE',  ( 1.219286470748990103, -4.381683165423610582, 6.712979431025659416 ) ) ;
#11722=CARTESIAN_POINT ( 'NONE',  ( -1.407651048079459288, -5.273305084745764759, 2.450250343405070641 ) ) ;
#11724=ORIENTED_EDGE ( 'NONE', *, *, #12538, .F. ) ;
#11732=CARTESIAN_POINT ( 'NONE',  ( 1.630703155447489561, -2.332313796054251487, 2.606218513833050920 ) ) ;
#11734=CARTESIAN_POINT ( 'NONE',  ( 1.327748599278330000, -0.4480353997208159633, 2.745754414290000334 ) ) ;
#11737=CARTESIAN_POINT ( 'NONE',  ( -1.724579595320040015, -1.660794312053859967, 3.098572228637930248 ) ) ;
#11741=CARTESIAN_POINT ( 'NONE',  ( 0.2270348434643680025, -5.304612347394249916, 2.348896311281980065 ) ) ;
#11742=CARTESIAN_POINT ( 'NONE',  ( -1.132648842710420656, -1.493935417675870791, 7.100045893750492887 ) ) ;
#11743=EDGE_CURVE ( 'NONE', #14300, #13175, #1924, .T. ) ;
#11747=CARTESIAN_POINT ( 'NONE',  ( -1.588913656382020756, -5.080331814072260421, 3.399901838171254020 ) ) ;
#11750=CARTESIAN_POINT ( 'NONE',  ( 1.978267656359410154, -0.4023305084745769644, 5.974740860598790171 ) ) ;
#11754=CARTESIAN_POINT ( 'NONE',  ( 0.9788656693287738353, -5.320452325212859712, 2.556357798777459944 ) ) ;
#11764=CARTESIAN_POINT ( 'NONE',  ( -2.159566522375440112, -3.240557039297490061, 5.635424033751089468 ) ) ;
#11768=CARTESIAN_POINT ( 'NONE',  ( 2.351526912647309953, -5.373093220338979847, 4.606040641882800379 ) ) ;
#11771=CARTESIAN_POINT ( 'NONE',  ( 0.9170541073686970801, -1.284340823081270067, 6.867431071947180499 ) ) ;
#11772=CARTESIAN_POINT ( 'NONE',  ( 1.724579595320000047, -3.939205687946140344, 3.098572228637889836 ) ) ;
#11774=CARTESIAN_POINT ( 'NONE',  ( 1.966895454505939833, -3.896469987729531681, 5.288408118292026394 ) ) ;
#11776=CARTESIAN_POINT ( 'NONE',  ( 0.1365430262726380628, -0.1468220338983061424, 6.748423079423377047 ) ) ;
#11781=CARTESIAN_POINT ( 'NONE',  ( 1.647941990407678636, -0.3444915254237289615, 3.475676388127089123 ) ) ;
#11782=CARTESIAN_POINT ( 'NONE',  ( -1.507201387235980183, -3.124115597856050197, 6.507509243627219497 ) ) ;
#11787=CARTESIAN_POINT ( 'NONE',  ( 2.316639661709690046, -3.780028546288089153, 4.285359956977720763 ) ) ;
#11790=CARTESIAN_POINT ( 'NONE',  ( 2.578017356471871135, -5.086440677966105994, 5.329826563567761077 ) ) ;
#11794=CARTESIAN_POINT ( 'NONE',  ( -1.713314936023349944, -0.5610169491525430763, 3.089913064446579760 ) ) ;
#11799=CARTESIAN_POINT ( 'NONE',  ( 1.366362128262241571, -3.915917399657852904, 3.167695729602394206 ) ) ;
#11800=CARTESIAN_POINT ( 'NONE',  ( -1.851400890972779045, -0.4868644067796619179, 6.601359968904141340 ) ) ;
#11805=CARTESIAN_POINT ( 'NONE',  ( 0.008535039157541330149, -0.3147268565821629838, 2.281464080633810010 ) ) ;
#11807=CARTESIAN_POINT ( 'NONE',  ( -1.661700935788390288, -0.2625000000000000111, 3.038299064211610112 ) ) ;
#11808=CARTESIAN_POINT ( 'NONE',  ( 0.6919952253610313075, -4.451548030288480895, 7.262080463427998289 ) ) ;
#11811=CARTESIAN_POINT ( 'NONE',  ( 1.669205944673859854, -2.452596113855660231, 6.359065158982410537 ) ) ;
#11814=CARTESIAN_POINT ( 'NONE',  ( 1.727468145286579659, -3.966334852594401994, 5.809394271505055052 ) ) ;
#11817=CARTESIAN_POINT ( 'NONE',  ( 1.417606053559480328, -0.8922807985403484743, 6.185023541745921172 ) ) ;
#11820=FACE_OUTER_BOUND ( 'NONE', #12449, .T. ) ;
#11821=CARTESIAN_POINT ( 'NONE',  ( -2.107551805806941125, -1.311469987729540376, 6.312866726931216199 ) ) ;
#11824=CARTESIAN_POINT ( 'NONE',  ( -2.135041058613629694, -4.800872354612799597, 5.690123914223820023 ) ) ;
#11827=CARTESIAN_POINT ( 'NONE',  ( -0.5889081234606770021, -5.162076271186439413, 6.978529000034869867 ) ) ;
#11833=ORIENTED_EDGE ( 'NONE', *, *, #5650, .T. ) ;
#11835=CARTESIAN_POINT ( 'NONE',  ( 2.212163452524050111, -2.704926408666860738, 6.166099093621837390 ) ) ;
#11836=CARTESIAN_POINT ( 'NONE',  ( 0.5110358699406184479, -0.3612150962701983770, 2.697283651280069527 ) ) ;
#11837=CARTESIAN_POINT ( 'NONE',  ( -0.009452110982655708218, -0.5998079552954630467, 2.350000000000000089 ) ) ;
#11839=CARTESIAN_POINT ( 'NONE',  ( -2.075124426334559846, -2.918361879621429900, 5.810227140144559321 ) ) ;
#11841=CARTESIAN_POINT ( 'NONE',  ( 2.650521604678268694, -1.004881363621820567, 4.833599835830299618 ) ) ;
#11844=CARTESIAN_POINT ( 'NONE',  ( 0.7983658734558030101, -0.4334745762711870176, 6.913847129767330735 ) ) ;
#11857=CARTESIAN_POINT ( 'NONE',  ( 1.764807890102179977, -2.378890372630820149, 3.143016121304719857 ) ) ;
#11859=CARTESIAN_POINT ( 'NONE',  ( 1.677844243193131746, -0.4963825586767564024, 3.040248005478333848 ) ) ;
#11860=CARTESIAN_POINT ( 'NONE',  ( -1.661700935788390066, -0.5625000000000000000, 3.038299064211610112 ) ) ;
#11861=CARTESIAN_POINT ( 'NONE',  ( 1.652654650382400003, -0.7952867690272209522, 3.029252778805620050 ) ) ;
#11863=CARTESIAN_POINT ( 'NONE',  ( 2.262450597846779932, -4.195376859117310175, 5.348122657979680561 ) ) ;
#11864=CARTESIAN_POINT ( 'NONE',  ( 1.872456193198871022, -1.098034516774970770, 5.541908336565965598 ) ) ;
#11869=CARTESIAN_POINT ( 'NONE',  ( -1.494593880360799432, -0.2610169491525428653, 3.295456077495951153 ) ) ;
#11870=CARTESIAN_POINT ( 'NONE',  ( 2.343457872958619959, -4.148800282540729967, 4.916681529328559286 ) ) ;
#11878=CARTESIAN_POINT ( 'NONE',  ( -2.653602652190420574, -5.224364406779660186, 4.735326402787099376 ) ) ;
#11880=CARTESIAN_POINT ( 'NONE',  ( 0.7983658734558030101, -0.4334745762711870176, 6.913847129767330735 ) ) ;
#11884=CARTESIAN_POINT ( 'NONE',  ( -0.6050872056802790722, -3.659746228486683073, 2.738171435586149727 ) ) ;
#11885=CARTESIAN_POINT ( 'NONE',  ( -2.578017356471871135, -0.5135593220338985354, 5.329826563567776176 ) ) ;
#11889=CARTESIAN_POINT ( 'NONE',  ( 1.800129581279440893, -0.03559322033898339871, 2.750028594811110061 ) ) ;
#11894=CARTESIAN_POINT ( 'NONE',  ( 0.7983658734558031211, -0.1334745762711870287, 6.913847129767330735 ) ) ;
#11895=CARTESIAN_POINT ( 'NONE',  ( -0.04351999560413650353, -4.521412895153344103, 7.353529668759054339 ) ) ;
#11897=CARTESIAN_POINT ( 'NONE',  ( -0.3413183941262150078, -2.685478996738539958, 7.028571974690709823 ) ) ;
#11900=CARTESIAN_POINT ( 'NONE',  ( -1.854389246811851022, -3.151244762504313179, 3.819010576716904026 ) ) ;
#11902=CARTESIAN_POINT ( 'NONE',  ( -0.5381211601353440566, -1.148451969711520082, 6.681243917250651698 ) ) ;
#11904=CARTESIAN_POINT ( 'NONE',  ( 1.307725206348619995, -0.7471169921413569615, 2.732408283416570161 ) ) ;
#11910=CARTESIAN_POINT ( 'NONE',  ( -0.8570167067220350043, -5.282203389830510076, 2.508190348879359988 ) ) ;
#11912=EDGE_CURVE ( 'NONE', #12628, #8096, #16089, .T. ) ;
#11919=CARTESIAN_POINT ( 'NONE',  ( 2.619177996481910853, -2.518620102360551893, 4.272191262657148769 ) ) ;
#11924=CARTESIAN_POINT ( 'NONE',  ( 2.340959815966380031, -3.849893411152960354, 4.942183458383420103 ) ) ;
#11925=CARTESIAN_POINT ( 'NONE',  ( 2.174104834890520976, -1.144611093351550091, 6.221966445066246187 ) ) ;
#11931=CARTESIAN_POINT ( 'NONE',  ( 2.043014502273419186, -5.341949152542365908, 3.006203457898239062 ) ) ;
#11935=EDGE_LOOP ( 'NONE', ( #15153, #10641, #11422, #15211 ) ) ;
#11939=CARTESIAN_POINT ( 'NONE',  ( -1.236334101859210000, -2.029566048306499670, 2.697445712080720259 ) ) ;
#11943=CARTESIAN_POINT ( 'NONE',  ( -2.340959815966380031, -1.750106588847040179, 4.942183458383479611 ) ) ;
#11944=CARTESIAN_POINT ( 'NONE',  ( 0.6096110657044089276, -3.799475958216410376, 2.426869991387509806 ) ) ;
#11945=CARTESIAN_POINT ( 'NONE',  ( 1.683529720875211799, -1.144611093351550091, 5.875001924065625936 ) ) ;
#11948=CARTESIAN_POINT ( 'NONE',  ( -1.449568901432419343, -0.5625000000000005551, 3.250431098567584165 ) ) ;
#11952=CARTESIAN_POINT ( 'NONE',  ( -0.2453710345350140487, -0.1557203389830511819, 6.738252723719333481 ) ) ;
#11953=CARTESIAN_POINT ( 'NONE',  ( 2.262450597846779932, -4.195376859117310175, 5.348122657979680561 ) ) ;
#11958=CARTESIAN_POINT ( 'NONE',  ( -1.652654650382402668, -4.804713230972782689, 3.029252778805632484 ) ) ;
#11960=CARTESIAN_POINT ( 'NONE',  ( -0.1565249325564300187, -5.153177966101689655, 7.048192310558509810 ) ) ;
#11962=CARTESIAN_POINT ( 'NONE',  ( 1.978267656359410154, -0.4023305084745769644, 5.974740860598790171 ) ) ;
#11965=CARTESIAN_POINT ( 'NONE',  ( -0.2220816246931631155, -4.544701183441625325, 6.740975647723836950 ) ) ;
#11968=CARTESIAN_POINT ( 'NONE',  ( 1.255262969126039558E-16, -2.775557561562890858E-16, 2.050000000000001155 ) ) ;
#11974=CARTESIAN_POINT ( 'NONE',  ( 2.601107615185130673, -0.3845338983050847759, 5.226397344856369642 ) ) ;
#11977=CARTESIAN_POINT ( 'NONE',  ( -1.057242234132100167, -5.577754237288139905, 2.597442975781530272 ) ) ;
#11978=CARTESIAN_POINT ( 'NONE',  ( -1.026235786675429473, -1.195028546288090077, 6.817920158464569447 ) ) ;
#11979=CARTESIAN_POINT ( 'NONE',  ( -0.7101077586918816964, -0.2831443699174400752, 2.770804889310179764 ) ) ;
#11980=CARTESIAN_POINT ( 'NONE',  ( 2.105672170043351166, -3.962493976234419790, 3.084680091961101045 ) ) ;
#11982=CARTESIAN_POINT ( 'NONE',  ( 0.009452110982653640428, -5.000192044704539818, 2.350000000000000089 ) ) ;
#11983=CARTESIAN_POINT ( 'NONE',  ( 1.881914957835459923, -3.663587104846649734, 3.286797332666310023 ) ) ;
#11984=CARTESIAN_POINT ( 'NONE',  ( -1.670747221194377685, -5.103620102360557631, 3.047345349617607724 ) ) ;
#11986=CARTESIAN_POINT ( 'NONE',  ( 0.1352600594606461204, -4.199217735477280833, 6.748562071049542865 ) ) ;
#11990=CARTESIAN_POINT ( 'NONE',  ( -1.366362128262280429, -1.684082600342149627, 3.167695729602423516 ) ) ;
#11999=CARTESIAN_POINT ( 'NONE',  ( -1.057242234132100167, -5.277754237288139194, 2.597442975781530272 ) ) ;
#12006=CARTESIAN_POINT ( 'NONE',  ( -2.022304719220918479, -5.533262711864405325, 4.346496488058700258 ) ) ;
#12007=CARTESIAN_POINT ( 'NONE',  ( 2.197904923864649529, -2.406019537279079579, 6.187389538303071923 ) ) ;
#12008=CARTESIAN_POINT ( 'NONE',  ( -1.503451935564901643, -3.100827309567759205, 6.886949009567437052 ) ) ;
#12012=CARTESIAN_POINT ( 'NONE',  ( 1.417709711196429856, -3.593722239981790079, 2.821478011237759986 ) ) ;
#12016=CARTESIAN_POINT ( 'NONE',  ( -1.176011442874419943, -2.052854336594789331, 2.320901267448050476 ) ) ;
#12021=CARTESIAN_POINT ( 'NONE',  ( 0.01716182025089369942, -2.169295778036230082, 2.346608583467340026 ) ) ;
#12022=CARTESIAN_POINT ( 'NONE',  ( 0.009452039534070141164, -0.3001931771041043140, 2.350000000173209092 ) ) ;
#12023=CARTESIAN_POINT ( 'NONE',  ( -0.6493550500446439999, -5.586652542372879005, 2.437955526623099889 ) ) ;
#12034=CARTESIAN_POINT ( 'NONE',  ( -0.9485663501270049647, -3.054250732991179440, 6.853826262002260528 ) ) ;
#12035=CARTESIAN_POINT ( 'NONE',  ( 0.2812789908084389889, -5.444279661016950378, 7.036533610117280624 ) ) ;
#12038=CARTESIAN_POINT ( 'NONE',  ( -2.005512128484160161, -1.913124606865060029, 3.468469736471389897 ) ) ;
#12040=CARTESIAN_POINT ( 'NONE',  ( 0.3949552299394610277, -3.776187669928119828, 2.379923265530350385 ) ) ;
#12041=CARTESIAN_POINT ( 'NONE',  ( -1.903446074666951260, -1.680241723982170754, 5.469282057156605426 ) ) ;
#12047=CARTESIAN_POINT ( 'NONE',  ( 1.641313093088730080, -5.335726896972119881, 3.058686906911260106 ) ) ;
#12049=CARTESIAN_POINT ( 'NONE',  ( 0.6096110657044089276, -3.799475958216410376, 2.426869991387509806 ) ) ;
#12052=B_SPLINE_CURVE_WITH_KNOTS ( 'NONE', 3,
 ( #11180, #6836, #2950, #6742, #12567, #3955, #18013, #16727, #5444, #8321, #9979, #7124, #15266, #14044, #12480 ),
 .UNSPECIFIED., .F., .F.,
 ( 4, 1, 1, 1, 1, 1, 1, 1, 1, 1, 1, 1, 4 ),
 ( 0.000000000000000000, 0.04238993203358450146, 0.08487769703118749898, 0.1274691104749350046, 0.1700369147468580033, 0.2126104510726569974, 0.2551841450615619511, 0.2977574123560440267, 0.3403308656858579639, 0.3829042603267339695, 0.4254776701663789962, 0.4680510765563200004, 0.4999998211434326656 ),
 .UNSPECIFIED. ) ;
#12058=CARTESIAN_POINT ( 'NONE',  ( -1.549742865090599997, -5.184322033898309812, 6.471102547561460305 ) ) ;
#12063=CARTESIAN_POINT ( 'NONE',  ( -0.7778405029480311983, -4.614566048306495638, 6.599964735094220991 ) ) ;
#12064=CARTESIAN_POINT ( 'NONE',  ( -2.416676968769249090, -0.5046610169491535514, 5.796598111919839980 ) ) ;
#12067=CARTESIAN_POINT ( 'NONE',  ( 2.011500846714319835, -0.3489406779661020086, 3.478373409938460448 ) ) ;
#12068=CARTESIAN_POINT ( 'NONE',  ( 2.011500846714319835, -0.04894067796610199889, 3.478373409938460448 ) ) ;
#12072=CARTESIAN_POINT ( 'NONE',  ( -1.549742865090599997, -5.484322033898309634, 6.471102547561460305 ) ) ;
#12074=CARTESIAN_POINT ( 'NONE',  ( -1.869848057046539669, -1.311469987729539710, 6.129130480762059463 ) ) ;
#12075=CARTESIAN_POINT ( 'NONE',  ( 2.234315482767910144, -5.359745762711869865, 3.960850823455320580 ) ) ;
#12077=CARTESIAN_POINT ( 'NONE',  ( -0.9279264017968105183, -1.171740257999810852, 7.186376135231811624 ) ) ;
#12082=CARTESIAN_POINT ( 'NONE',  ( 1.586727176531399941, -3.617010528270069969, 2.961885344765599726 ) ) ;
#12087=CARTESIAN_POINT ( 'NONE',  ( 0.3681613504764975620, -3.477280798540335560, 2.680257674196191431 ) ) ;
#12091=CARTESIAN_POINT ( 'NONE',  ( -1.835037444103819970, -1.358046564306109261, 5.620619042473610882 ) ) ;
#12095=CARTESIAN_POINT ( 'NONE',  ( 1.159526867004269768, -0.4480353997208165184, 2.996084454861921209 ) ) ;
#12096=CARTESIAN_POINT ( 'NONE',  ( -1.152986057740030379, -1.753947465207011058, 2.309657588616440549 ) ) ;
#12099=CARTESIAN_POINT ( 'NONE',  ( 2.287919158821199783, -1.051457940198389895, 5.251517552016890633 ) ) ;
#12101=CARTESIAN_POINT ( 'NONE',  ( -2.253200202764409799, -5.211016949152540434, 5.379408587037509903 ) ) ;
#12103=( BOUNDED_SURFACE ( )  B_SPLINE_SURFACE ( 3, 3, ( 
 ( #4926, #12170, #3633, #14946, #10774, #6404, #12075, #8183, #17697, #5323, #5029, #15229, #10685, #2257, #9190, #10969, #10584, #773, #13558, #7809, #7907, #873, #16523, #16237, #6513, #3833, #12447, #16418, #3725, #9383, #8100, #2360, #3914, #6697, #12260, #16614, #13654, #12354, #3543, #6602, #9481, #2533, #15141, #13832, #1152, #6799, #2453, #13739, #17978, #2817, #18064, #16696, #8459, #1614, #3005, #9853, #12622, #12728, #14096, #15328, #4376, #18246 ),
 ( #2636, #5597, #5689, #1326, #16790, #11334, #4105, #17054, #7258, #5407, #11046, #12532, #8285, #1427, #4004, #11242, #4282, #15425, #9658, #13927, #9939, #1244, #2732, #8378, #7085, #14012, #11420, #16886, #6973, #46, #14293, #16970, #6886, #15512, #18145, #4193, #15599, #8560, #5493, #11136, #2912, #9760, #14206, #12816, #1527, #7176, #128, #5778, #10038, #15694, #8646, #17498, #14557, #578, #3170, #7439, #10384, #8989, #15966, #10299, #5953, #2048 ),
 ( #11593, #3267, #1871, #8909, #7520, #11511, #17141, #15861, #4544, #313, #6127, #4465, #11790, #10123, #15777, #6039, #16046, #12901, #10197, #13164, #13080, #1795, #480, #17412, #14372, #3344, #9074, #400, #4816, #3085, #14638, #7351, #8728, #4734, #11685, #4639, #1699, #17311, #1951, #14477, #17222, #7609, #8827, #11878, #223, #5864, #12993, #13258, #6219, #10466, #16126, #3423, #14734, #5017, #13349, #16221, #12242, #3528, #10669, #16315, #3708, #3620 ),
 ( #15126, #9270, #17774, #16404, #12335, #10950, #663, #14931, #17573, #9554, #950, #857, #9173, #13443, #13725, #753, #2150, #15029, #10852, #9464, #6497, #6387, #12156, #17862, #16597, #6301, #17957, #11960, #7795, #5200, #15213, #7703, #16500, #7993, #12058, #17678, #2241, #5107, #9358, #10759, #2344, #4907, #10562, #7885, #13539, #13639, #6588, #14835, #3814, #2439, #8086, #1041, #6677, #5303, #3900, #12428, #6781, #2794, #2520, #4081, #8438, #10016 ),
 ( #5668, #12514, #1502, #4257, #9831, #8536, #13988, #16947, #13808, #8167, #1398, #14186, #2706, #7157, #5754, #12794, #1221, #1133, #18047, #1306, #11310, #5391, #11031, #16679, #3987, #14072, #9636, #9740, #7065, #15303, #8355, #15403, #2615, #9916, #18127, #107, #15574, #15487, #11396, #6952, #2886, #8266, #13907, #12706, #17028, #12598, #4351, #6867, #5476, #11116, #16763, #23, #5574, #18219, #11219, #16863, #4170, #801, #7415, #10176, #10268, #376 ),
 ( #4610, #15840, #13056, #12877, #3139, #3242, #17201, #14347, #8885, #1672, #14881, #5060, #15676, #2985, #10104, #191, #17284, #8627, #8797, #2096, #12968, #14269, #5836, #7747, #11488, #292, #5930, #11660, #11570, #9217, #14448, #4525, #15937, #12111, #14535, #1592, #6016, #17120, #1768, #13393, #6342, #15755, #3062, #707, #7322, #12006, #10618, #4444, #17624, #17730, #4963, #16267, #3570, #2195, #7839, #13486, #6442, #7234, #8705, #8213, #6827, #13761 ),
 ( #10993, #5151, #2395, #3758, #8125, #12383, #1083, #6729, #9311, #14980, #13685, #8043, #16447, #3943, #2291, #9598, #993, #9419, #18005, #5349, #16641, #15254, #7944, #13592, #6630, #12287, #15085, #2559, #907, #13860, #6545, #12198, #3859, #1179, #10711, #17814, #10801, #17908, #12471, #16357, #5249, #18089, #18171, #16552, #10905, #9512, #5436, #15170, #9685, #11076, #16720, #4031, #2481, #15356, #3662, #2660, #8313, #13951, #1268, #6912, #12560, #15795 ) ),
 .UNSPECIFIED., .T., .F., .F. ) 
 B_SPLINE_SURFACE_WITH_KNOTS ( ( 4, 3, 4 ),
 ( 4, 1, 1, 1, 1, 1, 1, 1, 1, 1, 1, 1, 1, 1, 1, 1, 1, 1, 1, 1, 1, 1, 1, 1, 1, 1, 1, 1, 1, 1, 1, 1, 1, 1, 1, 1, 1, 1, 1, 1, 1, 1, 1, 1, 1, 1, 1, 1, 1, 1, 1, 1, 1, 1, 1, 1, 1, 1, 1, 4 ),
 ( 0.000000000000000000, 3.141592653589790007, 6.283185307179590673 ),
 ( 0.7853981633974479459, 0.8785809963429079827, 0.9717638292883680196, 1.064946662233830166, 1.158129495179289981, 1.251312328124750017, 1.344495161070210054, 1.437677994015669869, 1.530860826961130128, 1.624043659906589943, 1.717226492852049979, 1.810409325797510016, 1.903592158742969831, 1.996774991688430090, 2.089957824633889683, 2.183140657579349941, 2.276323490524809756, 2.369506323470270015, 2.462689156415730274, 2.555871989361190089, 2.649054822306649903, 2.742237655252109718, 2.835420488197569977, 2.928603321143030236, 3.021786154088490051, 3.114968987033949865, 3.208151819979410124, 3.301334652924869939, 3.394517485870330198, 3.487700318815790013, 3.580883151761249827, 3.674065984706710086, 3.767248817652169901, 3.860431650597620390, 3.953614483543080205, 4.046797316488540019, 4.139980149433999834, 4.233162982379460537, 4.326345815324920352, 4.419528648270380167, 4.512711481215839981, 4.605894314161299796, 4.699077147106759611, 4.792259980052219426, 4.885442812997680129, 4.978625645943139943, 5.071808478888599758, 5.164991311834059573, 5.258174144779520276, 5.351356977724980091, 5.444539810670439905, 5.537722643615899720, 5.630905476561360423, 5.724088309506820238, 5.817271142452280053, 5.910453975397739868, 6.003636808343199682, 6.096819641288659497, 6.190002474234119312, 6.283185307179590673 ),
 .UNSPECIFIED. ) 
 GEOMETRIC_REPRESENTATION_ITEM ( )  RATIONAL_B_SPLINE_SURFACE ( (
 ( 1.000000000000000000, 1.000000000000000000, 1.000000000000000000, 1.000000000000000000, 1.000000000000000000, 1.000000000000000000, 1.000000000000000000, 1.000000000000000000, 1.000000000000000000, 1.000000000000000000, 1.000000000000000000, 1.000000000000000000, 1.000000000000000000, 1.000000000000000000, 1.000000000000000000, 1.000000000000000000, 1.000000000000000000, 1.000000000000000000, 1.000000000000000000, 1.000000000000000000, 1.000000000000000000, 1.000000000000000000, 1.000000000000000000, 1.000000000000000000, 1.000000000000000000, 1.000000000000000000, 1.000000000000000000, 1.000000000000000000, 1.000000000000000000, 1.000000000000000000, 1.000000000000000000, 1.000000000000000000, 1.000000000000000000, 1.000000000000000000, 1.000000000000000000, 1.000000000000000000, 1.000000000000000000, 1.000000000000000000, 1.000000000000000000, 1.000000000000000000, 1.000000000000000000, 1.000000000000000000, 1.000000000000000000, 1.000000000000000000, 1.000000000000000000, 1.000000000000000000, 1.000000000000000000, 1.000000000000000000, 1.000000000000000000, 1.000000000000000000, 1.000000000000000000, 1.000000000000000000, 1.000000000000000000, 1.000000000000000000, 1.000000000000000000, 1.000000000000000000, 1.000000000000000000, 1.000000000000000000, 1.000000000000000000, 1.000000000000000000, 1.000000000000000000, 1.000000000000000000),
 ( 0.3333333333333329818, 0.3333333333333329818, 0.3333333333333329818, 0.3333333333333329818, 0.3333333333333329818, 0.3333333333333329818, 0.3333333333333329818, 0.3333333333333329818, 0.3333333333333329818, 0.3333333333333329818, 0.3333333333333329818, 0.3333333333333329818, 0.3333333333333329818, 0.3333333333333329818, 0.3333333333333329818, 0.3333333333333329818, 0.3333333333333329818, 0.3333333333333329818, 0.3333333333333329818, 0.3333333333333329818, 0.3333333333333329818, 0.3333333333333329818, 0.3333333333333329818, 0.3333333333333329818, 0.3333333333333329818, 0.3333333333333329818, 0.3333333333333329818, 0.3333333333333329818, 0.3333333333333329818, 0.3333333333333329818, 0.3333333333333329818, 0.3333333333333329818, 0.3333333333333329818, 0.3333333333333329818, 0.3333333333333329818, 0.3333333333333329818, 0.3333333333333329818, 0.3333333333333329818, 0.3333333333333329818, 0.3333333333333329818, 0.3333333333333329818, 0.3333333333333329818, 0.3333333333333329818, 0.3333333333333329818, 0.3333333333333329818, 0.3333333333333329818, 0.3333333333333329818, 0.3333333333333329818, 0.3333333333333329818, 0.3333333333333329818, 0.3333333333333329818, 0.3333333333333329818, 0.3333333333333329818, 0.3333333333333329818, 0.3333333333333329818, 0.3333333333333329818, 0.3333333333333329818, 0.3333333333333329818, 0.3333333333333329818, 0.3333333333333329818, 0.3333333333333329818, 0.3333333333333329818),
 ( 0.3333333333333329818, 0.3333333333333329818, 0.3333333333333329818, 0.3333333333333329818, 0.3333333333333329818, 0.3333333333333329818, 0.3333333333333329818, 0.3333333333333329818, 0.3333333333333329818, 0.3333333333333329818, 0.3333333333333329818, 0.3333333333333329818, 0.3333333333333329818, 0.3333333333333329818, 0.3333333333333329818, 0.3333333333333329818, 0.3333333333333329818, 0.3333333333333329818, 0.3333333333333329818, 0.3333333333333329818, 0.3333333333333329818, 0.3333333333333329818, 0.3333333333333329818, 0.3333333333333329818, 0.3333333333333329818, 0.3333333333333329818, 0.3333333333333329818, 0.3333333333333329818, 0.3333333333333329818, 0.3333333333333329818, 0.3333333333333329818, 0.3333333333333329818, 0.3333333333333329818, 0.3333333333333329818, 0.3333333333333329818, 0.3333333333333329818, 0.3333333333333329818, 0.3333333333333329818, 0.3333333333333329818, 0.3333333333333329818, 0.3333333333333329818, 0.3333333333333329818, 0.3333333333333329818, 0.3333333333333329818, 0.3333333333333329818, 0.3333333333333329818, 0.3333333333333329818, 0.3333333333333329818, 0.3333333333333329818, 0.3333333333333329818, 0.3333333333333329818, 0.3333333333333329818, 0.3333333333333329818, 0.3333333333333329818, 0.3333333333333329818, 0.3333333333333329818, 0.3333333333333329818, 0.3333333333333329818, 0.3333333333333329818, 0.3333333333333329818, 0.3333333333333329818, 0.3333333333333329818),
 ( 1.000000000000000000, 1.000000000000000000, 1.000000000000000000, 1.000000000000000000, 1.000000000000000000, 1.000000000000000000, 1.000000000000000000, 1.000000000000000000, 1.000000000000000000, 1.000000000000000000, 1.000000000000000000, 1.000000000000000000, 1.000000000000000000, 1.000000000000000000, 1.000000000000000000, 1.000000000000000000, 1.000000000000000000, 1.000000000000000000, 1.000000000000000000, 1.000000000000000000, 1.000000000000000000, 1.000000000000000000, 1.000000000000000000, 1.000000000000000000, 1.000000000000000000, 1.000000000000000000, 1.000000000000000000, 1.000000000000000000, 1.000000000000000000, 1.000000000000000000, 1.000000000000000000, 1.000000000000000000, 1.000000000000000000, 1.000000000000000000, 1.000000000000000000, 1.000000000000000000, 1.000000000000000000, 1.000000000000000000, 1.000000000000000000, 1.000000000000000000, 1.000000000000000000, 1.000000000000000000, 1.000000000000000000, 1.000000000000000000, 1.000000000000000000, 1.000000000000000000, 1.000000000000000000, 1.000000000000000000, 1.000000000000000000, 1.000000000000000000, 1.000000000000000000, 1.000000000000000000, 1.000000000000000000, 1.000000000000000000, 1.000000000000000000, 1.000000000000000000, 1.000000000000000000, 1.000000000000000000, 1.000000000000000000, 1.000000000000000000, 1.000000000000000000, 1.000000000000000000),
 ( 0.3333333333333329818, 0.3333333333333329818, 0.3333333333333329818, 0.3333333333333329818, 0.3333333333333329818, 0.3333333333333329818, 0.3333333333333329818, 0.3333333333333329818, 0.3333333333333329818, 0.3333333333333329818, 0.3333333333333329818, 0.3333333333333329818, 0.3333333333333329818, 0.3333333333333329818, 0.3333333333333329818, 0.3333333333333329818, 0.3333333333333329818, 0.3333333333333329818, 0.3333333333333329818, 0.3333333333333329818, 0.3333333333333329818, 0.3333333333333329818, 0.3333333333333329818, 0.3333333333333329818, 0.3333333333333329818, 0.3333333333333329818, 0.3333333333333329818, 0.3333333333333329818, 0.3333333333333329818, 0.3333333333333329818, 0.3333333333333329818, 0.3333333333333329818, 0.3333333333333329818, 0.3333333333333329818, 0.3333333333333329818, 0.3333333333333329818, 0.3333333333333329818, 0.3333333333333329818, 0.3333333333333329818, 0.3333333333333329818, 0.3333333333333329818, 0.3333333333333329818, 0.3333333333333329818, 0.3333333333333329818, 0.3333333333333329818, 0.3333333333333329818, 0.3333333333333329818, 0.3333333333333329818, 0.3333333333333329818, 0.3333333333333329818, 0.3333333333333329818, 0.3333333333333329818, 0.3333333333333329818, 0.3333333333333329818, 0.3333333333333329818, 0.3333333333333329818, 0.3333333333333329818, 0.3333333333333329818, 0.3333333333333329818, 0.3333333333333329818, 0.3333333333333329818, 0.3333333333333329818),
 ( 0.3333333333333329818, 0.3333333333333329818, 0.3333333333333329818, 0.3333333333333329818, 0.3333333333333329818, 0.3333333333333329818, 0.3333333333333329818, 0.3333333333333329818, 0.3333333333333329818, 0.3333333333333329818, 0.3333333333333329818, 0.3333333333333329818, 0.3333333333333329818, 0.3333333333333329818, 0.3333333333333329818, 0.3333333333333329818, 0.3333333333333329818, 0.3333333333333329818, 0.3333333333333329818, 0.3333333333333329818, 0.3333333333333329818, 0.3333333333333329818, 0.3333333333333329818, 0.3333333333333329818, 0.3333333333333329818, 0.3333333333333329818, 0.3333333333333329818, 0.3333333333333329818, 0.3333333333333329818, 0.3333333333333329818, 0.3333333333333329818, 0.3333333333333329818, 0.3333333333333329818, 0.3333333333333329818, 0.3333333333333329818, 0.3333333333333329818, 0.3333333333333329818, 0.3333333333333329818, 0.3333333333333329818, 0.3333333333333329818, 0.3333333333333329818, 0.3333333333333329818, 0.3333333333333329818, 0.3333333333333329818, 0.3333333333333329818, 0.3333333333333329818, 0.3333333333333329818, 0.3333333333333329818, 0.3333333333333329818, 0.3333333333333329818, 0.3333333333333329818, 0.3333333333333329818, 0.3333333333333329818, 0.3333333333333329818, 0.3333333333333329818, 0.3333333333333329818, 0.3333333333333329818, 0.3333333333333329818, 0.3333333333333329818, 0.3333333333333329818, 0.3333333333333329818, 0.3333333333333329818),
 ( 1.000000000000000000, 1.000000000000000000, 1.000000000000000000, 1.000000000000000000, 1.000000000000000000, 1.000000000000000000, 1.000000000000000000, 1.000000000000000000, 1.000000000000000000, 1.000000000000000000, 1.000000000000000000, 1.000000000000000000, 1.000000000000000000, 1.000000000000000000, 1.000000000000000000, 1.000000000000000000, 1.000000000000000000, 1.000000000000000000, 1.000000000000000000, 1.000000000000000000, 1.000000000000000000, 1.000000000000000000, 1.000000000000000000, 1.000000000000000000, 1.000000000000000000, 1.000000000000000000, 1.000000000000000000, 1.000000000000000000, 1.000000000000000000, 1.000000000000000000, 1.000000000000000000, 1.000000000000000000, 1.000000000000000000, 1.000000000000000000, 1.000000000000000000, 1.000000000000000000, 1.000000000000000000, 1.000000000000000000, 1.000000000000000000, 1.000000000000000000, 1.000000000000000000, 1.000000000000000000, 1.000000000000000000, 1.000000000000000000, 1.000000000000000000, 1.000000000000000000, 1.000000000000000000, 1.000000000000000000, 1.000000000000000000, 1.000000000000000000, 1.000000000000000000, 1.000000000000000000, 1.000000000000000000, 1.000000000000000000, 1.000000000000000000, 1.000000000000000000, 1.000000000000000000, 1.000000000000000000, 1.000000000000000000, 1.000000000000000000, 1.000000000000000000, 1.000000000000000000) ) ) 
 REPRESENTATION_ITEM ( '' )  SURFACE ( )  );
#12111=CARTESIAN_POINT ( 'NONE',  ( -1.202278654260740876, -5.479872881355935199, 6.364093491318035589 ) ) ;
#12112=CARTESIAN_POINT ( 'NONE',  ( -2.398725280367459245, -3.151244762504313179, 3.564557036955213754 ) ) ;
#12114=CARTESIAN_POINT ( 'NONE',  ( -1.700860513939528751, -3.124115597856051085, 6.737200825918551850 ) ) ;
#12117=CARTESIAN_POINT ( 'NONE',  ( -1.928817277882840076, -4.455388906648449776, 6.048484184565969812 ) ) ;
#12121=CARTESIAN_POINT ( 'NONE',  ( -1.963178672446121098, -1.959701183441630024, 2.914210764660470687 ) ) ;
#12125=CARTESIAN_POINT ( 'NONE',  ( 1.928817277882869829, -1.144611093351550091, 6.048484184565929844 ) ) ;
#12128=CARTESIAN_POINT ( 'NONE',  ( -1.248294325655370018, -5.573305084745760141, 2.704938983774309857 ) ) ;
#12134=AXIS2_PLACEMENT_3D ( 'NONE', #6746, #12398, #18017 ) ;
#12135=CARTESIAN_POINT ( 'NONE',  ( 1.832842064134690085, -2.728214696955149954, 6.176291182464479945 ) ) ;
#12137=CARTESIAN_POINT ( 'NONE',  ( -1.057242234132100167, -5.577754237288139905, 2.597442975781530272 ) ) ;
#12139=CARTESIAN_POINT ( 'NONE',  ( -1.044181395669830259, -2.052854336594790219, 2.590869634085910089 ) ) ;
#12141=CARTESIAN_POINT ( 'NONE',  ( -1.978802102381380879, -1.843259742000191048, 4.152967933079680485 ) ) ;
#12142=CARTESIAN_POINT ( 'NONE',  ( 1.194742379459969861, -0.4245762711864409789, 6.727584234649759409 ) ) ;
#12146=CARTESIAN_POINT ( 'NONE',  ( 1.553986151955640160, -0.6610754142986889903, 3.144168668454419890 ) ) ;
#12148=CARTESIAN_POINT ( 'NONE',  ( 1.994983296312400123, -4.265241723982169830, 5.948514050749290405 ) ) ;
#12156=CARTESIAN_POINT ( 'NONE',  ( 0.9150601050661639757, -5.130932203389829915, 6.868218666554230190 ) ) ;
#12161=CARTESIAN_POINT ( 'NONE',  ( -2.260890494820599894, -1.544352870612419881, 4.046455925041199997 ) ) ;
#12163=CARTESIAN_POINT ( 'NONE',  ( -1.117157304995339606, -4.661142624883069630, 6.422457952614126775 ) ) ;
#12164=CARTESIAN_POINT ( 'NONE',  ( 0.5889081234606849957, -0.1379237288135600203, 6.978529000034869867 ) ) ;
#12166=CARTESIAN_POINT ( 'NONE',  ( -2.191755591049691532, -0.2536016949152540834, 3.203650300307721466 ) ) ;
#12168=CARTESIAN_POINT ( 'NONE',  ( -0.6493550500446439999, -5.586652542372879005, 2.437955526623099889 ) ) ;
#12169=CARTESIAN_POINT ( 'NONE',  ( -1.994983296312368815, -1.334758276017820045, 5.948514050749341919 ) ) ;
#12170=CARTESIAN_POINT ( 'NONE',  ( 1.713314936023349944, -5.338983050847460277, 3.089913064446569546 ) ) ;
#12171=CARTESIAN_POINT ( 'NONE',  ( 1.835211330903820937, -0.8922807985403484743, 6.617058440403981834 ) ) ;
#12173=CARTESIAN_POINT ( 'NONE',  ( -1.505092429369619955, -5.128627060139309357, 2.879659483602799774 ) ) ;
#12174=CARTESIAN_POINT ( 'NONE',  ( 0.3752419433107369584, -4.175929447188989840, 7.023346545710360544 ) ) ;
#12175=CARTESIAN_POINT ( 'NONE',  ( 0.9279264017968674727, -4.428259742000194343, 7.186376135231798301 ) ) ;
#12178=CARTESIAN_POINT ( 'NONE',  ( -1.292934267244330471, -4.385524041783587457, 6.294748514096648151 ) ) ;
#12180=CARTESIAN_POINT ( 'NONE',  ( -2.053018524985070314, -1.474488005747551567, 4.695903819313384631 ) ) ;
#12186=CARTESIAN_POINT ( 'NONE',  ( 2.435897774776379698, -2.359442960702510472, 5.753335522918191280 ) ) ;
#12191=CARTESIAN_POINT ( 'NONE',  ( 1.782460458101500889, -5.099788135593215976, 5.718585207845976015 ) ) ;
#12198=CARTESIAN_POINT ( 'NONE',  ( -1.000896394980330006, -5.470974576271190770, 6.829956240957379521 ) ) ;
#12199=CARTESIAN_POINT ( 'NONE',  ( -1.853635285637788899, -4.408812330071866015, 6.599249831075526984 ) ) ;
#12203=CARTESIAN_POINT ( 'NONE',  ( -2.046174187462380445, -4.478677194936739880, 5.862719605944009871 ) ) ;
#12207=CARTESIAN_POINT ( 'NONE',  ( 2.398725280367429047, -2.448755237495690462, 3.564557036955152913 ) ) ;
#12211=CARTESIAN_POINT ( 'NONE',  ( 1.438959988998139914E-16, -0.2999999999999999889, 2.350000000000000089 ) ) ;
#12213=CARTESIAN_POINT ( 'NONE',  ( 1.611907055891590002, -2.355602084342530045, 2.985210995296850189 ) ) ;
#12216=CARTESIAN_POINT ( 'NONE',  ( -2.306642602145299925, -5.515466101694909362, 5.166805192608490138 ) ) ;
#12219=CARTESIAN_POINT ( 'NONE',  ( 0.009417288784633505092, -0.3007439470567257467, 2.370019840861780303 ) ) ;
#12222=CARTESIAN_POINT ( 'NONE',  ( 1.397172971746949877, -3.892629111369559691, 2.806153814454899642 ) ) ;
#12225=CARTESIAN_POINT ( 'NONE',  ( -0.2189795514005259958, -5.595550847457629651, 2.356806637999020015 ) ) ;
#12227=CARTESIAN_POINT ( 'NONE',  ( -0.5320716618283710675, -3.007674156414609890, 6.992519451207139802 ) ) ;
#12228=CARTESIAN_POINT ( 'NONE',  ( -1.670747221194380128, -5.103620102360550526, 3.047345349617600174 ) ) ;
#12229=CARTESIAN_POINT ( 'NONE',  ( -1.491388273268980491, -1.587088570829020551, 6.110908523251552538 ) ) ;
#12232=CARTESIAN_POINT ( 'NONE',  ( -0.2097343361107079085, -0.5962015548080615845, 2.050670208512068715 ) ) ;
#12234=CARTESIAN_POINT ( 'NONE',  ( 1.554908741750600232, -5.202797822590530252, 3.145091258249389732 ) ) ;
#12236=CARTESIAN_POINT ( 'NONE',  ( -2.239137794397029868, -4.987178660919110662, 3.975425900939220103 ) ) ;
#12242=CARTESIAN_POINT ( 'NONE',  ( -0.9664230948142090716, -5.282203389830510076, 2.228384861502259895 ) ) ;
#12245=CARTESIAN_POINT ( 'NONE',  ( 1.820241257191439921, -0.5196681859277348936, 3.208199930689769719 ) ) ;
#12247=CARTESIAN_POINT ( 'NONE',  ( 2.329383452786330189, -1.028169651910100013, 5.035735636132829818 ) ) ;
#12248=CARTESIAN_POINT ( 'NONE',  ( 1.889104232906359870, -0.04449152542372909747, 3.296507079072520163 ) ) ;
#12252=CARTESIAN_POINT ( 'NONE',  ( -1.940327948426050941, -0.5091101694915260989, 5.370677689277675526 ) ) ;
#12254=CARTESIAN_POINT ( 'NONE',  ( -2.321479326063761395, -0.2491525423728809807, 3.414080590619972710 ) ) ;
#12258=CARTESIAN_POINT ( 'NONE',  ( -2.353452300571019506, -1.474488005747550456, 4.697179287168410156 ) ) ;
#12260=CARTESIAN_POINT ( 'NONE',  ( -1.549742865090599997, -5.484322033898309634, 6.471102547561460305 ) ) ;
#12261=CARTESIAN_POINT ( 'NONE',  ( -1.579331079541819394, -1.241605122864670285, 6.832797935622397567 ) ) ;
#12263=CARTESIAN_POINT ( 'NONE',  ( -0.1686436619862690112, -4.981295943764799894, 2.349239845786320391 ) ) ;
#12264=CARTESIAN_POINT ( 'NONE',  ( 1.003115764947319910, -4.106064582324129297, 6.828967930617570126 ) ) ;
#12268=CARTESIAN_POINT ( 'NONE',  ( -1.919159680931840084, -1.866548030288480042, 3.970803207828165426 ) ) ;
#12270=CARTESIAN_POINT ( 'NONE',  ( 2.045969882616350155, -3.803316834576382366, 4.529973290172005562 ) ) ;
#12274=CARTESIAN_POINT ( 'NONE',  ( -2.030998484741458832, -0.2180084745762719822, 4.999543428097190656 ) ) ;
#12275=CARTESIAN_POINT ( 'NONE',  ( 1.458615186838411626, -0.4963798976394455664, 3.259477383973563125 ) ) ;
#12276=CARTESIAN_POINT ( 'NONE',  ( 2.197904923864649529, -2.406019537279079579, 6.187389538303071923 ) ) ;
#12280=CARTESIAN_POINT ( 'NONE',  ( -1.246151616534680651, -5.268855932203385883, 3.068501529594771071 ) ) ;
#12287=CARTESIAN_POINT ( 'NONE',  ( 0.2812789908084389889, -5.444279661016950378, 7.036533610117280624 ) ) ;
#12288=CARTESIAN_POINT ( 'NONE',  ( 1.351547610267151533, -4.082776294035843634, 6.983951126925231456 ) ) ;
#12289=CARTESIAN_POINT ( 'NONE',  ( 1.545075033357670158, -0.4774152569121719036, 2.920238509828300799 ) ) ;
#12290=CARTESIAN_POINT ( 'NONE',  ( -2.589141052314440916, -3.287133615874059611, 5.282633936723525991 ) ) ;
#12293=CARTESIAN_POINT ( 'NONE',  ( -0.7109160811435620841, -4.292370888630429704, 6.943511536198419876 ) ) ;
#12296=CARTESIAN_POINT ( 'NONE',  ( -0.3578984759183553854, -2.984385868126320673, 7.329643012642057087 ) ) ;
#12299=CARTESIAN_POINT ( 'NONE',  ( 2.318251751302029984, -0.3667372881355940306, 4.294764266798990704 ) ) ;
#12300=CARTESIAN_POINT ( 'NONE',  ( -1.044181395669830259, -2.052854336594790219, 2.590869634085910089 ) ) ;
#12301=CARTESIAN_POINT ( 'NONE',  ( -1.300961508564169922, -0.4779661016949160457, 6.661123742937279602 ) ) ;
#12302=CARTESIAN_POINT ( 'NONE',  ( -2.011500846714319835, -5.551059322033900401, 3.478373409938470218 ) ) ;
#12306=CARTESIAN_POINT ( 'NONE',  ( -1.194742379459959869, -5.175423728813559165, 6.727584234649758521 ) ) ;
#12308=CARTESIAN_POINT ( 'NONE',  ( 0.006176317641841110387, -0.3521105953074989969, 2.465914288053659753 ) ) ;
#12314=CARTESIAN_POINT ( 'NONE',  ( 0.6150581927482109412, -4.451548030288480895, 6.971662190339319665 ) ) ;
#12320=CARTESIAN_POINT ( 'NONE',  ( -0.6343239990445920240, -2.099430913171359769, 2.433641963034089972 ) ) ;
#12322=CARTESIAN_POINT ( 'NONE',  ( 1.810994336139499783, -2.681638120378568857, 5.667058093962681120 ) ) ;
#12325=CARTESIAN_POINT ( 'NONE',  ( -1.873832970144350130, -0.5625000000000005551, 2.826167029855650270 ) ) ;
#12335=CARTESIAN_POINT ( 'NONE',  ( 2.058670345754650022, -5.050847457627120285, 3.559656372813920111 ) ) ;
#12340=CARTESIAN_POINT ( 'NONE',  ( -2.316126390218390618, -4.734848366107908824, 3.404364157709380390 ) ) ;
#12341=DIRECTION ( 'NONE',  ( -0.06030856937325100586, -0.9963562379592471041, 0.06030856937324956257 ) ) ;
#12342=CARTESIAN_POINT ( 'NONE',  ( -1.197297565406129971, -1.517223705964160008, 6.726135293448209929 ) ) ;
#12344=CARTESIAN_POINT ( 'NONE',  ( 2.180207327701309872, -0.09343220338983100615, 5.586116916730190063 ) ) ;
#12346=CARTESIAN_POINT ( 'NONE',  ( -2.155845792290839835, -0.5447033898305089217, 3.756158857535780271 ) ) ;
#12349=CARTESIAN_POINT ( 'NONE',  ( 2.087380238839969593, -0.1067796610169500227, 6.338810156469096846 ) ) ;
#12353=CARTESIAN_POINT ( 'NONE',  ( 1.626408692231650299, -0.8922807985403480302, 6.401040991074950171 ) ) ;
#12354=CARTESIAN_POINT ( 'NONE',  ( -1.978267656359410154, -5.497669491525420504, 5.974740860598790171 ) ) ;
#12356=CARTESIAN_POINT ( 'NONE',  ( -2.471388659209118543, -1.381334852594401363, 5.667135868497515716 ) ) ;
#12360=CARTESIAN_POINT ( 'NONE',  ( 2.036910256464071090, -0.6593979156574641953, 4.443293066459086837 ) ) ;
#12361=CARTESIAN_POINT ( 'NONE',  ( -0.2908063684825371031, -4.544701183441625325, 7.337905485238597869 ) ) ;
#12366=CARTESIAN_POINT ( 'NONE',  ( 0.8014931112107362976, -1.284340823081270733, 6.590108630558003000 ) ) ;
#12371=CARTESIAN_POINT ( 'NONE',  ( 0.5664586606772286093, -0.3133474576271193524, 2.726727161522279452 ) ) ;
#12373=CARTESIAN_POINT ( 'NONE',  ( -2.339254516529639449, -2.918361879621429011, 5.953396186326395778 ) ) ;
#12374=CARTESIAN_POINT ( 'NONE',  ( -0.8092638295168710361, -4.911779243796849492, 2.486823565593869745 ) ) ;
#12375=CARTESIAN_POINT ( 'NONE',  ( -1.088937603231280304, -5.273305084745764759, 2.959627624143549074 ) ) ;
#12383=CARTESIAN_POINT ( 'NONE',  ( 2.155845792290829621, -5.355296610169490101, 3.756158857535770057 ) ) ;
#12386=CARTESIAN_POINT ( 'NONE',  ( -2.306572132003601450, -4.478677194936736328, 6.012569500204175910 ) ) ;
#12387=CARTESIAN_POINT ( 'NONE',  ( -2.008025181017680794, -3.520016498756949552, 2.964791492240541171 ) ) ;
#12389=CARTESIAN_POINT ( 'NONE',  ( -2.151546283159490258, -4.711560077819619607, 3.746273477677509955 ) ) ;
#12394=CARTESIAN_POINT ( 'NONE',  ( 1.255262969126039558E-16, -0.3000000000000002665, 2.050000000000001155 ) ) ;
#12396=CARTESIAN_POINT ( 'NONE',  ( 2.347833536521260367, -2.541908390648839777, 4.537447324629859224 ) ) ;
#12398=DIRECTION ( 'NONE',  ( 0.7071067811865470176, 4.329780281177469511E-17, -0.7071067811865480168 ) ) ;
#12399=CARTESIAN_POINT ( 'NONE',  ( 0.3171869470818560743, -5.444279661016954819, 7.334814496515233095 ) ) ;
#12402=CARTESIAN_POINT ( 'NONE',  ( 0.2812789908084389334, -5.144279661016949667, 7.036533610117277959 ) ) ;
#12406=CARTESIAN_POINT ( 'NONE',  ( 1.219286470748990103, -4.381683165423610582, 6.712979431025659416 ) ) ;
#12412=CARTESIAN_POINT ( 'NONE',  ( -0.4201920264140019956, -2.122719201459649874, 2.384360920086639801 ) ) ;
#12414=CARTESIAN_POINT ( 'NONE',  ( -0.9123513484652393535, -2.052854336594789331, 2.860838000723768815 ) ) ;
#12420=CARTESIAN_POINT ( 'NONE',  ( -0.2564439965878500538, -4.544701183441629766, 7.039440566481220074 ) ) ;
#12424=ORIENTED_EDGE ( 'NONE', *, *, #17579, .F. ) ;
#12428=CARTESIAN_POINT ( 'NONE',  ( -1.057242234132100167, -5.277754237288139194, 2.597442975781530272 ) ) ;
#12434=CARTESIAN_POINT ( 'NONE',  ( 2.151546283159470274, -0.8884399221803740421, 3.746273477677459773 ) ) ;
#12435=CARTESIAN_POINT ( 'NONE',  ( -2.321479326063761395, -0.2491525423728809807, 3.414080590619972710 ) ) ;
#12440=CARTESIAN_POINT ( 'NONE',  ( -1.467041701146829746, -0.1779661016949160846, 6.911479965439912831 ) ) ;
#12445=CARTESIAN_POINT ( 'NONE',  ( 1.097561405233190568, -1.986830348089889897, 2.618148744692250673 ) ) ;
#12447=CARTESIAN_POINT ( 'NONE',  ( 0.06264882350516240428, -5.448728813559320372, 7.052569299041220319 ) ) ;
#12448=CARTESIAN_POINT ( 'NONE',  ( 2.199635523370541357, -0.5429564742160235546, 3.215170965528963531 ) ) ;
#12449=EDGE_LOOP ( 'NONE', ( #17180, #452, #1933, #1862 ) ) ;
#12450=CARTESIAN_POINT ( 'NONE',  ( -0.8001898266890440370, -1.470647129387580021, 6.913242401714570384 ) ) ;
#12451=CARTESIAN_POINT ( 'NONE',  ( 1.861802609626429961, -0.7991276453871953844, 5.565212624397201324 ) ) ;
#12452=CARTESIAN_POINT ( 'NONE',  ( -1.008962495263940662, -4.614566048306495638, 7.154609617872592864 ) ) ;
#12456=CARTESIAN_POINT ( 'NONE',  ( 1.790316459643169100, -0.8651516338920848259, 3.695177221627173214 ) ) ;
#12461=CARTESIAN_POINT ( 'NONE',  ( -1.432215783582709401, -0.1868644067796619845, 6.170863372171116801 ) ) ;
#12463=CARTESIAN_POINT ( 'NONE',  ( -0.1366863161730529075, -2.662190708450249854, 7.350364228549148393 ) ) ;
#12464=CARTESIAN_POINT ( 'NONE',  ( 0.009452110982653640428, -5.000192044704539818, 2.350000000000000089 ) ) ;
#12465=CARTESIAN_POINT ( 'NONE',  ( 1.134881315981519645, -5.422033898305085309, 6.410767520434657918 ) ) ;
#12471=CARTESIAN_POINT ( 'NONE',  ( -2.088297318559229954, -5.502118644067800268, 5.785136623276639689 ) ) ;
#12472=CARTESIAN_POINT ( 'NONE',  ( -2.185196738168510233, -4.758136654396205145, 3.194002352996703653 ) ) ;
#12473=CARTESIAN_POINT ( 'NONE',  ( 2.642463257358089734, -4.148800282540726414, 4.945970783863369746 ) ) ;
#12476=CARTESIAN_POINT ( 'NONE',  ( -1.803891155489810050, -4.781424942684489920, 3.188470185434129966 ) ) ;
#12480=CARTESIAN_POINT ( 'NONE',  ( 1.661700935665417544, -5.037501140877957084, 3.038299064334577082 ) ) ;
#12481=CARTESIAN_POINT ( 'NONE',  ( -1.811729841638700211, -0.5580508474576270084, 3.197954009834299782 ) ) ;
#12482=CARTESIAN_POINT ( 'NONE',  ( 2.301223891756920104, -2.611773255513699876, 5.193066210047949660 ) ) ;
#12485=CARTESIAN_POINT ( 'NONE',  ( -2.560337424259679917, -5.537711864406785978, 4.001768473655595848 ) ) ;
#12488=CARTESIAN_POINT ( 'NONE',  ( -0.4360591020458099987, -5.291101694915249176, 2.387347919655840034 ) ) ;
#12494=CARTESIAN_POINT ( 'NONE',  ( 1.869848057046569867, -4.288530012270459935, 6.129130480762009725 ) ) ;
#12497=CARTESIAN_POINT ( 'NONE',  ( 1.151392222988870895, -5.028306595106930565, 2.990827770388080342 ) ) ;
#12500=CARTESIAN_POINT ( 'NONE',  ( 1.021156010535390068, -3.846052534792979927, 2.579625955254269964 ) ) ;
#12502=CARTESIAN_POINT ( 'NONE',  ( -1.279347147864589251, -3.566593075333521767, 3.094331068408299412 ) ) ;
#12504=CARTESIAN_POINT ( 'NONE',  ( 0.8570167067220200163, -0.3177966101694920664, 2.508190348879349774 ) ) ;
#12505=ORIENTED_EDGE ( 'NONE', *, *, #2983, .T. ) ;
#12507=CARTESIAN_POINT ( 'NONE',  ( -0.8934014991059870958, -4.614566048306490309, 6.877287176483410924 ) ) ;
#12508=VERTEX_POINT ( 'NONE', #5517 ) ;
#12514=CARTESIAN_POINT ( 'NONE',  ( 1.494593880360790550, -5.038983050847454237, 3.295456077495951153 ) ) ;
#12520=CARTESIAN_POINT ( 'NONE',  ( 1.794646911016580137, -1.167899381639829981, 6.222494056560660347 ) ) ;
#12521=CARTESIAN_POINT ( 'NONE',  ( 2.270487904532159984, -0.06228813559322070315, 4.080813552109670894 ) ) ;
#12523=CARTESIAN_POINT ( 'NONE',  ( 2.270487904532159984, -0.3622881355932209835, 4.080813552109670894 ) ) ;
#12524=CARTESIAN_POINT ( 'NONE',  ( 1.707817112497189926, -0.4112288135593229477, 6.319218296629480314 ) ) ;
#12526=CARTESIAN_POINT ( 'NONE',  ( 0.9222751404130974384, -0.02224576271186471527, 2.865854510788131027 ) ) ;
#12530=CARTESIAN_POINT ( 'NONE',  ( 2.349464193210359930, -2.243001519261069721, 4.563019372514570016 ) ) ;
#12532=CARTESIAN_POINT ( 'NONE',  ( 2.625437065641401446, -5.381991525423726053, 5.087214675345139270 ) ) ;
#12536=CARTESIAN_POINT ( 'NONE',  ( -1.981271652668300298, -1.633665147405599871, 5.970160748022450115 ) ) ;
#12537=CARTESIAN_POINT ( 'NONE',  ( -2.351212046067109984, -4.618406924666470736, 4.597298481426070893 ) ) ;
#12538=EDGE_CURVE ( 'NONE', #14665, #12508, #8127, .T. ) ;
#12545=CARTESIAN_POINT ( 'NONE',  ( 0.9742769543504904428, -1.261052534792989288, 6.507120986223561054 ) ) ;
#12546=ADVANCED_FACE ( 'NONE', ( #5970 ), #13102, .T. ) ;
#12551=CARTESIAN_POINT ( 'NONE',  ( 1.246151616534670215, -0.3311440677966111523, 3.068501529594759081 ) ) ;
#12552=CARTESIAN_POINT ( 'NONE',  ( 1.351547610267151533, -4.082776294035843634, 6.983951126925231456 ) ) ;
#12553=CARTESIAN_POINT ( 'NONE',  ( -1.074005996636800075, -5.164643153926310681, 2.934052701886380010 ) ) ;
#12554=CARTESIAN_POINT ( 'NONE',  ( 0.9707742057416334225, -5.126483050847465250, 6.508944043303927174 ) ) ;
#12556=CARTESIAN_POINT ( 'NONE',  ( 2.203023580853991081, -0.05783898305084791275, 3.872235369154280349 ) ) ;
#12560=CARTESIAN_POINT ( 'NONE',  ( -0.07299321914061848715, -5.598516949152539723, 2.350000000000000089 ) ) ;
#12561=CARTESIAN_POINT ( 'NONE',  ( 2.239137794397009884, -0.6128213390808879835, 3.975425900939169921 ) ) ;
#12564=CARTESIAN_POINT ( 'NONE',  ( 1.953802435660499048, -0.6128213390808875394, 4.069478085300975323 ) ) ;
#12567=CARTESIAN_POINT ( 'NONE',  ( 1.738765645129589865, -5.293166154074419261, 2.961234354870410090 ) ) ;
#12568=CARTESIAN_POINT ( 'NONE',  ( -1.713314936023349944, -0.5610169491525430763, 3.089913064446579760 ) ) ;
#12569=CARTESIAN_POINT ( 'NONE',  ( -2.295719155670160383, -3.287133615874060055, 5.218091927917240191 ) ) ;
#12572=CARTESIAN_POINT ( 'NONE',  ( 2.650076489488250697, -5.077542372881359789, 4.841243018609314497 ) ) ;
#12579=CARTESIAN_POINT ( 'NONE',  ( -0.2620510901103649815, -3.706322805063249959, 2.361180871966390260 ) ) ;
#12582=CARTESIAN_POINT ( 'NONE',  ( 1.338894208872951186, -5.333856471232010676, 3.139702328019969180 ) ) ;
#12585=CARTESIAN_POINT ( 'NONE',  ( 2.100188519621589922, -4.009070552810999999, 3.637948273607370275 ) ) ;
#12587=CARTESIAN_POINT ( 'NONE',  ( -0.03895741673419786388, -3.729611093351542284, 2.647347042895590086 ) ) ;
#12592=( NAMED_UNIT ( * ) PLANE_ANGLE_UNIT ( ) SI_UNIT ( $, .RADIAN. ) );
#12594=ORIENTED_EDGE ( 'NONE', *, *, #653, .T. ) ;
#12598=CARTESIAN_POINT ( 'NONE',  ( -2.022304719220918479, -5.233262711864406391, 4.346496488058700258 ) ) ;
#12600=CARTESIAN_POINT ( 'NONE',  ( -2.642175029090489513, -1.497776294035840561, 4.450952196049505538 ) ) ;
#12609=CARTESIAN_POINT ( 'NONE',  ( -1.588913656382020756, -5.080331814072260421, 3.399901838171254020 ) ) ;
#12610=CARTESIAN_POINT ( 'NONE',  ( -1.019987577504920528, -2.778632149891700376, 6.481720287913836920 ) ) ;
#12611=CARTESIAN_POINT ( 'NONE',  ( -2.043308330018790198, -0.2002118644067800157, 5.867646457774669422 ) ) ;
#12614=ORIENTED_EDGE ( 'NONE', *, *, #6297, .F. ) ;
#12615=CARTESIAN_POINT ( 'NONE',  ( 2.353194804772640314, -0.07563559322033940047, 4.731327187377229571 ) ) ;
#12616=CARTESIAN_POINT ( 'NONE',  ( 0.4985810152601650724, -1.330917399657850053, 7.000035360316460675 ) ) ;
#12621=CARTESIAN_POINT ( 'NONE',  ( -2.337178851518210365, -3.011515032774579659, 4.976298214796807784 ) ) ;
#12622=CARTESIAN_POINT ( 'NONE',  ( -0.8570167067220350043, -5.582203389830509899, 2.508190348879359988 ) ) ;
#12625=CARTESIAN_POINT ( 'NONE',  ( 2.231116159141619981, -0.9117282104686620370, 3.951089877392439664 ) ) ;
#12626=CARTESIAN_POINT ( 'NONE',  ( 1.489797906646480596, -0.4112288135593234473, 6.112509577910826941 ) ) ;
#12628=VERTEX_POINT ( 'NONE', #16061 ) ;
#12632=CARTESIAN_POINT ( 'NONE',  ( 1.572563554680340703, -0.8185750573155082810, 3.380172092915559645 ) ) ;
#12634=CARTESIAN_POINT ( 'NONE',  ( 1.747582379783020778, -0.4156779661016956062, 6.697200745122486865 ) ) ;
#12640=CARTESIAN_POINT ( 'NONE',  ( -1.940327948426050941, -0.2091101694915259990, 5.370677689277675526 ) ) ;
#12642=CARTESIAN_POINT ( 'NONE',  ( 1.558664967382918931, -4.059488005747546424, 6.847947208954417775 ) ) ;
#12643=AXIS2_PLACEMENT_3D ( 'NONE', #10859, #10954, #12341 ) ;
#12645=CARTESIAN_POINT ( 'NONE',  ( -1.695999708020951013, -5.128627060139315574, 2.646274854235481921 ) ) ;
#12646=CARTESIAN_POINT ( 'NONE',  ( -1.351903350398179438, -5.184322033898315141, 6.245004350000422200 ) ) ;
#12650=CARTESIAN_POINT ( 'NONE',  ( 1.851073041990159540, -0.1067796610169499810, 6.153284478378259870 ) ) ;
#12652=CARTESIAN_POINT ( 'NONE',  ( 1.811729841638690219, -5.341949152542369461, 3.197954009834290012 ) ) ;
#12659=CARTESIAN_POINT ( 'NONE',  ( -2.353452300571019506, -1.474488005747550012, 4.697179287168410156 ) ) ;
#12661=CARTESIAN_POINT ( 'NONE',  ( -2.043688444617268729, -1.497776294035840561, 4.504451070148879133 ) ) ;
#12668=CARTESIAN_POINT ( 'NONE',  ( 2.386628511786341722, -0.3533898305084745561, 3.539457309197775459 ) ) ;
#12669=CARTESIAN_POINT ( 'NONE',  ( -2.237394498046660019, -3.263845327585780165, 5.429939413646380331 ) ) ;
#12672=CARTESIAN_POINT ( 'NONE',  ( 2.020286629067969297, -5.108686440677975504, 6.420841923842827370 ) ) ;
#12681=CARTESIAN_POINT ( 'NONE',  ( 0.06913820924143311564, -1.377493976234431372, 7.352985789827153340 ) ) ;
#12683=CARTESIAN_POINT ( 'NONE',  ( 1.097896950867359500, -0.7068739681193977331, 2.280088753565270743 ) ) ;
#12684=CARTESIAN_POINT ( 'NONE',  ( 0.5677251586959709551, -5.311531839079339790, 2.399563163165729929 ) ) ;
#12686=CARTESIAN_POINT ( 'NONE',  ( -1.923406176634930853, -4.796950468210009255, 2.875176962145308934 ) ) ;
#12688=CARTESIAN_POINT ( 'NONE',  ( 1.401708661791409849, -4.358394877135329359, 6.590491606684049763 ) ) ;
#12692=CARTESIAN_POINT ( 'NONE',  ( 1.058024172752470182, -3.869340823081269587, 2.940600473883339561 ) ) ;
#12703=UNCERTAINTY_MEASURE_WITH_UNIT (LENGTH_MEASURE( 1.000000000000000082E-05 ), #9480, 'distance_accuracy_value', 'NONE');
#12706=CARTESIAN_POINT ( 'NONE',  ( -2.052786957354850728, -5.224364406779660186, 4.727327971967373976 ) ) ;
#12707=CARTESIAN_POINT ( 'NONE',  ( -2.549960444629829848, -1.544352870612421880, 3.964598460822165382 ) ) ;
#12714=CARTESIAN_POINT ( 'NONE',  ( 0.5570002967656469961, -2.891232714973159812, 6.986590552960210587 ) ) ;
#12715=CARTESIAN_POINT ( 'NONE',  ( 1.583713126240741564, -2.429307825567371459, 6.006428174987391344 ) ) ;
#12716=CARTESIAN_POINT ( 'NONE',  ( 1.901882987994760965, -0.09343220338983100615, 5.472995608211450147 ) ) ;
#12721=EDGE_CURVE ( 'NONE', #11001, #17501, #3268, .T. ) ;
#12722=CARTESIAN_POINT ( 'NONE',  ( -2.328217775191430139, -0.2180084745762720100, 5.043379051721170292 ) ) ;
#12723=CARTESIAN_POINT ( 'NONE',  ( 2.023259452208809872, -2.425466949207399914, 3.497849062500220096 ) ) ;
#12726=CARTESIAN_POINT ( 'NONE',  ( 2.334032080503399609, -2.289578095837639715, 5.001728246382188381 ) ) ;
#12728=CARTESIAN_POINT ( 'NONE',  ( -0.6493550500446439999, -5.586652542372879005, 2.437955526623099889 ) ) ;
#12732=CARTESIAN_POINT ( 'NONE',  ( -0.6187874668174415671, -0.4646186440677965712, 6.657494107589526422 ) ) ;
#12735=CARTESIAN_POINT ( 'NONE',  ( -1.385380178477320312, -1.982989471729918352, 3.184868453331453075 ) ) ;
#12737=CARTESIAN_POINT ( 'NONE',  ( 1.610878918935058524, -0.3311440677966099311, 2.590989782159081933 ) ) ;
#12742=CARTESIAN_POINT ( 'NONE',  ( -0.6187874668174415671, -0.4646186440677965712, 6.657494107589526422 ) ) ;
#12745=CARTESIAN_POINT ( 'NONE',  ( -1.209303714320900003, -4.865515740159329638, 2.662663894020049771 ) ) ;
#12746=CARTESIAN_POINT ( 'NONE',  ( -0.1365430262726299304, -5.453177966101685037, 6.748423079423377047 ) ) ;
#12753=CARTESIAN_POINT ( 'NONE',  ( 2.033393610350129777, -0.8224159336754830463, 5.884928737465320303 ) ) ;
#12756=CARTESIAN_POINT ( 'NONE',  ( -1.333132471082830506, -2.825208726468270370, 6.261300629978947541 ) ) ;
#12762=CARTESIAN_POINT ( 'NONE',  ( 2.653602652190420574, -0.07563559322033948373, 4.735326402787084277 ) ) ;
#12763=CARTESIAN_POINT ( 'NONE',  ( -1.465095039565370127, -3.566593075333519991, 2.858195935359880480 ) ) ;
#12766=CARTESIAN_POINT ( 'NONE',  ( -1.407651048079459288, -5.573305084745765470, 2.450250343405070641 ) ) ;
#12772=CARTESIAN_POINT ( 'NONE',  ( 2.626509418457480649, -1.028169651910100679, 5.080213055741780614 ) ) ;
#12777=CARTESIAN_POINT ( 'NONE',  ( -2.510208264418979596, -4.525253771513313872, 5.561375738133230939 ) ) ;
#12781=CARTESIAN_POINT ( 'NONE',  ( 1.214457691475989920, -3.869340823081270031, 2.684103622926340194 ) ) ;
#12784=CARTESIAN_POINT ( 'NONE',  ( 0.3429245540020083860, -3.776187669928120272, 2.675820019639898906 ) ) ;
#12794=CARTESIAN_POINT ( 'NONE',  ( 1.782460458101500889, -5.099788135593215976, 5.718585207845976015 ) ) ;
#12798=CARTESIAN_POINT ( 'NONE',  ( -0.009452110982656879157, -5.299807955295460005, 2.350000000000000089 ) ) ;
#12802=CARTESIAN_POINT ( 'NONE',  ( -2.295719155670160383, -3.287133615874060055, 5.218091927917240191 ) ) ;
#12803=CARTESIAN_POINT ( 'NONE',  ( 1.642659730162729925, -3.663587104846653730, 3.468508687188663675 ) ) ;
#12804=CARTESIAN_POINT ( 'NONE',  ( 1.351903350398191206, -0.1156779661016950206, 6.245004350000406212 ) ) ;
#12809=CARTESIAN_POINT ( 'NONE',  ( -1.713314936023349944, -0.2610169491525429764, 3.089913064446579760 ) ) ;
#12810=CARTESIAN_POINT ( 'NONE',  ( -1.417709711196470046, -2.006277760018209566, 2.821478011237799954 ) ) ;
#12814=CARTESIAN_POINT ( 'NONE',  ( -1.265407828724339767, -3.290974492234039595, 2.715689360385571405 ) ) ;
#12816=CARTESIAN_POINT ( 'NONE',  ( -2.653602652190420574, -5.524364406779660897, 4.735326402787099376 ) ) ;
#12818=CARTESIAN_POINT ( 'NONE',  ( 2.011500846714319835, -0.3489406779661020086, 3.478373409938460448 ) ) ;
#12823=CARTESIAN_POINT ( 'NONE',  ( 1.764143222953819867, -2.425466949207401690, 3.649904513135025841 ) ) ;
#12824=CARTESIAN_POINT ( 'NONE',  ( 1.554165089654128584, -0.4201271186440683758, 6.851145244874527584 ) ) ;
#12829=CARTESIAN_POINT ( 'NONE',  ( 0.002826310976700510246, -0.4052053642593020366, 2.204978094066170069 ) ) ;
#12830=CARTESIAN_POINT ( 'NONE',  ( -1.351903350398179438, -5.484322033898315851, 6.245004350000422200 ) ) ;
#12831=CARTESIAN_POINT ( 'NONE',  ( 2.318251751302029984, -0.06673728813559361150, 4.294764266798991592 ) ) ;
#12832=CARTESIAN_POINT ( 'NONE',  ( -0.1565249325564300187, -5.453177966101690366, 7.048192310558509810 ) ) ;
#12833=CARTESIAN_POINT ( 'NONE',  ( -1.221947981261169991, -0.5741044150835520332, 2.670403636935529956 ) ) ;
#12837=CARTESIAN_POINT ( 'NONE',  ( 0.04278372834676710118, -1.870388906648450034, 2.346934926511239805 ) ) ;
#12839=CARTESIAN_POINT ( 'NONE',  ( -0.4874850653659789645, -2.708767285026830951, 6.694306935672950765 ) ) ;
#12844=CARTESIAN_POINT ( 'NONE',  ( -2.630358833876468960, -0.5313559322033900578, 4.347767980622416317 ) ) ;
#12845=CARTESIAN_POINT ( 'NONE',  ( 0.5570002967656469961, -2.891232714973159812, 6.986590552960210587 ) ) ;
#12848=CARTESIAN_POINT ( 'NONE',  ( 0.7998959936908462964, -5.135381355932194580, 7.230419212249866945 ) ) ;
#12853=CARTESIAN_POINT ( 'NONE',  ( 0.000000000000000000, 0.000000000000000000, 0.000000000000000000 ) ) ;
#12857=CARTESIAN_POINT ( 'NONE',  ( -1.914021115237000137, -4.754295778036220277, 6.069404563272239983 ) ) ;
#12861=CARTESIAN_POINT ( 'NONE',  ( -2.347833536521260367, -3.058091609351150097, 4.537447324629909851 ) ) ;
#12863=CARTESIAN_POINT ( 'NONE',  ( -0.4790341583531910197, -3.683034516774959855, 2.395814251711740006 ) ) ;
#12865=CARTESIAN_POINT ( 'NONE',  ( -0.08304008649493913041, -2.961097579838030569, 6.751342532748503267 ) ) ;
#12877=CARTESIAN_POINT ( 'NONE',  ( 1.695509042132770761, -5.346398305084745672, 3.542446458728613301 ) ) ;
#12879=CARTESIAN_POINT ( 'NONE',  ( 2.435897774776379698, -2.359442960702510472, 5.753335522918191280 ) ) ;
#12882=CARTESIAN_POINT ( 'NONE',  ( -0.5027094486773525661, -4.952022267818764867, 2.083735201298030137 ) ) ;
#12885=CARTESIAN_POINT ( 'NONE',  ( -1.507201387235980183, -3.124115597856050197, 6.507509243627219497 ) ) ;
#12886=CARTESIAN_POINT ( 'NONE',  ( 1.079900583135640302, -3.570433951693503527, 2.953942563037689428 ) ) ;
#12888=CARTESIAN_POINT ( 'NONE',  ( -0.2812789908084309953, -0.1557203389830509876, 7.036533610117280624 ) ) ;
#12890=CARTESIAN_POINT ( 'NONE',  ( -1.695509042132779864, -0.5536016949152540167, 3.542446458728619518 ) ) ;
#12893=CARTESIAN_POINT ( 'NONE',  ( 2.180207327701309872, -0.09343220338983100615, 5.586116916730190063 ) ) ;
#12894=CARTESIAN_POINT ( 'NONE',  ( 2.169623098572349917, -2.658349832090280529, 5.611855963200990338 ) ) ;
#12899=CARTESIAN_POINT ( 'NONE',  ( 2.308170020371300257, -3.873181699441239800, 5.159452766389608591 ) ) ;
#12901=CARTESIAN_POINT ( 'NONE',  ( 2.020286629067969297, -5.108686440677975504, 6.420841923842827370 ) ) ;
#12905=CARTESIAN_POINT ( 'NONE',  ( 2.203023580853990193, -0.3578389830508479919, 3.872235369154280349 ) ) ;
#12908=CARTESIAN_POINT ( 'NONE',  ( 0.7616804549307097938, -2.262448931189378509, 2.793499350326721142 ) ) ;
#12912=CARTESIAN_POINT ( 'NONE',  ( 1.614765845140360589, -0.4067796610169500116, 5.967758800287426446 ) ) ;
#12916=CARTESIAN_POINT ( 'NONE',  ( 2.224278379903029901, -5.390889830508481140, 5.468825643806100700 ) ) ;
#12919=CARTESIAN_POINT ( 'NONE',  ( -2.224278379903029457, -0.2091101694915259712, 5.468825643806110470 ) ) ;
#12924=CARTESIAN_POINT ( 'NONE',  ( -1.401708661791369881, -1.241605122864670063, 6.590491606684079962 ) ) ;
#12927=CIRCLE ( 'NONE', #503, 0.1499999999999999944 ) ;
#12928=CARTESIAN_POINT ( 'NONE',  ( 0.4625564304288019568, -2.592325843585391532, 6.700235833919842676 ) ) ;
#12933=CARTESIAN_POINT ( 'NONE',  ( -2.586172839791708533, -0.5358050847457624943, 4.104546363490954697 ) ) ;
#12934=CARTESIAN_POINT ( 'NONE',  ( 1.401708661791409849, -4.358394877135329359, 6.590491606684049763 ) ) ;
#12937=CARTESIAN_POINT ( 'NONE',  ( 0.07064654565475687875, -5.148728813559319661, 7.352897294663512717 ) ) ;
#12943=CARTESIAN_POINT ( 'NONE',  ( 1.632373740989790045, -0.7935201267648649415, 3.049747554812159755 ) ) ;
#12946=CARTESIAN_POINT ( 'NONE',  ( -2.091881088960070745, -1.610376859117309767, 6.333140288723886790 ) ) ;
#12950=CARTESIAN_POINT ( 'NONE',  ( 2.062913653388430024, -2.382731248990799688, 5.832754583370790336 ) ) ;
#12951=CARTESIAN_POINT ( 'NONE',  ( 1.661700935788380074, -5.037500000000000533, 3.038299064211610112 ) ) ;
#12953=CARTESIAN_POINT ( 'NONE',  ( -1.752195476665039831, -1.563800282540731779, 6.693219682964347328 ) ) ;
#12954=DIRECTION ( 'NONE',  ( 0.000000000000000000, -1.000000000000000000, 0.000000000000000000 ) ) ;
#12955=CARTESIAN_POINT ( 'NONE',  ( -1.861802609626409089, -4.800872354612795156, 5.565212624397245733 ) ) ;
#12956=CARTESIAN_POINT ( 'NONE',  ( -2.143090896833110381, -0.5046610169491529962, 5.672454929438350391 ) ) ;
#12968=CARTESIAN_POINT ( 'NONE',  ( 1.134881315981519645, -5.422033898305085309, 6.410767520434657918 ) ) ;
#12969=CARTESIAN_POINT ( 'NONE',  ( -1.901407128523849632, -2.848497014756559143, 6.551422324754827109 ) ) ;
#12977=CARTESIAN_POINT ( 'NONE',  ( -2.351999299633229956, -3.333710192450639820, 4.782734406438290620 ) ) ;
#12978=CARTESIAN_POINT ( 'NONE',  ( 1.790316459643169100, -0.8651516338920848259, 3.695177221627173214 ) ) ;
#12980=CARTESIAN_POINT ( 'NONE',  ( -1.811729841638700211, -0.2580508474576269640, 3.197954009834299782 ) ) ;
#12985=CARTESIAN_POINT ( 'NONE',  ( 0.9490039995898825742, -3.523857375116919322, 2.221592224478729172 ) ) ;
#12986=CARTESIAN_POINT ( 'NONE',  ( -1.782460458101500889, -0.2002118644067801267, 5.718585207845990226 ) ) ;
#12987=CARTESIAN_POINT ( 'NONE',  ( 1.353103843060669886, -2.798079561820010053, 6.625579309552930063 ) ) ;
#12991=CARTESIAN_POINT ( 'NONE',  ( -1.902324933209428970, -3.197821339080880509, 3.314393441133570484 ) ) ;
#12993=CARTESIAN_POINT ( 'NONE',  ( -2.560337424259679917, -5.237711864406785267, 4.001768473655595848 ) ) ;
#12996=CARTESIAN_POINT ( 'NONE',  ( -0.06264882350515391107, -0.4512711864406790396, 7.052569299041220319 ) ) ;
#13001=CARTESIAN_POINT ( 'NONE',  ( -1.798783563193318891, -3.217268751009201289, 5.689585537188996511 ) ) ;
#13010=CARTESIAN_POINT ( 'NONE',  ( -0.002227590684724169937, -0.4853054260922249896, 2.202374039106750114 ) ) ;
#13011=CARTESIAN_POINT ( 'NONE',  ( 2.350067830300900162, -5.377542372881360500, 4.825253242917690422 ) ) ;
#13012=CARTESIAN_POINT ( 'NONE',  ( 0.5889081234606849957, -0.1379237288135600759, 6.978529000034869867 ) ) ;
#13014=CARTESIAN_POINT ( 'NONE',  ( -1.449852972480019764, -3.589881363621813648, 2.477154964647171109 ) ) ;
#13017=CARTESIAN_POINT ( 'NONE',  ( 2.283153923255319739, -2.196424942684489512, 4.129076318403449797 ) ) ;
#13019=CARTESIAN_POINT ( 'NONE',  ( 1.279347147864559275, -2.033406924666469884, 3.094331068408280760 ) ) ;
#13025=CARTESIAN_POINT ( 'NONE',  ( -2.239137794397029868, -4.987178660919110662, 3.975425900939220103 ) ) ;
#13028=CARTESIAN_POINT ( 'NONE',  ( -0.7322514394120432923, -5.286652542372874741, 2.149183891723918993 ) ) ;
#13037=CARTESIAN_POINT ( 'NONE',  ( -2.135041058613629694, -4.800872354612799597, 5.690123914223820023 ) ) ;
#13038=CARTESIAN_POINT ( 'NONE',  ( 0.009452110982655428928, -0.3001920447045380858, 2.649999999999998579 ) ) ;
#13040=CARTESIAN_POINT ( 'NONE',  ( -1.167621112247339887, -2.778632149891699932, 6.743381174846780013 ) ) ;
#13041=CARTESIAN_POINT ( 'NONE',  ( 0.5677251586959709551, -5.311531839079339790, 2.399563163165729929 ) ) ;
#13043=CARTESIAN_POINT ( 'NONE',  ( 2.510208264419000468, -1.074746228486680000, 5.561375738133185642 ) ) ;
#13046=CARTESIAN_POINT ( 'NONE',  ( 1.065036425888030713, -4.381683165423609694, 6.455163597548602361 ) ) ;
#13047=CARTESIAN_POINT ( 'NONE',  ( -1.925796468768790071, -0.4957627118644070130, 6.052706598917719560 ) ) ;
#13055=ORIENTED_EDGE ( 'NONE', *, *, #13786, .F. ) ;
#13056=CARTESIAN_POINT ( 'NONE',  ( 1.580445181003960586, -5.341949152542365908, 3.389704561770334301 ) ) ;
#13059=CARTESIAN_POINT ( 'NONE',  ( 0.8400312909773258729, -2.569037555297099651, 7.217431453521787610 ) ) ;
#13061=CARTESIAN_POINT ( 'NONE',  ( 1.740526006427820072, -0.5337085751346559714, 2.973047620154039894 ) ) ;
#13063=CARTESIAN_POINT ( 'NONE',  ( 2.145694642186089851, -1.098034516774969882, 5.666819626392539888 ) ) ;
#13065=CARTESIAN_POINT ( 'NONE',  ( -1.777964140657649850, -4.731007489747940831, 6.241943319976260618 ) ) ;
#13066=CARTESIAN_POINT ( 'NONE',  ( -0.6217226704572171858, -4.292370888630430592, 6.656620240022991908 ) ) ;
#13067=CARTESIAN_POINT ( 'NONE',  ( 0.3265524029357661506, -0.1423728813559330397, 6.726831181542982208 ) ) ;
#13072=CARTESIAN_POINT ( 'NONE',  ( 2.121170185508189476, -3.663587104846653730, 3.105085978143951486 ) ) ;
#13073=CARTESIAN_POINT ( 'NONE',  ( 1.754713504580569960, -0.04894067796610205440, 3.634325740584615883 ) ) ;
#13074=CARTESIAN_POINT ( 'NONE',  ( 2.347833536521260367, -2.541908390648839777, 4.537447324629859224 ) ) ;
#13078=CARTESIAN_POINT ( 'NONE',  ( -1.611907055891630414, -3.244397915657460274, 2.985210995296890601 ) ) ;
#13080=CARTESIAN_POINT ( 'NONE',  ( 1.467041701146838406, -5.122033898305085486, 6.911479965439912831 ) ) ;
#13086=CARTESIAN_POINT ( 'NONE',  ( -1.641808337277740115, -0.4868644067796619734, 6.386111670537629514 ) ) ;
#13090=CARTESIAN_POINT ( 'NONE',  ( -2.049636678546640667, -3.356998480738929924, 4.582138519505405405 ) ) ;
#13091=CARTESIAN_POINT ( 'NONE',  ( 0.08231150243515643339, -0.001483050847457899508, 2.050000000000001155 ) ) ;
#13094=CARTESIAN_POINT ( 'NONE',  ( 0.3265524029357661506, -0.4423728813559331119, 6.726831181542982208 ) ) ;
#13098=CARTESIAN_POINT ( 'NONE',  ( 2.143090896833110381, -5.395338983050850246, 5.672454929438339732 ) ) ;
#13102=PLANE ( 'NONE',  #3555 ) ;
#13105=CARTESIAN_POINT ( 'NONE',  ( -0.04661003995944364847, -3.729611093351542284, 2.046522810126899294 ) ) ;
#13108=CARTESIAN_POINT ( 'NONE',  ( -1.353103843060629918, -2.801920438179979822, 6.625579309552960261 ) ) ;
#13113=CARTESIAN_POINT ( 'NONE',  ( -1.019987577504920528, -2.778632149891700376, 6.481720287913836920 ) ) ;
#13118=CARTESIAN_POINT ( 'NONE',  ( -2.608006145151089861, -1.427911429170979352, 5.191342690854409803 ) ) ;
#13119=CARTESIAN_POINT ( 'NONE',  ( -0.8244235255442939891, -0.5829339996946389935, 2.492493020344019872 ) ) ;
#13122=CARTESIAN_POINT ( 'NONE',  ( 2.350067830300900162, -5.077542372881360677, 4.825253242917690422 ) ) ;
#13130=CARTESIAN_POINT ( 'NONE',  ( 2.594645788401200637, -2.611773255513701653, 5.257608218854235460 ) ) ;
#13131=CARTESIAN_POINT ( 'NONE',  ( 0.2151249875495270247, -0.3251990024832489556, 2.650810719223910983 ) ) ;
#13133=CARTESIAN_POINT ( 'NONE',  ( -1.866416942370660026, -1.637506023765569863, 3.266391446483499994 ) ) ;
#13135=CARTESIAN_POINT ( 'NONE',  ( 2.418933091173299577, -1.098034516774970770, 5.791730916219126613 ) ) ;
#13137=CARTESIAN_POINT ( 'NONE',  ( 0.8967027089123184025, -4.404971453711897134, 6.546842195331636916 ) ) ;
#13138=CARTESIAN_POINT ( 'NONE',  ( 2.353194804772640314, -0.3756355932203400139, 4.731327187377229571 ) ) ;
#13147=CARTESIAN_POINT ( 'NONE',  ( 2.322440385110930094, -2.518620102360550117, 4.319189883157390497 ) ) ;
#13151=CARTESIAN_POINT ( 'NONE',  ( -0.8001898266890440370, -1.470647129387580021, 6.913242401714570384 ) ) ;
#13152=CARTESIAN_POINT ( 'NONE',  ( -1.688800633088611836, -4.758136654396205145, 3.532586505616431616 ) ) ;
#13156=CARTESIAN_POINT ( 'NONE',  ( 0.5137283630188955730, -0.1379237288135599648, 6.687652957477222770 ) ) ;
#13157=CARTESIAN_POINT ( 'NONE',  ( 0.8242394280877100021, -4.428259742000189902, 6.904399023015010073 ) ) ;
#13162=CARTESIAN_POINT ( 'NONE',  ( -2.126557263589649249, -3.151244762504310071, 3.691783806836060222 ) ) ;
#13164=CARTESIAN_POINT ( 'NONE',  ( 1.666450993087180477, -5.117584745762705722, 6.765380371283858274 ) ) ;
#13167=CARTESIAN_POINT ( 'NONE',  ( -2.332582362116870200, -0.5313559322033900578, 4.387643303570819775 ) ) ;
#13171=CARTESIAN_POINT ( 'NONE',  ( -1.549925137359298599, -4.731007489747939054, 6.046340934239856857 ) ) ;
#13172=CARTESIAN_POINT ( 'NONE',  ( 0.4221287159901364605, -0.4423728813559331119, 7.320050063945812369 ) ) ;
#13175=VERTEX_POINT ( 'NONE', #16563 ) ;
#13176=CARTESIAN_POINT ( 'NONE',  ( -0.004607033757061119485, -0.5230175839438470087, 2.216967106706559498 ) ) ;
#13177=CARTESIAN_POINT ( 'NONE',  ( -0.8570167067220350043, -5.582203389830509899, 2.508190348879359988 ) ) ;
#13180=CARTESIAN_POINT ( 'NONE',  ( -2.043308330018789309, -0.2002118644067800435, 5.867646457774671198 ) ) ;
#13182=CARTESIAN_POINT ( 'NONE',  ( -2.161103922260861232, -3.496728210468663889, 3.159628768708461877 ) ) ;
#13184=CARTESIAN_POINT ( 'NONE',  ( -2.023259452208839626, -3.174533050792599731, 3.497849062500260064 ) ) ;
#13187=CARTESIAN_POINT ( 'NONE',  ( -0.01333550863832440661, -3.430704221963769562, 2.647020699851690306 ) ) ;
#13191=CARTESIAN_POINT ( 'NONE',  ( 1.117157304995380240, -0.9388573751169233539, 6.422457952614097465 ) ) ;
#13197=CARTESIAN_POINT ( 'NONE',  ( -0.1869574461324000070, -0.5962015548080630278, 2.350675676344399889 ) ) ;
#13201=CARTESIAN_POINT ( 'NONE',  ( 0.7093417302541469294, -5.135381355932199909, 6.943956659919690466 ) ) ;
#13211=CARTESIAN_POINT ( 'NONE',  ( 1.524497189778211581, -2.798079561820010941, 6.872331008700157007 ) ) ;
#13212=CARTESIAN_POINT ( 'NONE',  ( 1.159526867004269768, -0.4480353997208165184, 2.996084454861921209 ) ) ;
#13214=CARTESIAN_POINT ( 'NONE',  ( -0.8189529353761560992, -1.777235753495300052, 2.493631540942749858 ) ) ;
#13215=CARTESIAN_POINT ( 'NONE',  ( 0.8611469534735395337, -5.020626044399135068, 2.833474624362548600 ) ) ;
#13217=CARTESIAN_POINT ( 'NONE',  ( -2.218077401483159683, -4.824160642901089702, 5.486688202856539576 ) ) ;
#13219=CARTESIAN_POINT ( 'NONE',  ( 2.351212046067109984, -0.9815930753335269099, 4.597298481426010497 ) ) ;
#13222=CARTESIAN_POINT ( 'NONE',  ( -2.224278379903029901, -0.5091101694915259879, 5.468825643806110470 ) ) ;
#13235=B_SPLINE_CURVE_WITH_KNOTS ( 'NONE', 3,
 ( #9723, #6764, #1026, #2329, #13625, #13892, #5186 ),
 .UNSPECIFIED., .F., .F.,
 ( 4, 1, 1, 1, 4 ),
 ( 18.06415775814129887, 18.36448856483159986, 18.49670707487869947, 18.62179267666130045, 18.84955592153880133 ),
 .UNSPECIFIED. ) ;
#13236=CARTESIAN_POINT ( 'NONE',  ( 1.687170344132030042, -2.751502985243429844, 6.340793075730549511 ) ) ;
#13241=CARTESIAN_POINT ( 'NONE',  ( 1.571912189623089873, -4.335106588847041031, 6.451524409078630562 ) ) ;
#13243=CARTESIAN_POINT ( 'NONE',  ( -1.440522616026439495, -4.804713230972779137, 3.241384813161591438 ) ) ;
#13244=EDGE_CURVE ( 'NONE', #2833, #12628, #12052, .T. ) ;
#13250=CARTESIAN_POINT ( 'NONE',  ( -0.05465110135555984600, -0.1512711864406780515, 6.752241303418941243 ) ) ;
#13251=CARTESIAN_POINT ( 'NONE',  ( -1.332058588847369940, -3.100827309567760537, 6.640197310420220767 ) ) ;
#13258=CARTESIAN_POINT ( 'NONE',  ( -2.484260633728970546, -5.242161016949150820, 3.766563288620799366 ) ) ;
#13261=CARTESIAN_POINT ( 'NONE',  ( 1.707817112497189926, -0.4112288135593229477, 6.319218296629480314 ) ) ;
#13265=CARTESIAN_POINT ( 'NONE',  ( 2.044452488559148851, -4.148800282540726414, 4.887392274793745273 ) ) ;
#13266=CARTESIAN_POINT ( 'NONE',  ( 0.7322514394120266390, -0.01334745762711889508, 2.149183891723918993 ) ) ;
#13269=CARTESIAN_POINT ( 'NONE',  ( 0.6493550500446280127, -0.3133474576271190193, 2.437955526623099889 ) ) ;
#13272=CARTESIAN_POINT ( 'NONE',  ( 1.554165089654128584, -0.4201271186440683758, 6.851145244874527584 ) ) ;
#13277=DIRECTION ( 'NONE',  ( 1.000000000000000000, 1.741945227011179869E-17, 2.220446049250309876E-16 ) ) ;
#13278=CARTESIAN_POINT ( 'NONE',  ( 0.4469859058769135030, -3.776187669928120272, 2.084026511420788985 ) ) ;
#13281=CARTESIAN_POINT ( 'NONE',  ( 1.948278411993589865, -2.406019537279080467, 6.020210936496000365 ) ) ;
#13284=CARTESIAN_POINT ( 'NONE',  ( 0.8735826871841618768, -4.106064582324130185, 6.557889967484662463 ) ) ;
#13286=CARTESIAN_POINT ( 'NONE',  ( 1.555285212483259683, -2.079983501243050981, 3.359854578615069087 ) ) ;
#13288=CARTESIAN_POINT ( 'NONE',  ( 1.307725206348619995, -0.7471169921413569615, 2.732408283416570161 ) ) ;
#13295=CARTESIAN_POINT ( 'NONE',  ( 1.300961508564179914, -5.122033898305089927, 6.661123742937279602 ) ) ;
#13300=CARTESIAN_POINT ( 'NONE',  ( 1.652654650382400003, -0.7952867690272209522, 3.029252778805629820 ) ) ;
#13303=CARTESIAN_POINT ( 'NONE',  ( -0.4722227023514615762, -2.122719201459649874, 2.088464165977090836 ) ) ;
#13307=EDGE_CURVE ( 'NONE', #17501, #15103, #16220, .T. ) ;
#13309=CARTESIAN_POINT ( 'NONE',  ( -2.126557263589650137, -3.151244762504310071, 3.691783806836059778 ) ) ;
#13310=CARTESIAN_POINT ( 'NONE',  ( 0.1969988207263408952, -5.304612347394259686, 2.648915996644538584 ) ) ;
#13311=CARTESIAN_POINT ( 'NONE',  ( 2.516451517878131927, -0.9117282104686613708, 3.857037693030633818 ) ) ;
#13314=CARTESIAN_POINT ( 'NONE',  ( 1.851400890972779045, -5.413135593220339992, 6.601359968904126241 ) ) ;
#13316=CARTESIAN_POINT ( 'NONE',  ( 1.661700935788380074, -5.337500000000000355, 3.038299064211610112 ) ) ;
#13317=ORIENTED_EDGE ( 'NONE', *, *, #1873, .T. ) ;
#13325=CARTESIAN_POINT ( 'NONE',  ( 2.023259452208809872, -2.425466949207399914, 3.497849062500220096 ) ) ;
#13332=CARTESIAN_POINT ( 'NONE',  ( -1.197297565406129971, -1.517223705964160008, 6.726135293448209929 ) ) ;
#13334=CARTESIAN_POINT ( 'NONE',  ( -0.4790341583531910197, -3.683034516774959855, 2.395814251711740006 ) ) ;
#13335=CARTESIAN_POINT ( 'NONE',  ( -1.996236309555629251, -4.548542059801595094, 5.179523137126564869 ) ) ;
#13337=CARTESIAN_POINT ( 'NONE',  ( -1.494593880360799432, -0.5610169491525425212, 3.295456077495951153 ) ) ;
#13341=CARTESIAN_POINT ( 'NONE',  ( 1.821706171509118954, -0.09788135593220394226, 5.646608543709396244 ) ) ;
#13342=CARTESIAN_POINT ( 'NONE',  ( -2.036228139452650243, -3.473439922180369788, 3.519948877554409883 ) ) ;
#13349=CARTESIAN_POINT ( 'NONE',  ( -1.407651048079459288, -5.273305084745764759, 2.450250343405070641 ) ) ;
#13352=CARTESIAN_POINT ( 'NONE',  ( -1.791574935211209807, -0.4913135593220339659, 6.226029630577610163 ) ) ;
#13355=CARTESIAN_POINT ( 'NONE',  ( 0.5381211601353905749, -4.451548030288480895, 6.681243917250638376 ) ) ;
#13356=CARTESIAN_POINT ( 'NONE',  ( 0.9002849211310119948, -0.4334745762711874617, 7.196465912290821443 ) ) ;
#13358=CARTESIAN_POINT ( 'NONE',  ( -1.679950111053631900, -0.4957627118644069575, 5.880020650119711867 ) ) ;
#13360=CARTESIAN_POINT ( 'NONE',  ( -2.651721837666119796, -0.5269067796610176213, 4.594045830208265180 ) ) ;
#13364=CARTESIAN_POINT ( 'NONE',  ( 0.8934014991060327260, -0.9854339516935011201, 6.877287176483389608 ) ) ;
#13365=CARTESIAN_POINT ( 'NONE',  ( -1.303682947472720954, -0.2673043920988010802, 3.104350467804975366 ) ) ;
#13366=CARTESIAN_POINT ( 'NONE',  ( -1.650842931266140790, -3.566593075333521767, 2.622060802311461547 ) ) ;
#13369=CARTESIAN_POINT ( 'NONE',  ( 0.7435598031058590074, -2.569037555297100095, 6.932904947974519949 ) ) ;
#13372=CARTESIAN_POINT ( 'NONE',  ( -1.102492180652080211, -3.290974492234041815, 2.968118700883599193 ) ) ;
#13375=CARTESIAN_POINT ( 'NONE',  ( -1.508881462028629716, -1.288181699441250050, 6.092184821126286565 ) ) ;
#13379=CARTESIAN_POINT ( 'NONE',  ( -0.9279264017968105183, -1.171740257999810852, 7.186376135231811624 ) ) ;
#13385=CARTESIAN_POINT ( 'NONE',  ( -0.07299321914061848715, -5.298516949152539901, 2.350000000000000089 ) ) ;
#13387=( BOUNDED_SURFACE ( )  B_SPLINE_SURFACE ( 3, 3, ( 
 ( #11644, #11741, #13041, #9035, #3227, #17270, #10349 ),
 ( #8959, #15742, #7486, #11558, #15916, #6087, #17462 ),
 ( #7665, #1755, #2008, #3316, #446, #8690, #1655 ),
 ( #17542, #626, #17374, #4696, #16015, #14604, #12951 ),
 ( #1919, #7304, #7569, #13215, #4782, #10432, #16094 ),
 ( #3390, #13310, #6264, #14692, #4871, #277, #4512 ),
 ( #10163, #15823, #3126, #10518, #9226, #9519, #6452 ) ),
 .UNSPECIFIED., .T., .F., .F. ) 
 B_SPLINE_SURFACE_WITH_KNOTS ( ( 4, 3, 4 ),
 ( 4, 1, 1, 1, 4 ),
 ( 0.000000000000000000, 3.141592653589790007, 6.283185307179590673 ),
 ( 0.000000000000000000, 0.3003308066894049833, 0.4325493167363730351, 0.5576349185191149527, 0.7853981633974479459 ),
 .UNSPECIFIED. ) 
 GEOMETRIC_REPRESENTATION_ITEM ( )  RATIONAL_B_SPLINE_SURFACE ( (
 ( 1.000000000000000000, 1.000000000000000000, 1.000000000000000000, 1.000000000000000000, 1.000000000000000000, 1.000000000000000000, 1.000000000000000000),
 ( 0.3333333333333329818, 0.3333333333333329818, 0.3333333333333329818, 0.3333333333333329818, 0.3333333333333329818, 0.3333333333333329818, 0.3333333333333329818),
 ( 0.3333333333333329818, 0.3333333333333329818, 0.3333333333333329818, 0.3333333333333329818, 0.3333333333333329818, 0.3333333333333329818, 0.3333333333333329818),
 ( 1.000000000000000000, 1.000000000000000000, 1.000000000000000000, 1.000000000000000000, 1.000000000000000000, 1.000000000000000000, 1.000000000000000000),
 ( 0.3333333333333329818, 0.3333333333333329818, 0.3333333333333329818, 0.3333333333333329818, 0.3333333333333329818, 0.3333333333333329818, 0.3333333333333329818),
 ( 0.3333333333333329818, 0.3333333333333329818, 0.3333333333333329818, 0.3333333333333329818, 0.3333333333333329818, 0.3333333333333329818, 0.3333333333333329818),
 ( 1.000000000000000000, 1.000000000000000000, 1.000000000000000000, 1.000000000000000000, 1.000000000000000000, 1.000000000000000000, 1.000000000000000000) ) ) 
 REPRESENTATION_ITEM ( '' )  SURFACE ( )  );
#13393=CARTESIAN_POINT ( 'NONE',  ( -1.901882987994748975, -5.506567796610171150, 5.472995608211450147 ) ) ;
#13394=CARTESIAN_POINT ( 'NONE',  ( -2.647661051184980519, -3.058091609351150986, 4.518328177639144627 ) ) ;
#13396=CARTESIAN_POINT ( 'NONE',  ( 2.146130664537611032, -2.402178660919109365, 3.138834773724044958 ) ) ;
#13399=CARTESIAN_POINT ( 'NONE',  ( 1.197297565406180153, -4.082776294035840969, 6.726135293448179731 ) ) ;
#13402=CARTESIAN_POINT ( 'NONE',  ( 1.630703155447489561, -2.332313796054251487, 2.606218513833050920 ) ) ;
#13406=CARTESIAN_POINT ( 'NONE',  ( 1.661700935665417544, -5.037501140877957084, 3.038299064334577082 ) ) ;
#13408=CARTESIAN_POINT ( 'NONE',  ( -0.4201920264140019956, -2.122719201459649874, 2.384360920086639801 ) ) ;
#13410=CARTESIAN_POINT ( 'NONE',  ( -2.340070819011249803, -5.519915254237290014, 4.950151441910549899 ) ) ;
#13418=CARTESIAN_POINT ( 'NONE',  ( -1.586727176531439909, -1.982989471729919906, 2.961885344765640138 ) ) ;
#13420=CARTESIAN_POINT ( 'NONE',  ( -1.378221871957430178, -5.479872881355929870, 6.607619368096279366 ) ) ;
#13424=CARTESIAN_POINT ( 'NONE',  ( 2.342931736853870017, -4.102223705964150646, 4.477701633099130163 ) ) ;
#13425=CARTESIAN_POINT ( 'NONE',  ( 2.039016451601951108, -2.588484967225421762, 4.939402908764060740 ) ) ;
#13428=B_SPLINE_CURVE_WITH_KNOTS ( 'NONE', 3,
 ( #454, #6361, #6095, #11754, #16102, #7675, #13316 ),
 .UNSPECIFIED., .F., .F.,
 ( 4, 1, 1, 1, 4 ),
 ( 0.000000000000000000, 0.3003308066894049833, 0.4325493167363730351, 0.5576349185191149527, 0.7853981633974479459 ),
 .UNSPECIFIED. ) ;
#13433=CARTESIAN_POINT ( 'NONE',  ( -1.286937324407759986, -3.589881363621809651, 2.729584305145209999 ) ) ;
#13443=CARTESIAN_POINT ( 'NONE',  ( 2.224278379903029901, -5.090889830508480429, 5.468825643806100700 ) ) ;
#13447=CARTESIAN_POINT ( 'NONE',  ( 0.1608173401625761778, -4.498124606865046893, 6.746714348835997299 ) ) ;
#13448=CARTESIAN_POINT ( 'NONE',  ( 0.6640878839024751956, -0.4379237288135597317, 7.269405042592523181 ) ) ;
#13450=CARTESIAN_POINT ( 'NONE',  ( 0.4360591020457930123, -0.3088983050847460277, 2.387347919655840034 ) ) ;
#13453=CARTESIAN_POINT ( 'NONE',  ( -1.851400890972779045, -0.1868644067796610686, 6.601359968904141340 ) ) ;
#13455=CARTESIAN_POINT ( 'NONE',  ( 0.03714311608463249925, -1.078587104846650435, 7.053160869216426931 ) ) ;
#13456=CARTESIAN_POINT ( 'NONE',  ( -0.1869574461324000070, -0.5962015548080630278, 2.350675676344399889 ) ) ;
#13457=CARTESIAN_POINT ( 'NONE',  ( -2.199635523370571111, -5.057043525783965876, 3.215170965529011493 ) ) ;
#13460=CARTESIAN_POINT ( 'NONE',  ( -1.265407828724339989, -3.290974492234040483, 2.715689360385570073 ) ) ;
#13461=CARTESIAN_POINT ( 'NONE',  ( -0.7756407636288503715, -4.591277760018214416, 7.238010066725332869 ) ) ;
#13464=CARTESIAN_POINT ( 'NONE',  ( -0.4365326870213908639, -4.269082600342137823, 6.706076034398992469 ) ) ;
#13467=CARTESIAN_POINT ( 'NONE',  ( -1.217499609005920025, -1.707370888630439065, 3.046943272389440960 ) ) ;
#13472=CARTESIAN_POINT ( 'NONE',  ( 0.5637478356992829953, -0.6606104644819250638, 2.398845082743519708 ) ) ;
#13473=CARTESIAN_POINT ( 'NONE',  ( 1.292937800126339631, -2.522460978720530989, 7.017633607369027082 ) ) ;
#13476=CARTESIAN_POINT ( 'NONE',  ( 2.046174187462399985, -1.121322805063259986, 5.862719605943959245 ) ) ;
#13478=CARTESIAN_POINT ( 'NONE',  ( 0.06264882350516240428, -5.148728813559320550, 7.052569299041220319 ) ) ;
#13486=CARTESIAN_POINT ( 'NONE',  ( -0.9222751404131109831, -5.577754237288145234, 2.865854510788139908 ) ) ;
#13487=CARTESIAN_POINT ( 'NONE',  ( 1.788074174585509768, -3.617010528270069525, 2.738902236199779239 ) ) ;
#13489=CARTESIAN_POINT ( 'NONE',  ( -1.292937800126279679, -3.077539021279473097, 7.017633607369056392 ) ) ;
#13495=CARTESIAN_POINT ( 'NONE',  ( -1.303621121494419999, -4.362235753495300905, 6.659417683669699883 ) ) ;
#13498=CARTESIAN_POINT ( 'NONE',  ( -1.883442729065680776, -3.147403886144331420, 6.569694408006696129 ) ) ;
#13503=CARTESIAN_POINT ( 'NONE',  ( -0.1569242594330230167, -1.400782264522720144, 7.048216443236290374 ) ) ;
#13504=CARTESIAN_POINT ( 'NONE',  ( -1.943632316591239917, -0.5536016949152539057, 3.373048379518170048 ) ) ;
#13506=CARTESIAN_POINT ( 'NONE',  ( -3.408368997776849933E-15, -5.599999999999999645, 2.350000000000000089 ) ) ;
#13517=CARTESIAN_POINT ( 'NONE',  ( -2.199335452462570117, -1.866548030288480042, 3.862342996790939953 ) ) ;
#13518=CARTESIAN_POINT ( 'NONE',  ( -2.180207327701300102, -5.506567796610169374, 5.586116916730199833 ) ) ;
#13520=CARTESIAN_POINT ( 'NONE',  ( 2.169623098572349917, -2.658349832090280529, 5.611855963200990338 ) ) ;
#13524=CARTESIAN_POINT ( 'NONE',  ( -0.1352600594605981310, -1.400782264522720366, 6.748562071049556188 ) ) ;
#13531=CARTESIAN_POINT ( 'NONE',  ( -2.219956784870669608, -3.426863345603790023, 3.918630970161619764 ) ) ;
#13539=CARTESIAN_POINT ( 'NONE',  ( -2.345900685764729765, -5.228813559322030180, 4.512231114381339836 ) ) ;
#13542=CARTESIAN_POINT ( 'NONE',  ( -2.102728310581289950, -1.358046564306109927, 5.757014351541099195 ) ) ;
#13546=CARTESIAN_POINT ( 'NONE',  ( 1.627161714697888728, -3.962493976234419790, 3.448102801005814122 ) ) ;
#13547=CARTESIAN_POINT ( 'NONE',  ( -2.304156201936080617, -0.2002118644067801267, 6.016707707703351282 ) ) ;
#13551=CARTESIAN_POINT ( 'NONE',  ( -2.625437065641401446, -0.2180084745762719822, 5.087214675345155257 ) ) ;
#13556=CARTESIAN_POINT ( 'NONE',  ( -2.345900685764729765, -5.528813559322030002, 4.512231114381339836 ) ) ;
#13557=CARTESIAN_POINT ( 'NONE',  ( 2.349129089426440054, -0.7059744922340410733, 4.842612091679071362 ) ) ;
#13558=CARTESIAN_POINT ( 'NONE',  ( 1.641808337277750107, -5.413135593220339103, 6.386111670537619744 ) ) ;
#13559=CARTESIAN_POINT ( 'NONE',  ( -2.006003143955999324, -4.731007489747939054, 6.437545705712661714 ) ) ;
#13563=CARTESIAN_POINT ( 'NONE',  ( -0.7046366965007886396, -4.911779243796845051, 2.768871435390180213 ) ) ;
#13564=CARTESIAN_POINT ( 'NONE',  ( -2.145694642186069867, -4.501965483225029985, 5.666819626392589626 ) ) ;
#13565=CARTESIAN_POINT ( 'NONE',  ( -2.051568858000911266, -5.080331814072260421, 3.016498023208352919 ) ) ;
#13570=CARTESIAN_POINT ( 'NONE',  ( -1.138568046961029978, -4.362235753495300905, 6.408380708468528475 ) ) ;
#13574=CARTESIAN_POINT ( 'NONE',  ( 1.272929729338649674, -0.9155690868286361361, 6.310761232086846917 ) ) ;
#13578=CARTESIAN_POINT ( 'NONE',  ( 1.652654650382400003, -0.7952867690272209522, 3.029252778805620050 ) ) ;
#13579=CARTESIAN_POINT ( 'NONE',  ( -1.720450724489941852, -2.825208726468270370, 6.720683794561613134 ) ) ;
#13584=CARTESIAN_POINT ( 'NONE',  ( 1.994315313497110997, -5.086440677966105994, 5.187224322759965922 ) ) ;
#13592=CARTESIAN_POINT ( 'NONE',  ( 0.7093417302541469294, -5.435381355932199732, 6.943956659919690466 ) ) ;
#13593=CARTESIAN_POINT ( 'NONE',  ( 2.603140590302639890, -3.873181699441240244, 5.216500493824248963 ) ) ;
#13595=ADVANCED_FACE ( 'NONE', ( #11820 ), #1920, .T. ) ;
#13598=CARTESIAN_POINT ( 'NONE',  ( -0.2818998297622349880, -4.245794312053860153, 7.036509827384409554 ) ) ;
#13601=CARTESIAN_POINT ( 'NONE',  ( 0.3832714063289482387, -2.914521003261450360, 7.326064873930673294 ) ) ;
#13606=CARTESIAN_POINT ( 'NONE',  ( -2.345213174852959881, -1.796683165423619943, 4.503223853122380049 ) ) ;
#13607=CARTESIAN_POINT ( 'NONE',  ( -2.043308330018790198, -0.5002118644067800046, 5.867646457774669422 ) ) ;
#13609=CARTESIAN_POINT ( 'NONE',  ( -2.345900685764729765, -5.528813559322030002, 4.512231114381339836 ) ) ;
#13619=CARTESIAN_POINT ( 'NONE',  ( 1.728413393879709936, -4.311818300558750039, 6.297289212178290185 ) ) ;
#13622=CARTESIAN_POINT ( 'NONE',  ( 2.143090896833110381, -5.395338983050850246, 5.672454929438339732 ) ) ;
#13624=CARTESIAN_POINT ( 'NONE',  ( 2.245209214543399945, -2.635061543801989981, 5.405536158119010004 ) ) ;
#13625=CARTESIAN_POINT ( 'NONE',  ( -0.4446501070882828421, -4.952022267818758650, 2.379695998155090031 ) ) ;
#13626=CARTESIAN_POINT ( 'NONE',  ( 1.102492180652039577, -2.309025507765959606, 2.968118700883580541 ) ) ;
#13629=CARTESIAN_POINT ( 'NONE',  ( -1.377628188826471423, -0.5741044150835525883, 2.411088859383701433 ) ) ;
#13631=CARTESIAN_POINT ( 'NONE',  ( 1.555847953988059862, -5.162332993428189631, 3.144152046011940094 ) ) ;
#13633=FILL_AREA_STYLE_COLOUR ( '', #73 ) ;
#13638=CARTESIAN_POINT ( 'NONE',  ( -2.053221424930789407, -4.734848366107910600, 3.549770689668290125 ) ) ;
#13639=CARTESIAN_POINT ( 'NONE',  ( -2.318251751302029984, -5.233262711864409056, 4.294764266798999586 ) ) ;
#13644=CARTESIAN_POINT ( 'NONE',  ( 0.4735094604799090501, -1.032010528270079996, 7.005327412390689901 ) ) ;
#13646=CARTESIAN_POINT ( 'NONE',  ( -0.5902886515192680150, -1.447358841099289917, 6.978224088050050788 ) ) ;
#13647=CARTESIAN_POINT ( 'NONE',  ( -2.630358833876468960, -0.2313559322033900412, 4.347767980622416317 ) ) ;
#13649=CARTESIAN_POINT ( 'NONE',  ( 2.116444151961470066, -0.3533898305084750002, 3.670839500609349937 ) ) ;
#13652=CARTESIAN_POINT ( 'NONE',  ( -2.262450597846769718, -1.404623140882690135, 5.348122657979730299 ) ) ;
#13654=CARTESIAN_POINT ( 'NONE',  ( -1.851073041990159984, -5.493220338983049622, 6.153284478378270528 ) ) ;
#13655=CARTESIAN_POINT ( 'NONE',  ( -0.6919952253609726878, -1.148451969711520082, 7.262080463428013388 ) ) ;
#13658=CARTESIAN_POINT ( 'NONE',  ( 2.316639661709690046, -3.780028546288089597, 4.285359956977719875 ) ) ;
#13661=CARTESIAN_POINT ( 'NONE',  ( -1.872456193198849705, -4.501965483225034426, 5.541908336566010007 ) ) ;
#13664=CARTESIAN_POINT ( 'NONE',  ( -0.5805547688319036004, -3.360839357098899693, 2.730772231808969774 ) ) ;
#13669=CARTESIAN_POINT ( 'NONE',  ( 1.545075033357670158, -0.4774152569121719591, 2.920238509828300355 ) ) ;
#13670=CARTESIAN_POINT ( 'NONE',  ( 1.236224677598260158, -1.986830348089900777, 2.351625617688071657 ) ) ;
#13674=CARTESIAN_POINT ( 'NONE',  ( -2.012177589105470066, -5.215466101694915757, 5.107213040360599088 ) ) ;
#13678=ORIENTED_EDGE ( 'NONE', *, *, #10868, .F. ) ;
#13685=CARTESIAN_POINT ( 'NONE',  ( 2.350067830300900162, -5.377542372881360500, 4.825253242917690422 ) ) ;
#13686=CARTESIAN_POINT ( 'NONE',  ( 1.670747221194369914, -0.4963798976394459550, 3.047345349617600174 ) ) ;
#13687=CARTESIAN_POINT ( 'NONE',  ( 0.009452039534070141164, -0.3001931771041043140, 2.350000000173209092 ) ) ;
#13688=CARTESIAN_POINT ( 'NONE',  ( -2.295344368707641358, -3.473439922180372452, 3.367893426919611688 ) ) ;
#13690=CARTESIAN_POINT ( 'NONE',  ( 1.854177340199709922, -3.989623140882689434, 6.149404042554680316 ) ) ;
#13694=CARTESIAN_POINT ( 'NONE',  ( 2.212163452524050111, -2.704926408666860738, 6.166099093621837390 ) ) ;
#13697=CARTESIAN_POINT ( 'NONE',  ( 2.116444151961470066, -0.3533898305084750002, 3.670839500609349937 ) ) ;
#13698=CARTESIAN_POINT ( 'NONE',  ( -0.8429265834919730249, -2.076142624883080323, 2.502678798553459760 ) ) ;
#13699=CARTESIAN_POINT ( 'NONE',  ( -1.477796163681079911, -0.4824152542372879826, 6.531563725478150673 ) ) ;
#13701=CARTESIAN_POINT ( 'NONE',  ( 2.304156201936080617, -5.399788135593215799, 6.016707707703351282 ) ) ;
#13705=CARTESIAN_POINT ( 'NONE',  ( 0.9150601050661637537, -5.130932203389829027, 6.868218666554229301 ) ) ;
#13709=CARTESIAN_POINT ( 'NONE',  ( 1.021156010535390068, -3.846052534792979927, 2.579625955254269964 ) ) ;
#13710=CARTESIAN_POINT ( 'NONE',  ( 1.791574935211219799, -5.408686440677969998, 6.226029630577610163 ) ) ;
#13712=CARTESIAN_POINT ( 'NONE',  ( -1.816660071039029933, -3.170692174432619748, 6.196159040268240936 ) ) ;
#13714=CARTESIAN_POINT ( 'NONE',  ( 0.01333550863827670518, -2.169295778036230526, 2.647020699851690306 ) ) ;
#13716=CARTESIAN_POINT ( 'NONE',  ( -0.5058614788087384406, -0.2909039927201511055, 2.084176093893880921 ) ) ;
#13720=CARTESIAN_POINT ( 'NONE',  ( -1.951437470830620136, -5.057043525783970317, 3.384463041838880137 ) ) ;
#13725=CARTESIAN_POINT ( 'NONE',  ( 2.143090896833110381, -5.095338983050850423, 5.672454929438339732 ) ) ;
#13729=CARTESIAN_POINT ( 'NONE',  ( 1.670747221194369914, -0.4963798976394459550, 3.047345349617600174 ) ) ;
#13731=CARTESIAN_POINT ( 'NONE',  ( 1.644832646965660006, -1.191187669928119863, 6.383232381746459794 ) ) ;
#13732=CARTESIAN_POINT ( 'NONE',  ( -1.666450993087168930, -0.1824152542372889096, 6.765380371283871597 ) ) ;
#13733=CARTESIAN_POINT ( 'NONE',  ( -2.350067830300900162, -0.5224576271186440746, 4.825253242917699303 ) ) ;
#13736=CARTESIAN_POINT ( 'NONE',  ( 0.2189795514005130062, -0.004449152542373159894, 2.356806637999009801 ) ) ;
#13738=CARTESIAN_POINT ( 'NONE',  ( 2.161802606005189809, -0.5895330507925999886, 3.769755311421790989 ) ) ;
#13739=CARTESIAN_POINT ( 'NONE',  ( -2.203023580853999963, -5.542161016949149754, 3.872235369154300333 ) ) ;
#13740=CARTESIAN_POINT ( 'NONE',  ( -2.248786803694121428, -1.334758276017820267, 6.109280527266697014 ) ) ;
#13743=CARTESIAN_POINT ( 'NONE',  ( -2.329383452786330189, -4.571830348089889640, 5.035735636132879556 ) ) ;
#13746=CARTESIAN_POINT ( 'NONE',  ( -1.876226141297921091, -4.711560077819614278, 3.866526959224360294 ) ) ;
#13751=CARTESIAN_POINT ( 'NONE',  ( -1.795861365445549973, -0.2491525423728821742, 3.705232155007899930 ) ) ;
#13752=CARTESIAN_POINT ( 'NONE',  ( 2.649291707874080970, -2.243001519261071053, 4.543900225523779035 ) ) ;
#13755=CARTESIAN_POINT ( 'NONE',  ( 1.562863241354470523, -5.408686440677975327, 6.031217337312382298 ) ) ;
#13758=CARTESIAN_POINT ( 'NONE',  ( 1.943632316591230147, -5.346398305084740343, 3.373048379518159834 ) ) ;
#13761=CARTESIAN_POINT ( 'NONE',  ( -3.503171016405825766E-15, -5.600000000000000533, 2.649999999999998579 ) ) ;
#13762=CARTESIAN_POINT ( 'NONE',  ( 2.358786130710011086, -3.943046564306109669, 5.916240799583690979 ) ) ;
#13763=CARTESIAN_POINT ( 'NONE',  ( 1.152986057739970205, -3.846052534792983923, 2.309657588616410351 ) ) ;
#13765=CARTESIAN_POINT ( 'NONE',  ( 2.051973656473811136, -0.6826862039457533005, 4.634380218157459375 ) ) ;
#13773=CARTESIAN_POINT ( 'NONE',  ( -1.477796163681079911, -0.4824152542372879826, 6.531563725478150673 ) ) ;
#13774=CARTESIAN_POINT ( 'NONE',  ( 2.276802572547980130, -2.495331814072260013, 4.104251954998760610 ) ) ;
#13776=CARTESIAN_POINT ( 'NONE',  ( -0.1698804968610999888, -0.2965485159365569556, 2.349238660949160007 ) ) ;
#13777=CARTESIAN_POINT ( 'NONE',  ( 2.586172839791708533, -5.064194915254235596, 4.104546363490936045 ) ) ;
#13785=CARTESIAN_POINT ( 'NONE',  ( -2.137408332595969629, -3.450151633892079683, 3.714996798363980002 ) ) ;
#13786=EDGE_CURVE ( 'NONE', #6595, #14665, #12927, .T. ) ;
#13792=CARTESIAN_POINT ( 'NONE',  ( -2.334032080503389839, -3.310421904162350160, 5.001728246382240783 ) ) ;
#13794=CARTESIAN_POINT ( 'NONE',  ( -2.065623031241579977, -5.033755237495680213, 3.572193642975310279 ) ) ;
#13796=CARTESIAN_POINT ( 'NONE',  ( 0.5805547688318586363, -2.239160642901089293, 2.730772231808960449 ) ) ;
#13799=CARTESIAN_POINT ( 'NONE',  ( -0.9193620247240871235, -0.2831443699174389095, 2.206709149717571261 ) ) ;
#13808=CARTESIAN_POINT ( 'NONE',  ( 2.034805890357269220, -5.068644067796615360, 4.427518626519221456 ) ) ;
#13814=CARTESIAN_POINT ( 'NONE',  ( -2.306572132003601450, -4.478677194936736328, 6.012569500204175910 ) ) ;
#13817=CARTESIAN_POINT ( 'NONE',  ( 1.303621121494459967, -1.237764246504700072, 6.659417683669679455 ) ) ;
#13819=CARTESIAN_POINT ( 'NONE',  ( 1.438959988998139914E-16, -2.775557561562889872E-16, 2.350000000000000089 ) ) ;
#13821=CARTESIAN_POINT ( 'NONE',  ( -1.925796468768790071, -0.4957627118644070130, 6.052706598917719560 ) ) ;
#13822=CARTESIAN_POINT ( 'NONE',  ( -2.051331987628511211, -0.5269067796610176213, 4.618035453557344461 ) ) ;
#13826=CARTESIAN_POINT ( 'NONE',  ( -0.3171869470818471370, -0.1557203389830511819, 7.334814496515233095 ) ) ;
#13831=CARTESIAN_POINT ( 'NONE',  ( -0.5570002967655938164, -2.708767285026831395, 6.986590552960220357 ) ) ;
#13832=CARTESIAN_POINT ( 'NONE',  ( -2.353194804772640314, -5.524364406779660008, 4.731327187377240229 ) ) ;
#13834=CARTESIAN_POINT ( 'NONE',  ( -2.437122747866789840, -5.010466949207390108, 3.649501829874993941 ) ) ;
#13837=CARTESIAN_POINT ( 'NONE',  ( 2.049150047780149642, -0.7059744922340407403, 4.826039376028505856 ) ) ;
#13838=CARTESIAN_POINT ( 'NONE',  ( -2.649108131072720695, -4.894025507765944916, 4.859184807329705258 ) ) ;
#13842=CARTESIAN_POINT ( 'NONE',  ( -0.3257255101953093757, -1.424070552811000701, 6.727018681373241549 ) ) ;
#13848=CARTESIAN_POINT ( 'NONE',  ( 1.980638384804650931, -0.3622881355932213721, 4.159858630563753934 ) ) ;
#13851=CARTESIAN_POINT ( 'NONE',  ( 1.011820239713300484, -1.963542059801608897, 2.246566997958089118 ) ) ;
#13852=CARTESIAN_POINT ( 'NONE',  ( -1.676695548152530968, -4.829629811528105776, 2.630596693608521885 ) ) ;
#13853=CARTESIAN_POINT ( 'NONE',  ( -1.392553072310521278, -5.264406779661021218, 3.191531554476531252 ) ) ;
#13860=CARTESIAN_POINT ( 'NONE',  ( -0.5889081234606770021, -5.462076271186440124, 6.978529000034869867 ) ) ;
#13863=CARTESIAN_POINT ( 'NONE',  ( -2.651429253058529945, -4.618406924666464519, 4.585822029124955179 ) ) ;
#13864=CARTESIAN_POINT ( 'NONE',  ( 2.470260739716200860, -4.032358841099289215, 3.729986819255199926 ) ) ;
#13866=CARTESIAN_POINT ( 'NONE',  ( -1.741179788930630190, -1.334758276017820267, 5.787747574231985936 ) ) ;
#13871=DIRECTION ( 'NONE',  ( 0.7045302523384989746, -0.08528919673497019349, -0.7045302523385029714 ) ) ;
#13872=CARTESIAN_POINT ( 'NONE',  ( 2.653602652190420574, -0.3756355932203404024, 4.735326402787084277 ) ) ;
#13874=CARTESIAN_POINT ( 'NONE',  ( 1.866416942370620058, -3.962493976234419790, 3.266391446483460026 ) ) ;
#13875=CARTESIAN_POINT ( 'NONE',  ( -0.004607033757067210099, -5.223017583943910580, 2.216967106706590140 ) ) ;
#13877=CARTESIAN_POINT ( 'NONE',  ( -2.230812463554230352, -5.497669491525425833, 6.137473736419926773 ) ) ;
#13880=CARTESIAN_POINT ( 'NONE',  ( -2.253200202764409354, -5.211016949152539546, 5.379408587037509903 ) ) ;
#13885=CARTESIAN_POINT ( 'NONE',  ( -0.6918414964982418924, -3.659746228486680408, 2.450533167346770291 ) ) ;
#13887=CARTESIAN_POINT ( 'NONE',  ( 0.6410058658986126368, -5.311531839079355777, 2.106117395030960626 ) ) ;
#13891=CARTESIAN_POINT ( 'NONE',  ( -2.349464193210359930, -3.356998480738930368, 4.563019372514619754 ) ) ;
#13892=CARTESIAN_POINT ( 'NONE',  ( -0.1686436619862690112, -4.981295943764798118, 2.349239845786320391 ) ) ;
#13893=CARTESIAN_POINT ( 'NONE',  ( -1.555285212483289659, -3.520016498756949552, 3.359854578615099285 ) ) ;
#13898=CARTESIAN_POINT ( 'NONE',  ( -2.161802606005209793, -5.010466949207389220, 3.769755311421840283 ) ) ;
#13907=CARTESIAN_POINT ( 'NONE',  ( -2.041338374031088865, -5.219915254237295521, 4.918217215283674726 ) ) ;
#13909=CARTESIAN_POINT ( 'NONE',  ( -1.945845091386011250, -1.660794312053860633, 2.895339208235828909 ) ) ;
#13913=CARTESIAN_POINT ( 'NONE',  ( -1.670747221194380128, -5.103620102360550526, 3.047345349617600174 ) ) ;
#13916=CARTESIAN_POINT ( 'NONE',  ( -2.340959815966380031, -1.750106588847040179, 4.942183458383479611 ) ) ;
#13917=CARTESIAN_POINT ( 'NONE',  ( -1.031876288691620625, -0.1690677966101698793, 7.145012538880312292 ) ) ;
#13918=CARTESIAN_POINT ( 'NONE',  ( 0.5889081234606849957, -0.4379237288135600092, 6.978529000034869867 ) ) ;
#13920=CARTESIAN_POINT ( 'NONE',  ( -1.925796468768790071, -0.1957627118644069963, 6.052706598917719560 ) ) ;
#13921=CARTESIAN_POINT ( 'NONE',  ( 2.053221424930760097, -0.8651516338920849369, 3.549770689668250157 ) ) ;
#13925=CARTESIAN_POINT ( 'NONE',  ( 1.816660071039059465, -2.429307825567370571, 6.196159040268200968 ) ) ;
#13927=CARTESIAN_POINT ( 'NONE',  ( 1.666450993087180477, -5.417584745762705545, 6.765380371283858274 ) ) ;
#13929=CARTESIAN_POINT ( 'NONE',  ( -1.552749016687749783, -1.563800282540730002, 6.468535037441760061 ) ) ;
#13930=CARTESIAN_POINT ( 'NONE',  ( -1.652654650382400003, -4.804713230972780025, 3.029252778805629820 ) ) ;
#13934=CARTESIAN_POINT ( 'NONE',  ( -1.998374131852739266, -4.664983501243040287, 4.229465546630535755 ) ) ;
#13940=CARTESIAN_POINT ( 'NONE',  ( -2.034805890357269220, -0.2313559322033900412, 4.427518626519226785 ) ) ;
#13941=CARTESIAN_POINT ( 'NONE',  ( 1.597383073937500786, -3.593722239981783861, 2.580688553303249755 ) ) ;
#13943=CARTESIAN_POINT ( 'NONE',  ( -0.7252674547190166576, -5.211074464177385401, 2.776474344060209987 ) ) ;
#13944=CARTESIAN_POINT ( 'NONE',  ( -1.901882987994748975, -5.206567796610170440, 5.472995608211450147 ) ) ;
#13947=CARTESIAN_POINT ( 'NONE',  ( 2.345900685764729765, -0.07118644067796647823, 4.512231114381329178 ) ) ;
#13949=CARTESIAN_POINT ( 'NONE',  ( -0.8244235255442939891, -0.5829339996946389935, 2.492493020344019872 ) ) ;
#13951=CARTESIAN_POINT ( 'NONE',  ( -0.6493550500446439999, -5.586652542372879005, 2.437955526623099889 ) ) ;
#13952=CARTESIAN_POINT ( 'NONE',  ( 2.543624461644950152, -3.896469987729531681, 5.457025951419980814 ) ) ;
#13954=CARTESIAN_POINT ( 'NONE',  ( -1.224086244040909488, -1.241605122864670285, 6.348185277745776567 ) ) ;
#13958=CARTESIAN_POINT ( 'NONE',  ( -1.661700935788390066, -0.5625000000000000000, 3.038299064211610112 ) ) ;
#13959=CARTESIAN_POINT ( 'NONE',  ( -2.062913653388399826, -3.217268751009200400, 5.832754583370829415 ) ) ;
#13962=CARTESIAN_POINT ( 'NONE',  ( 2.519547246525509543, -5.059745762711855832, 3.866491354109194756 ) ) ;
#13968=CARTESIAN_POINT ( 'NONE',  ( 0.1768565782245979934, -3.752899381639830168, 2.353200596935780098 ) ) ;
#13970=CARTESIAN_POINT ( 'NONE',  ( 1.661700935788380074, -5.037500000000000533, 3.038299064211610112 ) ) ;
#13973=CARTESIAN_POINT ( 'NONE',  ( -0.6864473529425049181, -4.591277760018209975, 6.951118770549909343 ) ) ;
#13975=CARTESIAN_POINT ( 'NONE',  ( 0.5302109551885175742, -3.799475958216412153, 2.716624547488259989 ) ) ;
#13976=CARTESIAN_POINT ( 'NONE',  ( -1.112838723655040107, -0.4735169491525429986, 6.773667561836210105 ) ) ;
#13981=SURFACE_STYLE_FILL_AREA ( #10843 ) ;
#13985=( BOUNDED_SURFACE ( )  B_SPLINE_SURFACE ( 3, 3, ( 
 ( #8420, #9716, #5734, #18197, #2684, #7040, #8609 ),
 ( #18031, #9811, #13887, #8337, #2777, #2864, #1482 ),
 ( #2592, #9900, #8514, #4238, #6851, #9995, #14252 ),
 ( #11099, #89, #7139, #14057, #9622, #5460, #13970 ),
 ( #15659, #15469, #1203, #1291, #12497, #5377, #2967 ),
 ( #5553, #15282, #16746, #18111, #4059, #12582, #15383 ),
 ( #11199, #6934, #12684, #16842, #5, #5647, #11290 ) ),
 .UNSPECIFIED., .T., .F., .F. ) 
 B_SPLINE_SURFACE_WITH_KNOTS ( ( 4, 3, 4 ),
 ( 4, 1, 1, 1, 4 ),
 ( 0.000000000000000000, 3.141592653589790007, 6.283185307179590673 ),
 ( 0.000000000000000000, 0.3003308066894049833, 0.4325493167363730351, 0.5576349185191149527, 0.7853981633974479459 ),
 .UNSPECIFIED. ) 
 GEOMETRIC_REPRESENTATION_ITEM ( )  RATIONAL_B_SPLINE_SURFACE ( (
 ( 1.000000000000000000, 1.000000000000000000, 1.000000000000000000, 1.000000000000000000, 1.000000000000000000, 1.000000000000000000, 1.000000000000000000),
 ( 0.3333333333333329818, 0.3333333333333329818, 0.3333333333333329818, 0.3333333333333329818, 0.3333333333333329818, 0.3333333333333329818, 0.3333333333333329818),
 ( 0.3333333333333329818, 0.3333333333333329818, 0.3333333333333329818, 0.3333333333333329818, 0.3333333333333329818, 0.3333333333333329818, 0.3333333333333329818),
 ( 1.000000000000000000, 1.000000000000000000, 1.000000000000000000, 1.000000000000000000, 1.000000000000000000, 1.000000000000000000, 1.000000000000000000),
 ( 0.3333333333333329818, 0.3333333333333329818, 0.3333333333333329818, 0.3333333333333329818, 0.3333333333333329818, 0.3333333333333329818, 0.3333333333333329818),
 ( 0.3333333333333329818, 0.3333333333333329818, 0.3333333333333329818, 0.3333333333333329818, 0.3333333333333329818, 0.3333333333333329818, 0.3333333333333329818),
 ( 1.000000000000000000, 1.000000000000000000, 1.000000000000000000, 1.000000000000000000, 1.000000000000000000, 1.000000000000000000, 1.000000000000000000) ) ) 
 REPRESENTATION_ITEM ( '' )  SURFACE ( )  );
#13988=CARTESIAN_POINT ( 'NONE',  ( 1.949083719010301197, -5.059745762711855832, 4.055210292801453953 ) ) ;
#13994=CARTESIAN_POINT ( 'NONE',  ( -1.003115764947269950, -1.493935417675869903, 6.828967930617589666 ) ) ;
#13995=CARTESIAN_POINT ( 'NONE',  ( -2.039016451601939117, -3.011515032774579215, 4.939402908764104261 ) ) ;
#13997=CARTESIAN_POINT ( 'NONE',  ( -2.224278379903029901, -0.2091101694915259990, 5.468825643806110470 ) ) ;
#13999=CARTESIAN_POINT ( 'NONE',  ( 2.253200202764420013, -0.3889830508474579895, 5.379408587037500133 ) ) ;
#14000=EDGE_CURVE ( 'NONE', #14847, #11001, #11397, .T. ) ;
#14004=CARTESIAN_POINT ( 'NONE',  ( 2.345900685764729765, -0.07118644067796649211, 4.512231114381330066 ) ) ;
#14010=CARTESIAN_POINT ( 'NONE',  ( 1.669205944673859854, -2.452596113855660676, 6.359065158982410537 ) ) ;
#14011=( NAMED_UNIT ( * ) PLANE_ANGLE_UNIT ( ) SI_UNIT ( $, .RADIAN. ) );
#14012=CARTESIAN_POINT ( 'NONE',  ( 0.3171869470818560743, -5.444279661016954819, 7.334814496515233095 ) ) ;
#14015=CARTESIAN_POINT ( 'NONE',  ( -1.580445181003969912, -0.5580508474576266753, 3.389704561770339630 ) ) ;
#14020=CARTESIAN_POINT ( 'NONE',  ( -1.945780800405131350, -4.688271789531334832, 4.045142061754299689 ) ) ;
#14026=CARTESIAN_POINT ( 'NONE',  ( 1.846259792136599076, -0.3533898305084745561, 3.802221692020924415 ) ) ;
#14027=CARTESIAN_POINT ( 'NONE',  ( 0.4722227023514015687, -3.477280798540335560, 2.088464165977070408 ) ) ;
#14030=CARTESIAN_POINT ( 'NONE',  ( -0.4649462444738060030, -5.251463457376920552, 2.383584851084299849 ) ) ;
#14031=CARTESIAN_POINT ( 'NONE',  ( 0.05465110135556765225, -5.148728813559319661, 6.752241303418941243 ) ) ;
#14033=CARTESIAN_POINT ( 'NONE',  ( 1.194742379459969861, -0.1245762711864410038, 6.727584234649758521 ) ) ;
#14034=CARTESIAN_POINT ( 'NONE',  ( 1.661700935788380074, -5.337500000000000355, 3.038299064211610112 ) ) ;
#14038=CARTESIAN_POINT ( 'NONE',  ( -0.8189529353761560992, -1.777235753495300052, 2.493631540942749858 ) ) ;
#14040=CARTESIAN_POINT ( 'NONE',  ( -2.231116159141639965, -4.688271789531330391, 3.951089877392499616 ) ) ;
#14044=CARTESIAN_POINT ( 'NONE',  ( 1.668798118857418133, -5.037502670768956747, 3.031201881142577381 ) ) ;
#14045=CARTESIAN_POINT ( 'NONE',  ( -1.112838723655040107, -0.4735169491525429986, 6.773667561836210105 ) ) ;
#14046=CARTESIAN_POINT ( 'NONE',  ( -2.036228139452650243, -3.473439922180369788, 3.519948877554409883 ) ) ;
#14048=CARTESIAN_POINT ( 'NONE',  ( 2.416676968769261080, -5.095338983050850423, 5.796598111919825769 ) ) ;
#14053=B_SPLINE_CURVE_WITH_KNOTS ( 'NONE', 3,
 ( #8672, #1828, #1905, #13119, #6070, #13197, #6166 ),
 .UNSPECIFIED., .F., .F.,
 ( 4, 1, 1, 1, 4 ),
 ( 5.497787143782139729, 5.798117950472390092, 5.930336460519450625, 6.055422062302069364, 6.283185307179590673 ),
 .UNSPECIFIED. ) ;
#14056=CARTESIAN_POINT ( 'NONE',  ( 0.8001094918299610503, -1.307629111369559949, 7.230402832373829192 ) ) ;
#14057=CARTESIAN_POINT ( 'NONE',  ( 0.9866023595736967966, -5.020626044399130627, 2.560054107758459985 ) ) ;
#14061=CARTESIAN_POINT ( 'NONE',  ( 1.567709126316360058, -3.915917399657849796, 2.944712621036570166 ) ) ;
#14063=CARTESIAN_POINT ( 'NONE',  ( -1.698651900122509995, -3.193980462720909408, 5.853032334688971439 ) ) ;
#14066=CARTESIAN_POINT ( 'NONE',  ( -1.066267773695860122, -0.5741044150835525883, 2.929718414487351374 ) ) ;
#14072=CARTESIAN_POINT ( 'NONE',  ( 0.2453710345350221533, -5.144279661016955885, 6.738252723719333481 ) ) ;
#14073=CARTESIAN_POINT ( 'NONE',  ( 1.449852972479971358, -2.010118636378181112, 2.477154964647140911 ) ) ;
#14075=CARTESIAN_POINT ( 'NONE',  ( 1.751366433340660000, -0.7186644140778950529, 2.939816763756370133 ) ) ;
#14080=CARTESIAN_POINT ( 'NONE',  ( 2.169623098572349917, -2.658349832090280529, 5.611855963200990338 ) ) ;
#14081=CARTESIAN_POINT ( 'NONE',  ( -1.259207372045990869, -3.267686203945749490, 3.078488779929933639 ) ) ;
#14082=CARTESIAN_POINT ( 'NONE',  ( -0.4974685680287780354, -0.1601694915254240070, 7.000224381598740386 ) ) ;
#14084=CARTESIAN_POINT ( 'NONE',  ( -1.661700935788390066, -0.5625000000000000000, 3.038299064211610112 ) ) ;
#14087=CARTESIAN_POINT ( 'NONE',  ( -2.224278379903029901, -0.2091101694915259990, 5.468825643806110470 ) ) ;
#14088=CARTESIAN_POINT ( 'NONE',  ( 0.1226612266411070129, -2.937809291549740021, 7.050255286338659388 ) ) ;
#14093=ORIENTED_EDGE ( 'NONE', *, *, #14128, .F. ) ;
#14094=CARTESIAN_POINT ( 'NONE',  ( 2.351999299633229956, -2.266289807549349611, 4.782734406438239994 ) ) ;
#14095=SHAPE_REPRESENTATION_RELATIONSHIP ( 'NONE' , 'NONE' ,  #4513, #5334 ) ;
#14096=CARTESIAN_POINT ( 'NONE',  ( -0.4360591020458099987, -5.591101694915249887, 2.387347919655840034 ) ) ;
#14100=CARTESIAN_POINT ( 'NONE',  ( 1.644832646965660006, -1.191187669928119863, 6.383232381746459794 ) ) ;
#14103=CARTESIAN_POINT ( 'NONE',  ( -1.494593880360799432, -0.5610169491525425212, 3.295456077495951153 ) ) ;
#14109=CARTESIAN_POINT ( 'NONE',  ( 1.893291846171430981, -2.658349832090279197, 5.493944474033856551 ) ) ;
#14111=CARTESIAN_POINT ( 'NONE',  ( 0.4917262214558945632, -0.3088983050847459166, 2.092115739186370948 ) ) ;
#14117=CARTESIAN_POINT ( 'NONE',  ( -0.4339619423229766348, -0.4601694915254239682, 6.706578715862737461 ) ) ;
#14121=CARTESIAN_POINT ( 'NONE',  ( -2.046424002475610404, -5.528813559322025561, 4.536201610417774255 ) ) ;
#14125=CARTESIAN_POINT ( 'NONE',  ( 0.6493550500446279017, -0.01334745762711889855, 2.437955526623101665 ) ) ;
#14128=EDGE_CURVE ( 'NONE', #2833, #7005, #8068, .T. ) ;
#14134=CARTESIAN_POINT ( 'NONE',  ( -0.6150581927481590938, -1.148451969711520082, 6.971662190339330323 ) ) ;
#14137=CARTESIAN_POINT ( 'NONE',  ( -2.350542563031990273, -4.595118636378179744, 4.817027120179790067 ) ) ;
#14146=CARTESIAN_POINT ( 'NONE',  ( 1.800129581279440893, -0.3355932203389832558, 2.750028594811110061 ) ) ;
#14147=CARTESIAN_POINT ( 'NONE',  ( 0.1768565782245979934, -3.752899381639830168, 2.353200596935780098 ) ) ;
#14150=CARTESIAN_POINT ( 'NONE',  ( -0.2469343877495291661, -5.595550847457635868, 2.057675570509529539 ) ) ;
#14161=CARTESIAN_POINT ( 'NONE',  ( -2.161802606005209793, -5.010466949207389220, 3.769755311421840283 ) ) ;
#14163=CARTESIAN_POINT ( 'NONE',  ( 1.475946938622679783, -0.7471169921413568504, 2.482078242844649729 ) ) ;
#14166=CARTESIAN_POINT ( 'NONE',  ( 2.349129089426440054, -0.7059744922340409623, 4.842612091679070474 ) ) ;
#14168=CARTESIAN_POINT ( 'NONE',  ( -2.137408332595969629, -3.450151633892079683, 3.714996798363980002 ) ) ;
#14171=CARTESIAN_POINT ( 'NONE',  ( -0.4625564304287554940, -3.007674156414608557, 6.700235833919871986 ) ) ;
#14176=CARTESIAN_POINT ( 'NONE',  ( -0.7197963925281907205, -0.5829339996946386604, 2.774540890140321014 ) ) ;
#14186=CARTESIAN_POINT ( 'NONE',  ( 2.030998484741458832, -5.081991525423726230, 4.999543428097175557 ) ) ;
#14187=CARTESIAN_POINT ( 'NONE',  ( 2.409576349373750315, -2.149848366107909303, 3.587770028483080242 ) ) ;
#14193=CARTESIAN_POINT ( 'NONE',  ( -2.137408332595969629, -3.450151633892079683, 3.714996798363980002 ) ) ;
#14194=CARTESIAN_POINT ( 'NONE',  ( 1.798783563193339985, -2.382731248990799244, 5.689585537188965425 ) ) ;
#14195=CARTESIAN_POINT ( 'NONE',  ( -2.155845792290839835, -0.2447033898305089883, 3.756158857535780271 ) ) ;
#14199=CARTESIAN_POINT ( 'NONE',  ( -2.234315482767910144, -0.2402542372881359967, 3.960850823455329905 ) ) ;
#14200=CARTESIAN_POINT ( 'NONE',  ( 0.3413183941262679655, -2.914521003261450360, 7.028571974690709823 ) ) ;
#14204=CARTESIAN_POINT ( 'NONE',  ( 1.465095039565329715, -2.033406924666470328, 2.858195935359850726 ) ) ;
#14206=CARTESIAN_POINT ( 'NONE',  ( -2.638803263991410741, -5.519915254237295343, 4.982085668537435730 ) ) ;
#14208=CARTESIAN_POINT ( 'NONE',  ( -1.854177340199669954, -1.610376859117309989, 6.149404042554720284 ) ) ;
#14210=CARTESIAN_POINT ( 'NONE',  ( 0.6493550500446280127, -0.3133474576271190193, 2.437955526623099889 ) ) ;
#14214=CARTESIAN_POINT ( 'NONE',  ( -0.7368491673940088527, -2.076142624883081211, 2.783765372628170809 ) ) ;
#14216=CARTESIAN_POINT ( 'NONE',  ( 2.130266475405040882, -0.3444915254237289615, 3.117337770017949428 ) ) ;
#14218=CARTESIAN_POINT ( 'NONE',  ( -0.4649462444738060030, -5.251463457376920552, 2.383584851084299849 ) ) ;
#14220=ADVANCED_FACE ( 'NONE', ( #11015 ), #13985, .T. ) ;
#14224=CARTESIAN_POINT ( 'NONE',  ( -1.202278654260740876, -5.479872881355935199, 6.364093491318035589 ) ) ;
#14226=CARTESIAN_POINT ( 'NONE',  ( 0.06264882350516240428, -5.448728813559320372, 7.052569299041220319 ) ) ;
#14229=CARTESIAN_POINT ( 'NONE',  ( -0.4005155088301869948, -1.125163681423230200, 7.019123328904779413 ) ) ;
#14232=CARTESIAN_POINT ( 'NONE',  ( 1.951270856817530319, -2.336154672414218592, 5.338313313320885989 ) ) ;
#14238=CARTESIAN_POINT ( 'NONE',  ( -1.873832970144350130, -0.5625000000000005551, 2.826167029855650270 ) ) ;
#14240=CARTESIAN_POINT ( 'NONE',  ( 1.021156010535390068, -3.846052534792979927, 2.579625955254269964 ) ) ;
#14244=CARTESIAN_POINT ( 'NONE',  ( -2.484260633728970546, -5.242161016949150820, 3.766563288620799366 ) ) ;
#14247=CARTESIAN_POINT ( 'NONE',  ( -1.889104232906368974, -5.255508474576268796, 3.296507079072530377 ) ) ;
#14250=CARTESIAN_POINT ( 'NONE',  ( 2.185196738168471153, -0.8418633456037974971, 3.194002352996649474 ) ) ;
#14251=CARTESIAN_POINT ( 'NONE',  ( 0.8675710780368863784, -0.4076464065212254684, 2.836323152971460981 ) ) ;
#14252=CARTESIAN_POINT ( 'NONE',  ( 1.873832970144350130, -5.037500000000000533, 2.826167029855650270 ) ) ;
#14254=CARTESIAN_POINT ( 'NONE',  ( -2.301223891756910334, -2.988226744486289999, 5.193066210047999398 ) ) ;
#14256=CARTESIAN_POINT ( 'NONE',  ( -1.626408692231610109, -4.707719201459649838, 6.401040991074980369 ) ) ;
#14258=CARTESIAN_POINT ( 'NONE',  ( 2.043688444617268729, -4.102223705964154199, 4.504451070148833836 ) ) ;
#14261=CARTESIAN_POINT ( 'NONE',  ( 1.889104232906359870, -0.3444915254237289615, 3.296507079072520163 ) ) ;
#14266=EDGE_LOOP ( 'NONE', ( #3446, #10762, #7173, #14093 ) ) ;
#14268=ORIENTED_EDGE ( 'NONE', *, *, #9832, .T. ) ;
#14269=CARTESIAN_POINT ( 'NONE',  ( 0.9707742057416334225, -5.426483050847465073, 6.508944043303927174 ) ) ;
#14278=CARTESIAN_POINT ( 'NONE',  ( 0.4539185741479240255, -2.215872354612800521, 2.390735265170440105 ) ) ;
#14279=CARTESIAN_POINT ( 'NONE',  ( -1.404946080800599351, -3.244397915657463827, 3.202993536195951840 ) ) ;
#14280=CARTESIAN_POINT ( 'NONE',  ( -2.234315482767910144, -0.2402542372881359967, 3.960850823455329905 ) ) ;
#14284=CARTESIAN_POINT ( 'NONE',  ( -1.795861365445549973, -0.5491525423728815802, 3.705232155007899930 ) ) ;
#14287=CARTESIAN_POINT ( 'NONE',  ( 2.306642602145299925, -0.08453389830508530045, 5.166805192608480368 ) ) ;
#14288=CARTESIAN_POINT ( 'NONE',  ( 2.322440385110930094, -2.518620102360550117, 4.319189883157390497 ) ) ;
#14291=CARTESIAN_POINT ( 'NONE',  ( 1.381042549632459426, -4.059488005747550865, 6.605640880016109051 ) ) ;
#14293=CARTESIAN_POINT ( 'NONE',  ( -0.9002849211310044453, -5.466525423728811006, 7.196465912290821443 ) ) ;
#14295=CARTESIAN_POINT ( 'NONE',  ( -1.289141334274979789, -0.4824152542372879826, 6.297747079672432413 ) ) ;
#14299=CARTESIAN_POINT ( 'NONE',  ( -0.6470883152343470668, -3.030962444702889780, 6.648378442427256729 ) ) ;
#14300=VERTEX_POINT ( 'NONE', #11837 ) ;
#14304=CARTESIAN_POINT ( 'NONE',  ( 1.821706171509118954, -0.3978813559322044724, 5.646608543709396244 ) ) ;
#14308=CARTESIAN_POINT ( 'NONE',  ( -3.503171016405825766E-15, -5.600000000000000533, 2.649999999999998579 ) ) ;
#14309=CARTESIAN_POINT ( 'NONE',  ( -1.641808337277739671, -0.1868644067796620678, 6.386111670537630403 ) ) ;
#14313=CARTESIAN_POINT ( 'NONE',  ( 1.626408692231650077, -0.8922807985403480302, 6.401040991074950171 ) ) ;
#14315=CARTESIAN_POINT ( 'NONE',  ( -1.503314099254069447, -1.660794312053860633, 3.301805249040033363 ) ) ;
#14320=CARTESIAN_POINT ( 'NONE',  ( 1.407651048079441525, -0.02669491525423760975, 2.450250343405061759 ) ) ;
#14321=CARTESIAN_POINT ( 'NONE',  ( 2.190084968185480374, -4.032358841099290103, 3.838447030292440054 ) ) ;
#14324=CARTESIAN_POINT ( 'NONE',  ( -1.610878918935079840, -5.268855932203385883, 2.590989782159090815 ) ) ;
#14327=CARTESIAN_POINT ( 'NONE',  ( -1.057242234132099723, -5.277754237288138306, 2.597442975781531160 ) ) ;
#14328=CARTESIAN_POINT ( 'NONE',  ( 1.646397141422329957, -0.7952877538855639417, 3.035510168540480169 ) ) ;
#14330=CARTESIAN_POINT ( 'NONE',  ( -1.930452136971070987, -1.587088570829020551, 6.521117305355617511 ) ) ;
#14332=CARTESIAN_POINT ( 'NONE',  ( 0.2451610102875899921, -0.3251990024832500104, 2.350791033861340029 ) ) ;
#14334=CARTESIAN_POINT ( 'NONE',  ( 1.097561405233190124, -1.986830348089889897, 2.618148744692249785 ) ) ;
#14337=CARTESIAN_POINT ( 'NONE',  ( -2.556942001999829905, -1.843259742000191048, 3.989253004641622358 ) ) ;
#14339=CARTESIAN_POINT ( 'NONE',  ( -1.549925137359298599, -4.731007489747939054, 6.046340934239856857 ) ) ;
#14347=CARTESIAN_POINT ( 'NONE',  ( 2.000624272291700034, -5.364194915254235418, 4.239366054775996595 ) ) ;
#14349=CARTESIAN_POINT ( 'NONE',  ( -2.653064503426820764, -3.034803321062870651, 4.766048721853594294 ) ) ;
#14355=CARTESIAN_POINT ( 'NONE',  ( -0.5230055860628765041, -5.251463457376924104, 2.087624054227240844 ) ) ;
#14358=CARTESIAN_POINT ( 'NONE',  ( 0.9719602541832789155, -2.844656138396589817, 6.843370931913530519 ) ) ;
#14359=CARTESIAN_POINT ( 'NONE',  ( -1.683529720875190705, -4.455388906648449776, 5.875001924065656134 ) ) ;
#14360=CARTESIAN_POINT ( 'NONE',  ( -1.112838723655040107, -0.1735169491525430097, 6.773667561836210105 ) ) ;
#14364=CARTESIAN_POINT ( 'NONE',  ( -0.02098813186357061100, -3.430704221963769562, 2.046196467083000403 ) ) ;
#14366=CARTESIAN_POINT ( 'NONE',  ( -1.580445181003969912, -0.2580508474576271305, 3.389704561770339630 ) ) ;
#14367=CARTESIAN_POINT ( 'NONE',  ( -2.199335452462570117, -1.866548030288480042, 3.862342996790939953 ) ) ;
#14370=CARTESIAN_POINT ( 'NONE',  ( 0.1569242594330759466, -4.199217735477281721, 7.048216443236287709 ) ) ;
#14372=CARTESIAN_POINT ( 'NONE',  ( 0.5609751937345880402, -5.139830508474575232, 7.293870047334757523 ) ) ;
#14378=CARTESIAN_POINT ( 'NONE',  ( -2.051331987628511211, -0.5269067796610176213, 4.618035453557344461 ) ) ;
#14380=CARTESIAN_POINT ( 'NONE',  ( 0.01333550863827670518, -2.169295778036230526, 2.647020699851690306 ) ) ;
#14385=CARTESIAN_POINT ( 'NONE',  ( 1.901882987994760965, -0.3934322033898309257, 5.472995608211450147 ) ) ;
#14389=CARTESIAN_POINT ( 'NONE',  ( 1.655443486440889789, -5.337500988460059936, 3.044556513559109945 ) ) ;
#14392=CARTESIAN_POINT ( 'NONE',  ( 2.332582362116870200, -5.368644067796609853, 4.387643303570810005 ) ) ;
#14400=CARTESIAN_POINT ( 'NONE',  ( -1.866416942370660026, -1.637506023765569863, 3.266391446483499994 ) ) ;
#14404=CARTESIAN_POINT ( 'NONE',  ( 0.2302241296434710538, -1.893677194936738806, 2.659926792304259990 ) ) ;
#14411=CARTESIAN_POINT ( 'NONE',  ( 2.649108131072720695, -0.7059744922340407403, 4.859184807329644862 ) ) ;
#14412=CARTESIAN_POINT ( 'NONE',  ( 1.973760952634081134, -0.04004237288135625850, 2.925986839873718992 ) ) ;
#14413=CARTESIAN_POINT ( 'NONE',  ( -2.218077401483159683, -4.824160642901089702, 5.486688202856539576 ) ) ;
#14416=CARTESIAN_POINT ( 'NONE',  ( -1.800129581279449775, -5.264406779661021218, 2.750028594811118943 ) ) ;
#14425=CARTESIAN_POINT ( 'NONE',  ( -2.334748642087669523, -4.940602084342530453, 4.403867486184871005 ) ) ;
#14429=CARTESIAN_POINT ( 'NONE',  ( -1.214457691476030110, -1.730659176918720066, 2.684103622926369948 ) ) ;
#14433=CARTESIAN_POINT ( 'NONE',  ( 2.426866425021050766, -0.8884399221803740421, 3.626019996130599665 ) ) ;
#14436=CARTESIAN_POINT ( 'NONE',  ( 1.704669856830330010, -0.8030495317899829510, 3.080704711052640210 ) ) ;
#14448=CARTESIAN_POINT ( 'NONE',  ( -0.6964468257805866980, -5.466525423728811006, 6.631228347243847132 ) ) ;
#14450=CARTESIAN_POINT ( 'NONE',  ( -0.02098813186357061100, -3.430704221963769562, 2.046196467083000403 ) ) ;
#14456=CARTESIAN_POINT ( 'NONE',  ( 2.350542563031990273, -1.004881363621820123, 4.817027120179740329 ) ) ;
#14458=CARTESIAN_POINT ( 'NONE',  ( -2.326448859701059746, -3.380286769027220029, 4.344498395672320434 ) ) ;
#14459=CARTESIAN_POINT ( 'NONE',  ( 1.353302556710500371, -4.036199717459260761, 6.243850391919140819 ) ) ;
#14465=CARTESIAN_POINT ( 'NONE',  ( 2.380466601827069262, -3.710163681423226389, 3.526759849567131955 ) ) ;
#14467=CARTESIAN_POINT ( 'NONE',  ( -2.030998484741458832, -0.2180084745762719822, 4.999543428097190656 ) ) ;
#14468=CARTESIAN_POINT ( 'NONE',  ( 1.611907055891590002, -2.355602084342530045, 2.985210995296850189 ) ) ;
#14475=CARTESIAN_POINT ( 'NONE',  ( 2.182690844914369599, -3.919758276017820453, 5.580117243900430068 ) ) ;
#14477=CARTESIAN_POINT ( 'NONE',  ( -2.458531667407850563, -5.206567796610170440, 5.699238225248945966 ) ) ;
#14480=CARTESIAN_POINT ( 'NONE',  ( 0.3743405594629510280, -0.4423728813559330009, 7.023440622744399953 ) ) ;
#14484=CARTESIAN_POINT ( 'NONE',  ( -1.454969160281959661, -3.147403886144331420, 6.148435909958226198 ) ) ;
#14491=CARTESIAN_POINT ( 'NONE',  ( -1.846259792136611066, -5.546610169491530407, 3.802221692020929744 ) ) ;
#14493=CARTESIAN_POINT ( 'NONE',  ( -3.108624468950439891E-15, -5.299999999999999822, 1.110223024625159893E-15 ) ) ;
#14495=CARTESIAN_POINT ( 'NONE',  ( -2.327043743583479429, -3.217268751009201289, 5.975923629552665872 ) ) ;
#14497=CARTESIAN_POINT ( 'NONE',  ( -1.902324933209429858, -3.197821339080880065, 3.314393441133570040 ) ) ;
#14499=CARTESIAN_POINT ( 'NONE',  ( -1.959085573314230055, -2.964938456198001671, 5.313910057793616026 ) ) ;
#14506=CARTESIAN_POINT ( 'NONE',  ( -2.248786803694121428, -1.334758276017820267, 6.109280527266697014 ) ) ;
#14507=CARTESIAN_POINT ( 'NONE',  ( 2.260890494820590124, -4.055647129387580208, 4.046455925041149371 ) ) ;
#14510=CARTESIAN_POINT ( 'NONE',  ( -2.386628511786350160, -5.246610169491530584, 3.539457309197792778 ) ) ;
#14518=CARTESIAN_POINT ( 'NONE',  ( 2.653064503426820764, -2.565196678937129438, 4.766048721853534786 ) ) ;
#14519=CARTESIAN_POINT ( 'NONE',  ( 0.009452110982655399438, -0.3001920447045380858, 2.050000000000001155 ) ) ;
#14521=CARTESIAN_POINT ( 'NONE',  ( -1.021156010535440029, -1.753947465207009948, 2.579625955254300163 ) ) ;
#14523=CARTESIAN_POINT ( 'NONE',  ( -2.235075160050040921, -1.633665147405598761, 6.130927224539796327 ) ) ;
#14526=CARTESIAN_POINT ( 'NONE',  ( 0.7205524543785531977, -4.428259742000194343, 6.622421910798232503 ) ) ;
#14535=CARTESIAN_POINT ( 'NONE',  ( -1.351903350398179438, -5.484322033898315851, 6.245004350000422200 ) ) ;
#14537=CARTESIAN_POINT ( 'NONE',  ( 2.329383452786330189, -1.028169651910100013, 5.035735636132829818 ) ) ;
#14539=CARTESIAN_POINT ( 'NONE',  ( 2.155845792290829621, -5.355296610169490101, 3.756158857535770057 ) ) ;
#14541=CARTESIAN_POINT ( 'NONE',  ( 1.644832646965660006, -1.191187669928119863, 6.383232381746459794 ) ) ;
#14542=CARTESIAN_POINT ( 'NONE',  ( 2.100188519621589922, -4.009070552810999999, 3.637948273607370275 ) ) ;
#14543=CARTESIAN_POINT ( 'NONE',  ( -1.790316459643189972, -4.734848366107908824, 3.695177221627210074 ) ) ;
#14544=CARTESIAN_POINT ( 'NONE',  ( -0.009452110982656868748, -5.299807955295460005, 2.350000000000000089 ) ) ;
#14547=CARTESIAN_POINT ( 'NONE',  ( -1.562863241354461641, -0.1913135593220339215, 6.031217337312382298 ) ) ;
#14548=CARTESIAN_POINT ( 'NONE',  ( 1.021156010535390068, -3.846052534792979927, 2.579625955254269964 ) ) ;
#14555=CARTESIAN_POINT ( 'NONE',  ( -2.145694642186068979, -4.501965483225029097, 5.666819626392590514 ) ) ;
#14557=CARTESIAN_POINT ( 'NONE',  ( -1.800129581279449775, -5.564406779661021041, 2.750028594811118943 ) ) ;
#14559=CARTESIAN_POINT ( 'NONE',  ( 1.194742379459969861, -0.4245762711864409789, 6.727584234649759409 ) ) ;
#14565=CARTESIAN_POINT ( 'NONE',  ( -1.861802609626409089, -4.800872354612795156, 5.565212624397245733 ) ) ;
#14567=CARTESIAN_POINT ( 'NONE',  ( -2.191755591049691532, -0.5536016949152540167, 3.203650300307721466 ) ) ;
#14572=CARTESIAN_POINT ( 'NONE',  ( -1.707817112497179934, -5.488771186440679628, 6.319218296629480314 ) ) ;
#14575=CARTESIAN_POINT ( 'NONE',  ( 1.947945325730759292, -4.311818300558746486, 6.502393603230323116 ) ) ;
#14578=( BOUNDED_SURFACE ( )  B_SPLINE_SURFACE ( 3, 3, ( 
 ( #8311, #11165, #12833, #13949, #2836, #18276, #11265 ),
 ( #16814, #4128, #18168, #2755, #65, #147, #14752 ),
 ( #418, #1722, #3444, #15793, #17242, #8929, #4560 ),
 ( #9092, #4839, #7537, #7721, #6148, #10484, #10217 ),
 ( #2067, #13365, #6317, #11979, #17591, #3101, #8748 ),
 ( #7374, #17787, #17878, #8009, #2168, #9571, #5124 ),
 ( #9284, #964, #10870, #15054, #1057, #13456, #16328 ) ),
 .UNSPECIFIED., .T., .F., .F. ) 
 B_SPLINE_SURFACE_WITH_KNOTS ( ( 4, 3, 4 ),
 ( 4, 1, 1, 1, 4 ),
 ( 0.000000000000000000, 3.141592653589790007, 6.283185307179590673 ),
 ( 5.497787143782139729, 5.798117950472390092, 5.930336460519450625, 6.055422062302069364, 6.283185307179590673 ),
 .UNSPECIFIED. ) 
 GEOMETRIC_REPRESENTATION_ITEM ( )  RATIONAL_B_SPLINE_SURFACE ( (
 ( 1.000000000000000000, 1.000000000000000000, 1.000000000000000000, 1.000000000000000000, 1.000000000000000000, 1.000000000000000000, 1.000000000000000000),
 ( 0.3333333333333329818, 0.3333333333333329818, 0.3333333333333329818, 0.3333333333333329818, 0.3333333333333329818, 0.3333333333333329818, 0.3333333333333329818),
 ( 0.3333333333333329818, 0.3333333333333329818, 0.3333333333333329818, 0.3333333333333329818, 0.3333333333333329818, 0.3333333333333329818, 0.3333333333333329818),
 ( 1.000000000000000000, 1.000000000000000000, 1.000000000000000000, 1.000000000000000000, 1.000000000000000000, 1.000000000000000000, 1.000000000000000000),
 ( 0.3333333333333329818, 0.3333333333333329818, 0.3333333333333329818, 0.3333333333333329818, 0.3333333333333329818, 0.3333333333333329818, 0.3333333333333329818),
 ( 0.3333333333333329818, 0.3333333333333329818, 0.3333333333333329818, 0.3333333333333329818, 0.3333333333333329818, 0.3333333333333329818, 0.3333333333333329818),
 ( 1.000000000000000000, 1.000000000000000000, 1.000000000000000000, 1.000000000000000000, 1.000000000000000000, 1.000000000000000000, 1.000000000000000000) ) ) 
 REPRESENTATION_ITEM ( '' )  SURFACE ( )  );
#14579=CARTESIAN_POINT ( 'NONE',  ( 1.145304265383909836, -2.522460978720529656, 6.755972720436079548 ) ) ;
#14583=CARTESIAN_POINT ( 'NONE',  ( 1.673492459604400961, -2.103271789531340641, 3.510746103527379702 ) ) ;
#14587=CARTESIAN_POINT ( 'NONE',  ( 2.408279507600870950, -0.7991276453871939411, 5.815035204050346351 ) ) ;
#14592=CARTESIAN_POINT ( 'NONE',  ( 1.851400890972779045, -5.113135593220339281, 6.601359968904126241 ) ) ;
#14599=CARTESIAN_POINT ( 'NONE',  ( -1.597383073937548970, -2.006277760018210898, 2.580688553303291943 ) ) ;
#14601=CARTESIAN_POINT ( 'NONE',  ( 0.009452110982655408111, -0.3001920447045370310, 2.350000000000000089 ) ) ;
#14603=CARTESIAN_POINT ( 'NONE',  ( -2.169623098572329933, -2.941650167909710234, 5.611855963201049846 ) ) ;
#14604=CARTESIAN_POINT ( 'NONE',  ( 1.536215498768950027, -5.033893599512579975, 2.912754292501710474 ) ) ;
#14605=CARTESIAN_POINT ( 'NONE',  ( 0.3162622016569809347, -1.354205687946139491, 7.334974746141788238 ) ) ;
#14608=CARTESIAN_POINT ( 'NONE',  ( 2.291237445532070094, -0.9350164987569499209, 4.162434510291790346 ) ) ;
#14610=CARTESIAN_POINT ( 'NONE',  ( 2.088297318559229954, -0.3978813559322040283, 5.785136623276629919 ) ) ;
#14620=CARTESIAN_POINT ( 'NONE',  ( -0.2023972492402590084, -2.146007489747939978, 2.355265251465770149 ) ) ;
#14623=CARTESIAN_POINT ( 'NONE',  ( -1.003115764947269950, -1.493935417675869903, 6.828967930617589666 ) ) ;
#14624=CARTESIAN_POINT ( 'NONE',  ( 0.1768565782245979934, -3.752899381639830168, 2.353200596935780098 ) ) ;
#14625=CARTESIAN_POINT ( 'NONE',  ( -1.872456193198849705, -4.501965483225034426, 5.541908336566010007 ) ) ;
#14629=CARTESIAN_POINT ( 'NONE',  ( 1.965557623688110933, -0.08898305084745804228, 5.292675575926325315 ) ) ;
#14630=CARTESIAN_POINT ( 'NONE',  ( -2.334032080503389839, -3.310421904162350160, 5.001728246382240783 ) ) ;
#14635=CARTESIAN_POINT ( 'NONE',  ( -0.6673090596498668647, -3.360839357098899693, 2.443133963569591671 ) ) ;
#14638=CARTESIAN_POINT ( 'NONE',  ( -0.9002849211310044453, -5.166525423728809407, 7.196465912290821443 ) ) ;
#14644=CARTESIAN_POINT ( 'NONE',  ( 0.8893259633308030487, -3.846052534792983923, 2.849594321892129134 ) ) ;
#14646=CARTESIAN_POINT ( 'NONE',  ( -2.586172839791708533, -0.5358050847457624943, 4.104546363490954697 ) ) ;
#14649=CARTESIAN_POINT ( 'NONE',  ( -2.353194804772640314, -5.524364406779660008, 4.731327187377240229 ) ) ;
#14656=CARTESIAN_POINT ( 'NONE',  ( 0.2041457401074358857, -4.498124606865046893, 7.346023093209487875 ) ) ;
#14658=CARTESIAN_POINT ( 'NONE',  ( -2.352760675243210198, -3.034803321062869763, 4.757121734156080528 ) ) ;
#14661=CARTESIAN_POINT ( 'NONE',  ( 1.842787987253230897, -3.710163681423226389, 3.794994874786191907 ) ) ;
#14664=CARTESIAN_POINT ( 'NONE',  ( -1.912899118714301183, -1.381334852594401363, 5.445465495009755408 ) ) ;
#14665=VERTEX_POINT ( 'NONE', #5353 ) ;
#14667=CARTESIAN_POINT ( 'NONE',  ( 1.882879255550339082, -0.4963798976394455664, 2.835213315261639000 ) ) ;
#14669=CARTESIAN_POINT ( 'NONE',  ( -1.914021115237000137, -4.754295778036220277, 6.069404563272239983 ) ) ;
#14673=CARTESIAN_POINT ( 'NONE',  ( -2.270487904532170198, -5.237711864406779938, 4.080813552109679776 ) ) ;
#14680=CARTESIAN_POINT ( 'NONE',  ( 0.5637478356992829953, -0.6606104644819250638, 2.398845082743519708 ) ) ;
#14683=B_SPLINE_CURVE_WITH_KNOTS ( 'NONE', 3,
 ( #3628, #7802, #6597, #5118, #13269, #4828, #9278, #10575, #10478, #16229, #14939, #3536, #12067, #7899, #17687, #10678, #866, #16876, #16608, #5313, #18137, #13999, #9563, #4184, #3996, #15497, #12524, #9843, #1144, #5399, #8366, #6964, #13918, #8277, #3908, #35, #4095, #2806, #15222, #1052, #9750, #1234, #6877, #15135, #2447, #13821, #2527, #8176, #15416, #8093, #2721, #13733, #6688, #9650, #1317, #10864, #12346, #17968, #10960, #11127, #16512, #14084 ),
 .UNSPECIFIED., .F., .F.,
 ( 4, 1, 1, 1, 1, 1, 1, 1, 1, 1, 1, 1, 1, 1, 1, 1, 1, 1, 1, 1, 1, 1, 1, 1, 1, 1, 1, 1, 1, 1, 1, 1, 1, 1, 1, 1, 1, 1, 1, 1, 1, 1, 1, 1, 1, 1, 1, 1, 1, 1, 1, 1, 1, 1, 1, 1, 1, 1, 1, 4 ),
 ( 0.000000000000000000, 0.09318283294546000906, 0.1863656658909200181, 0.2795484988363799994, 0.3727313317818400362, 0.4659141647272999620, 0.5590969976727599988, 0.6522798306182200356, 0.7454626635636800724, 0.8386454965091399982, 0.9318283294545990358, 1.025011162400059961, 1.118193995345519998, 1.211376828290979812, 1.304559661236440071, 1.397742494181900108, 1.490925327127360145, 1.584108160072819960, 1.677290993018279996, 1.770473825963740033, 1.863656658909199848, 1.956839491854659885, 2.050022324800119922, 2.143205157745580181, 2.236387990691039995, 2.329570823636499810, 2.422753656581960069, 2.515936489527420328, 2.609119322472880143, 2.702302155418339957, 2.795484988363799772, 2.888667821309260031, 2.981850654254720290, 3.075033487200179660, 3.168216320145639919, 3.261399153091099734, 3.354581986036559993, 3.447764818982019808, 3.540947651927480067, 3.634130484872939437, 3.727313317818399696, 3.820496150763859955, 3.913678983709319770, 4.006861816654780029, 4.100044649600239843, 4.193227482545699658, 4.286410315491160361, 4.379593148436620176, 4.472775981382079991, 4.565958814327539805, 4.659141647272999620, 4.752324480218450553, 4.845507313163910368, 4.938690146109370183, 5.031872979054829997, 5.125055812000289812, 5.218238644945749627, 5.311421477891210330, 5.404604310836670145, 5.497787143782139729 ),
 .UNSPECIFIED. ) ;
#14686=CARTESIAN_POINT ( 'NONE',  ( -0.6015868932279860859, -3.007674156414608557, 7.284803068494427158 ) ) ;
#14690=CARTESIAN_POINT ( 'NONE',  ( -2.226511124464849889, -4.525253771513310319, 5.462491901673850236 ) ) ;
#14692=CARTESIAN_POINT ( 'NONE',  ( 0.8534102632286154622, -5.320452325212860600, 2.829778315381550780 ) ) ;
#14693=CARTESIAN_POINT ( 'NONE',  ( -1.820241257191459905, -5.080331814072259533, 3.208199930689799917 ) ) ;
#14697=CARTESIAN_POINT ( 'NONE',  ( -1.661700935788390288, -0.2625000000000000111, 3.038299064211610112 ) ) ;
#14698=CARTESIAN_POINT ( 'NONE',  ( 2.508228811380011081, -5.390889830508485581, 5.566973598334535644 ) ) ;
#14708=CARTESIAN_POINT ( 'NONE',  ( -0.09706517602693919000, -2.961097579838030125, 7.051451474958980725 ) ) ;
#14713=CARTESIAN_POINT ( 'NONE',  ( 0.4985810152601650724, -1.330917399657850053, 7.000035360316460675 ) ) ;
#14714=CARTESIAN_POINT ( 'NONE',  ( -0.8934014991059870958, -4.614566048306490309, 6.877287176483410924 ) ) ;
#14716=CARTESIAN_POINT ( 'NONE',  ( -2.050563521385710075, -4.595118636378185073, 4.800454404529219232 ) ) ;
#14725=CARTESIAN_POINT ( 'NONE',  ( -2.034805890357269220, -0.2313559322033900412, 4.427518626519226785 ) ) ;
#14726=CARTESIAN_POINT ( 'NONE',  ( -0.04278372834682089842, -3.729611093351540063, 2.346934926511239805 ) ) ;
#14734=CARTESIAN_POINT ( 'NONE',  ( -1.800129581279449775, -5.264406779661021218, 2.750028594811118943 ) ) ;
#14743=CARTESIAN_POINT ( 'NONE',  ( -1.777111910197670008, -3.473439922180372452, 3.672004328189223621 ) ) ;
#14744=CARTESIAN_POINT ( 'NONE',  ( 2.087380238839969593, -0.1067796610169500227, 6.338810156469096846 ) ) ;
#14746=CARTESIAN_POINT ( 'NONE',  ( 1.248294325655350034, -0.3266949152542379942, 2.704938983774300088 ) ) ;
#14748=CARTESIAN_POINT ( 'NONE',  ( -2.625437065641401446, -0.5180084745762725262, 5.087214675345155257 ) ) ;
#14750=CARTESIAN_POINT ( 'NONE',  ( -1.428515267734880023, -5.568855932203390147, 2.829745655876930055 ) ) ;
#14751=CARTESIAN_POINT ( 'NONE',  ( 2.352190863465239978, -0.6826862039457533005, 4.622903765856330338 ) ) ;
#14752=CARTESIAN_POINT ( 'NONE',  ( -0.009452110982655715157, -0.5998079552954631577, 2.050000000000001155 ) ) ;
#14754=CARTESIAN_POINT ( 'NONE',  ( -2.652303127816829864, -3.333710192450643373, 4.791661394135809715 ) ) ;
#14758=CARTESIAN_POINT ( 'NONE',  ( -0.8748826269293140667, -3.337551068810609589, 2.515205712983220376 ) ) ;
#14761=CARTESIAN_POINT ( 'NONE',  ( -0.9361665894546699063, -3.314262780522333696, 2.872845392579789880 ) ) ;
#14764=CARTESIAN_POINT ( 'NONE',  ( -1.632144308286139989, -1.311469987729540376, 5.945394234592896510 ) ) ;
#14767=CARTESIAN_POINT ( 'NONE',  ( 1.526064881623949931, -0.7763906680874419486, 2.903976516638540062 ) ) ;
#14768=CARTESIAN_POINT ( 'NONE',  ( 1.008962495263989956, -0.9854339516935015642, 7.154609617872576877 ) ) ;
#14774=CARTESIAN_POINT ( 'NONE',  ( 1.449568901432419343, -5.037500000000000533, 3.250431098567584165 ) ) ;
#14781=CARTESIAN_POINT ( 'NONE',  ( 0.9490039995898825742, -3.523857375116919322, 2.221592224478729172 ) ) ;
#14783=CARTESIAN_POINT ( 'NONE',  ( -0.3578984759183553854, -2.984385868126320673, 7.329643012642057087 ) ) ;
#14788=CARTESIAN_POINT ( 'NONE',  ( 1.236334101859160040, -3.570433951693499974, 2.697445712080689617 ) ) ;
#14792=CARTESIAN_POINT ( 'NONE',  ( 2.339254516529669647, -2.681638120378568857, 5.953396186326336270 ) ) ;
#14798=( BOUNDED_SURFACE ( )  B_SPLINE_SURFACE ( 3, 3, ( 
 ( #14034, #15353, #12652, #13758, #2657, #5620, #11264, #16548, #3856, #9875, #15534, #8122, #1080, #6725, #16638, #5346, #3939, #146, #15629, #1544, #9964, #11355, #4302, #7193, #2937, #8578, #14226, #12832, #16989, #3780, #3591, #723, #5078, #6648, #9327, #10438, #2211, #6272, #6358, #6465, #922, #12216, #13410, #631, #13609, #6561, #14996, #4879, #9439, #12302, #17832, #9143, #16465, #5166, #12128, #7673, #3498, #12023, #4983, #15102, #2412, #13506 ),
 ( #17925, #9236, #11931, #16100, #17644, #2114, #10637, #3396, #8059, #16190, #10729, #14804, #9040, #14698, #16375, #13701, #1012, #7765, #13314, #14899, #7855, #3961, #9611, #18103, #6747, #12399, #8500, #18018, #5637, #5365, #9890, #11006, #6841, #15273, #15549, #15371, #1098, #13877, #2577, #10923, #11280, #4142, #16732, #2853, #1192, #4230, #12485, #5450, #15186, #2494, #5539, #5270, #11090, #16832, #12766, #4049, #9704, #8143, #9800, #14150, #16568, #4411 ),
 ( #2674, #3875, #1471, #15460, #8326, #7131, #13962, #13777, #1282, #6925, #12572, #2768, #18185, #8413, #14048, #1364, #7025, #12672, #14592, #7291, #4684, #2956, #15903, #12848, #4319, #7391, #12937, #10154, #15649, #266, #11457, #10233, #1908, #16001, #3212, #4498, #5990, #8862, #7555, #162, #8596, #1741, #79, #5904, #4576, #15730, #5724, #14244, #14510, #1561, #3036, #8675, #14416, #14324, #11722, #11545, #1644, #13028, #11370, #11630, #17003, #15808 ),
 ( #9984, #3304, #7206, #1831, #7474, #17178, #17092, #10078, #5808, #351, #13122, #434, #3114, #4419, #6074, #17355, #8766, #8947, #17807, #521, #13295, #17721, #2388, #13201, #5053, #16350, #13478, #3467, #3563, #11827, #6170, #14874, #1992, #17450, #4768, #16164, #4858, #614, #6432, #10420, #12101, #16081, #3378, #6335, #3654, #9022, #14673, #7739, #10705, #9304, #16260, #10608, #6252, #7650, #15077, #11999, #11910, #17530, #9117, #10504, #13385, #9411 ),
 ( #14774, #2088, #14971, #699, #2283, #17616, #4954, #9210, #7936, #2188, #7831, #794, #13584, #899, #6535, #12191, #5144, #10795, #16441, #3749, #10896, #12554, #8394, #15531, #2749, #15349, #14031, #1172, #4122, #986, #8034, #6906, #1345, #8206, #12646, #11261, #18271, #6722, #5617, #13944, #11067, #13674, #6622, #16711, #9871, #16903, #18083, #2553, #2654, #4024, #5241, #4210, #13853, #12280, #12375, #9678, #1261, #6998, #8307, #17901, #1077, #16545 ),
 ( #16809, #18163, #16635, #3853, #9781, #15442, #9506, #17997, #15161, #3935, #2472, #5343, #10987, #8118, #6820, #5514, #11160, #13755, #9589, #15249, #12465, #5430, #11527, #7457, #6053, #8479, #144, #12746, #414, #9961, #7371, #11610, #5791, #14224, #12830, #4661, #10134, #5968, #4558, #1628, #15625, #17239, #3192, #2933, #14121, #15880, #1542, #8844, #14491, #4478, #61, #7190, #11435, #15710, #333, #1815, #5884, #243, #17072, #10318, #2832, #14308 ),
 ( #1447, #15791, #8574, #7107, #5707, #4399, #10054, #3017, #14392, #11352, #13011, #16985, #4299, #12916, #13098, #8658, #17157, #3099, #8744, #11700, #17332, #17512, #16234, #5121, #3439, #4836, #495, #2165, #16326, #15979, #10682, #4922, #3631, #9088, #12072, #14572, #3285, #14851, #9282, #16138, #2253, #870, #7905, #14649, #13556, #9188, #674, #1886, #7533, #6314, #17785, #6509, #7719, #14750, #10579, #11977, #13177, #12168, #2063, #6145, #1966, #17588 ) ),
 .UNSPECIFIED., .T., .F., .F. ) 
 B_SPLINE_SURFACE_WITH_KNOTS ( ( 4, 3, 4 ),
 ( 4, 1, 1, 1, 1, 1, 1, 1, 1, 1, 1, 1, 1, 1, 1, 1, 1, 1, 1, 1, 1, 1, 1, 1, 1, 1, 1, 1, 1, 1, 1, 1, 1, 1, 1, 1, 1, 1, 1, 1, 1, 1, 1, 1, 1, 1, 1, 1, 1, 1, 1, 1, 1, 1, 1, 1, 1, 1, 1, 4 ),
 ( 0.000000000000000000, 3.141592653589790007, 6.283185307179590673 ),
 ( 0.7853981633974479459, 0.8785809963429079827, 0.9717638292883680196, 1.064946662233830166, 1.158129495179289981, 1.251312328124750017, 1.344495161070210054, 1.437677994015669869, 1.530860826961130128, 1.624043659906589943, 1.717226492852049979, 1.810409325797510016, 1.903592158742969831, 1.996774991688430090, 2.089957824633889683, 2.183140657579349941, 2.276323490524809756, 2.369506323470270015, 2.462689156415730274, 2.555871989361190089, 2.649054822306649903, 2.742237655252109718, 2.835420488197569977, 2.928603321143030236, 3.021786154088490051, 3.114968987033949865, 3.208151819979410124, 3.301334652924869939, 3.394517485870330198, 3.487700318815790013, 3.580883151761249827, 3.674065984706710086, 3.767248817652169901, 3.860431650597620390, 3.953614483543080205, 4.046797316488540019, 4.139980149433999834, 4.233162982379460537, 4.326345815324920352, 4.419528648270380167, 4.512711481215839981, 4.605894314161299796, 4.699077147106759611, 4.792259980052219426, 4.885442812997680129, 4.978625645943139943, 5.071808478888599758, 5.164991311834059573, 5.258174144779520276, 5.351356977724980091, 5.444539810670439905, 5.537722643615899720, 5.630905476561360423, 5.724088309506820238, 5.817271142452280053, 5.910453975397739868, 6.003636808343199682, 6.096819641288659497, 6.190002474234119312, 6.283185307179590673 ),
 .UNSPECIFIED. ) 
 GEOMETRIC_REPRESENTATION_ITEM ( )  RATIONAL_B_SPLINE_SURFACE ( (
 ( 1.000000000000000000, 1.000000000000000000, 1.000000000000000000, 1.000000000000000000, 1.000000000000000000, 1.000000000000000000, 1.000000000000000000, 1.000000000000000000, 1.000000000000000000, 1.000000000000000000, 1.000000000000000000, 1.000000000000000000, 1.000000000000000000, 1.000000000000000000, 1.000000000000000000, 1.000000000000000000, 1.000000000000000000, 1.000000000000000000, 1.000000000000000000, 1.000000000000000000, 1.000000000000000000, 1.000000000000000000, 1.000000000000000000, 1.000000000000000000, 1.000000000000000000, 1.000000000000000000, 1.000000000000000000, 1.000000000000000000, 1.000000000000000000, 1.000000000000000000, 1.000000000000000000, 1.000000000000000000, 1.000000000000000000, 1.000000000000000000, 1.000000000000000000, 1.000000000000000000, 1.000000000000000000, 1.000000000000000000, 1.000000000000000000, 1.000000000000000000, 1.000000000000000000, 1.000000000000000000, 1.000000000000000000, 1.000000000000000000, 1.000000000000000000, 1.000000000000000000, 1.000000000000000000, 1.000000000000000000, 1.000000000000000000, 1.000000000000000000, 1.000000000000000000, 1.000000000000000000, 1.000000000000000000, 1.000000000000000000, 1.000000000000000000, 1.000000000000000000, 1.000000000000000000, 1.000000000000000000, 1.000000000000000000, 1.000000000000000000, 1.000000000000000000, 1.000000000000000000),
 ( 0.3333333333333329818, 0.3333333333333329818, 0.3333333333333329818, 0.3333333333333329818, 0.3333333333333329818, 0.3333333333333329818, 0.3333333333333329818, 0.3333333333333329818, 0.3333333333333329818, 0.3333333333333329818, 0.3333333333333329818, 0.3333333333333329818, 0.3333333333333329818, 0.3333333333333329818, 0.3333333333333329818, 0.3333333333333329818, 0.3333333333333329818, 0.3333333333333329818, 0.3333333333333329818, 0.3333333333333329818, 0.3333333333333329818, 0.3333333333333329818, 0.3333333333333329818, 0.3333333333333329818, 0.3333333333333329818, 0.3333333333333329818, 0.3333333333333329818, 0.3333333333333329818, 0.3333333333333329818, 0.3333333333333329818, 0.3333333333333329818, 0.3333333333333329818, 0.3333333333333329818, 0.3333333333333329818, 0.3333333333333329818, 0.3333333333333329818, 0.3333333333333329818, 0.3333333333333329818, 0.3333333333333329818, 0.3333333333333329818, 0.3333333333333329818, 0.3333333333333329818, 0.3333333333333329818, 0.3333333333333329818, 0.3333333333333329818, 0.3333333333333329818, 0.3333333333333329818, 0.3333333333333329818, 0.3333333333333329818, 0.3333333333333329818, 0.3333333333333329818, 0.3333333333333329818, 0.3333333333333329818, 0.3333333333333329818, 0.3333333333333329818, 0.3333333333333329818, 0.3333333333333329818, 0.3333333333333329818, 0.3333333333333329818, 0.3333333333333329818, 0.3333333333333329818, 0.3333333333333329818),
 ( 0.3333333333333329818, 0.3333333333333329818, 0.3333333333333329818, 0.3333333333333329818, 0.3333333333333329818, 0.3333333333333329818, 0.3333333333333329818, 0.3333333333333329818, 0.3333333333333329818, 0.3333333333333329818, 0.3333333333333329818, 0.3333333333333329818, 0.3333333333333329818, 0.3333333333333329818, 0.3333333333333329818, 0.3333333333333329818, 0.3333333333333329818, 0.3333333333333329818, 0.3333333333333329818, 0.3333333333333329818, 0.3333333333333329818, 0.3333333333333329818, 0.3333333333333329818, 0.3333333333333329818, 0.3333333333333329818, 0.3333333333333329818, 0.3333333333333329818, 0.3333333333333329818, 0.3333333333333329818, 0.3333333333333329818, 0.3333333333333329818, 0.3333333333333329818, 0.3333333333333329818, 0.3333333333333329818, 0.3333333333333329818, 0.3333333333333329818, 0.3333333333333329818, 0.3333333333333329818, 0.3333333333333329818, 0.3333333333333329818, 0.3333333333333329818, 0.3333333333333329818, 0.3333333333333329818, 0.3333333333333329818, 0.3333333333333329818, 0.3333333333333329818, 0.3333333333333329818, 0.3333333333333329818, 0.3333333333333329818, 0.3333333333333329818, 0.3333333333333329818, 0.3333333333333329818, 0.3333333333333329818, 0.3333333333333329818, 0.3333333333333329818, 0.3333333333333329818, 0.3333333333333329818, 0.3333333333333329818, 0.3333333333333329818, 0.3333333333333329818, 0.3333333333333329818, 0.3333333333333329818),
 ( 1.000000000000000000, 1.000000000000000000, 1.000000000000000000, 1.000000000000000000, 1.000000000000000000, 1.000000000000000000, 1.000000000000000000, 1.000000000000000000, 1.000000000000000000, 1.000000000000000000, 1.000000000000000000, 1.000000000000000000, 1.000000000000000000, 1.000000000000000000, 1.000000000000000000, 1.000000000000000000, 1.000000000000000000, 1.000000000000000000, 1.000000000000000000, 1.000000000000000000, 1.000000000000000000, 1.000000000000000000, 1.000000000000000000, 1.000000000000000000, 1.000000000000000000, 1.000000000000000000, 1.000000000000000000, 1.000000000000000000, 1.000000000000000000, 1.000000000000000000, 1.000000000000000000, 1.000000000000000000, 1.000000000000000000, 1.000000000000000000, 1.000000000000000000, 1.000000000000000000, 1.000000000000000000, 1.000000000000000000, 1.000000000000000000, 1.000000000000000000, 1.000000000000000000, 1.000000000000000000, 1.000000000000000000, 1.000000000000000000, 1.000000000000000000, 1.000000000000000000, 1.000000000000000000, 1.000000000000000000, 1.000000000000000000, 1.000000000000000000, 1.000000000000000000, 1.000000000000000000, 1.000000000000000000, 1.000000000000000000, 1.000000000000000000, 1.000000000000000000, 1.000000000000000000, 1.000000000000000000, 1.000000000000000000, 1.000000000000000000, 1.000000000000000000, 1.000000000000000000),
 ( 0.3333333333333329818, 0.3333333333333329818, 0.3333333333333329818, 0.3333333333333329818, 0.3333333333333329818, 0.3333333333333329818, 0.3333333333333329818, 0.3333333333333329818, 0.3333333333333329818, 0.3333333333333329818, 0.3333333333333329818, 0.3333333333333329818, 0.3333333333333329818, 0.3333333333333329818, 0.3333333333333329818, 0.3333333333333329818, 0.3333333333333329818, 0.3333333333333329818, 0.3333333333333329818, 0.3333333333333329818, 0.3333333333333329818, 0.3333333333333329818, 0.3333333333333329818, 0.3333333333333329818, 0.3333333333333329818, 0.3333333333333329818, 0.3333333333333329818, 0.3333333333333329818, 0.3333333333333329818, 0.3333333333333329818, 0.3333333333333329818, 0.3333333333333329818, 0.3333333333333329818, 0.3333333333333329818, 0.3333333333333329818, 0.3333333333333329818, 0.3333333333333329818, 0.3333333333333329818, 0.3333333333333329818, 0.3333333333333329818, 0.3333333333333329818, 0.3333333333333329818, 0.3333333333333329818, 0.3333333333333329818, 0.3333333333333329818, 0.3333333333333329818, 0.3333333333333329818, 0.3333333333333329818, 0.3333333333333329818, 0.3333333333333329818, 0.3333333333333329818, 0.3333333333333329818, 0.3333333333333329818, 0.3333333333333329818, 0.3333333333333329818, 0.3333333333333329818, 0.3333333333333329818, 0.3333333333333329818, 0.3333333333333329818, 0.3333333333333329818, 0.3333333333333329818, 0.3333333333333329818),
 ( 0.3333333333333329818, 0.3333333333333329818, 0.3333333333333329818, 0.3333333333333329818, 0.3333333333333329818, 0.3333333333333329818, 0.3333333333333329818, 0.3333333333333329818, 0.3333333333333329818, 0.3333333333333329818, 0.3333333333333329818, 0.3333333333333329818, 0.3333333333333329818, 0.3333333333333329818, 0.3333333333333329818, 0.3333333333333329818, 0.3333333333333329818, 0.3333333333333329818, 0.3333333333333329818, 0.3333333333333329818, 0.3333333333333329818, 0.3333333333333329818, 0.3333333333333329818, 0.3333333333333329818, 0.3333333333333329818, 0.3333333333333329818, 0.3333333333333329818, 0.3333333333333329818, 0.3333333333333329818, 0.3333333333333329818, 0.3333333333333329818, 0.3333333333333329818, 0.3333333333333329818, 0.3333333333333329818, 0.3333333333333329818, 0.3333333333333329818, 0.3333333333333329818, 0.3333333333333329818, 0.3333333333333329818, 0.3333333333333329818, 0.3333333333333329818, 0.3333333333333329818, 0.3333333333333329818, 0.3333333333333329818, 0.3333333333333329818, 0.3333333333333329818, 0.3333333333333329818, 0.3333333333333329818, 0.3333333333333329818, 0.3333333333333329818, 0.3333333333333329818, 0.3333333333333329818, 0.3333333333333329818, 0.3333333333333329818, 0.3333333333333329818, 0.3333333333333329818, 0.3333333333333329818, 0.3333333333333329818, 0.3333333333333329818, 0.3333333333333329818, 0.3333333333333329818, 0.3333333333333329818),
 ( 1.000000000000000000, 1.000000000000000000, 1.000000000000000000, 1.000000000000000000, 1.000000000000000000, 1.000000000000000000, 1.000000000000000000, 1.000000000000000000, 1.000000000000000000, 1.000000000000000000, 1.000000000000000000, 1.000000000000000000, 1.000000000000000000, 1.000000000000000000, 1.000000000000000000, 1.000000000000000000, 1.000000000000000000, 1.000000000000000000, 1.000000000000000000, 1.000000000000000000, 1.000000000000000000, 1.000000000000000000, 1.000000000000000000, 1.000000000000000000, 1.000000000000000000, 1.000000000000000000, 1.000000000000000000, 1.000000000000000000, 1.000000000000000000, 1.000000000000000000, 1.000000000000000000, 1.000000000000000000, 1.000000000000000000, 1.000000000000000000, 1.000000000000000000, 1.000000000000000000, 1.000000000000000000, 1.000000000000000000, 1.000000000000000000, 1.000000000000000000, 1.000000000000000000, 1.000000000000000000, 1.000000000000000000, 1.000000000000000000, 1.000000000000000000, 1.000000000000000000, 1.000000000000000000, 1.000000000000000000, 1.000000000000000000, 1.000000000000000000, 1.000000000000000000, 1.000000000000000000, 1.000000000000000000, 1.000000000000000000, 1.000000000000000000, 1.000000000000000000, 1.000000000000000000, 1.000000000000000000, 1.000000000000000000, 1.000000000000000000, 1.000000000000000000, 1.000000000000000000) ) ) 
 REPRESENTATION_ITEM ( '' )  SURFACE ( )  );
#14801=CARTESIAN_POINT ( 'NONE',  ( 1.644832646965660006, -1.191187669928119863, 6.383232381746459794 ) ) ;
#14802=CARTESIAN_POINT ( 'NONE',  ( 1.378221871957440170, -0.4201271186440679872, 6.607619368096269596 ) ) ;
#14804=CARTESIAN_POINT ( 'NONE',  ( 2.625437065641401446, -5.381991525423726053, 5.087214675345139270 ) ) ;
#14813=CARTESIAN_POINT ( 'NONE',  ( -1.881914957835490121, -1.936412895153350133, 3.286797332666350435 ) ) ;
#14818=CARTESIAN_POINT ( 'NONE',  ( -2.316639661709700260, -1.819971453711900056, 4.285359956977770501 ) ) ;
#14819=CARTESIAN_POINT ( 'NONE',  ( -1.097561405233230092, -3.613169651910099756, 2.618148744692269769 ) ) ;
#14820=CARTESIAN_POINT ( 'NONE',  ( 1.658519201881180738, -2.402178660919109365, 3.489952108543023623 ) ) ;
#14821=CARTESIAN_POINT ( 'NONE',  ( 0.6964468257805941365, -0.1334745762711869732, 6.631228347243847132 ) ) ;
#14823=CARTESIAN_POINT ( 'NONE',  ( 1.438959988998139914E-16, -0.2999999999999999889, 2.350000000000000089 ) ) ;
#14826=CARTESIAN_POINT ( 'NONE',  ( 1.564316099353070033, -5.123660385842499387, 3.135683900646930145 ) ) ;
#14828=CARTESIAN_POINT ( 'NONE',  ( -2.295719155670160383, -3.287133615874060055, 5.218091927917240191 ) ) ;
#14835=CARTESIAN_POINT ( 'NONE',  ( -2.203023580853999963, -5.242161016949149932, 3.872235369154300333 ) ) ;
#14838=CARTESIAN_POINT ( 'NONE',  ( -1.811729841638700211, -0.5580508474576270084, 3.197954009834299782 ) ) ;
#14843=CARTESIAN_POINT ( 'NONE',  ( 1.508881462028659692, -4.311818300558746486, 6.092184821126257255 ) ) ;
#14844=CARTESIAN_POINT ( 'NONE',  ( 0.9002849211310119948, -0.1334745762711869732, 7.196465912290821443 ) ) ;
#14846=CARTESIAN_POINT ( 'NONE',  ( 1.750316316486830059, -0.3400423728813560253, 3.126818518378580158 ) ) ;
#14847=VERTEX_POINT ( 'NONE', #7541 ) ;
#14848=CARTESIAN_POINT ( 'NONE',  ( -1.254903241568450900, -0.4735169491525429986, 7.038391080368498365 ) ) ;
#14851=CARTESIAN_POINT ( 'NONE',  ( -1.978267656359410154, -5.497669491525420504, 5.974740860598790171 ) ) ;
#14853=CARTESIAN_POINT ( 'NONE',  ( 2.159308672244681482, -0.8457042219637719294, 6.242886823772496818 ) ) ;
#14855=CARTESIAN_POINT ( 'NONE',  ( -0.3865907654992132292, -4.952022267818764867, 2.675656795012148592 ) ) ;
#14857=CARTESIAN_POINT ( 'NONE',  ( -0.1226612266410539998, -2.662190708450249854, 7.050255286338659388 ) ) ;
#14861=CARTESIAN_POINT ( 'NONE',  ( -0.2475374578675481607, -4.245794312053864594, 6.738044908627027318 ) ) ;
#14864=CARTESIAN_POINT ( 'NONE',  ( -1.831349212334698828, -1.590929447188999646, 3.772065786216939554 ) ) ;
#14867=CARTESIAN_POINT ( 'NONE',  ( 1.495970331552388455, -0.4480353997208171291, 2.495424373718078570 ) ) ;
#14868=CARTESIAN_POINT ( 'NONE',  ( 1.700860513939579599, -2.475884402143949892, 6.737200825918507441 ) ) ;
#14874=CARTESIAN_POINT ( 'NONE',  ( -1.000896394980330006, -5.170974576271190948, 6.829956240957379521 ) ) ;
#14881=CARTESIAN_POINT ( 'NONE',  ( 2.050059171113549183, -5.377542372881360500, 4.809263467226075228 ) ) ;
#14882=CARTESIAN_POINT ( 'NONE',  ( -0.5134687485629449988, -3.384127645387192018, 2.096259702418250104 ) ) ;
#14884=CARTESIAN_POINT ( 'NONE',  ( 0.1366863161731129428, -2.937809291549738688, 7.350364228549148393 ) ) ;
#14888=CARTESIAN_POINT ( 'NONE',  ( 2.111627294540149968, -3.710163681423230386, 3.660877362176659933 ) ) ;
#14891=CARTESIAN_POINT ( 'NONE',  ( -1.292937800126279679, -3.077539021279473097, 7.017633607369056392 ) ) ;
#14896=CARTESIAN_POINT ( 'NONE',  ( 0.8748826269292639957, -2.262448931189380286, 2.515205712983200392 ) ) ;
#14897=CARTESIAN_POINT ( 'NONE',  ( -1.925796468768790071, -0.4957627118644070130, 6.052706598917719560 ) ) ;
#14899=CARTESIAN_POINT ( 'NONE',  ( 1.666450993087180477, -5.417584745762705545, 6.765380371283858274 ) ) ;
#14903=CARTESIAN_POINT ( 'NONE',  ( 2.043308330018789309, -5.099788135593219529, 5.867646457774661428 ) ) ;
#14910=CARTESIAN_POINT ( 'NONE',  ( 0.8748826269292639957, -2.262448931189380286, 2.515205712983200392 ) ) ;
#14911=CARTESIAN_POINT ( 'NONE',  ( -1.000896394980330006, -5.470974576271190770, 6.829956240957379521 ) ) ;
#14913=CARTESIAN_POINT ( 'NONE',  ( 0.01716182025089369942, -2.169295778036230082, 2.346608583467340026 ) ) ;
#14914=CARTESIAN_POINT ( 'NONE',  ( -1.460675875430050175, -4.684430913171359734, 6.545310725710059785 ) ) ;
#14915=CARTESIAN_POINT ( 'NONE',  ( 2.007801995112640903, -2.611773255513701653, 5.128524201241654978 ) ) ;
#14919=CARTESIAN_POINT ( 'NONE',  ( 1.618511124886439889, -5.326166231000110329, 3.081488875113560066 ) ) ;
#14922=CARTESIAN_POINT ( 'NONE',  ( -2.159566522375440112, -3.240557039297490061, 5.635424033751089468 ) ) ;
#14929=CARTESIAN_POINT ( 'NONE',  ( -2.291237445532080308, -4.664983501243040287, 4.162434510291850742 ) ) ;
#14931=CARTESIAN_POINT ( 'NONE',  ( 2.293398556041700065, -5.064194915254240037, 4.171956209133470317 ) ) ;
#14934=CARTESIAN_POINT ( 'NONE',  ( -1.994983296312370147, -1.334758276017820045, 5.948514050749340143 ) ) ;
#14936=CARTESIAN_POINT ( 'NONE',  ( 1.971820545011360171, -4.055647129387581984, 4.128313389260194199 ) ) ;
#14937=CARTESIAN_POINT ( 'NONE',  ( 0.2189795514005130062, -0.004449152542373159894, 2.356806637999009801 ) ) ;
#14939=CARTESIAN_POINT ( 'NONE',  ( 1.750316316486830059, -0.3400423728813560253, 3.126818518378580158 ) ) ;
#14940=CARTESIAN_POINT ( 'NONE',  ( 2.354888465609351389, -0.09788135593220394226, 5.923664702843856489 ) ) ;
#14945=CARTESIAN_POINT ( 'NONE',  ( 2.218077401483169453, -0.7758393570989060573, 5.486688202856499608 ) ) ;
#14946=CARTESIAN_POINT ( 'NONE',  ( 1.943632316591230147, -5.346398305084740343, 3.373048379518159834 ) ) ;
#14948=CARTESIAN_POINT ( 'NONE',  ( 2.408279507600870950, -0.7991276453871939411, 5.815035204050346351 ) ) ;
#14951=CARTESIAN_POINT ( 'NONE',  ( 1.934380261529039080, -0.7758393570989061683, 5.387804366397126010 ) ) ;
#14952=CARTESIAN_POINT ( 'NONE',  ( -1.648422021521479763, -4.684430913171365063, 6.779860219333237126 ) ) ;
#14955=CARTESIAN_POINT ( 'NONE',  ( -0.9742769543504515850, -4.338947465207014353, 6.507120986223577042 ) ) ;
#14960=CARTESIAN_POINT ( 'NONE',  ( 1.777111910197639810, -2.126560077819629413, 3.672004328189181432 ) ) ;
#14965=CARTESIAN_POINT ( 'NONE',  ( 0.009452110982655428928, -0.3001920447045380858, 2.649999999999998579 ) ) ;
#14966=CARTESIAN_POINT ( 'NONE',  ( -0.9250303514741213817, -1.777235753495299608, 2.212544966868041474 ) ) ;
#14971=CARTESIAN_POINT ( 'NONE',  ( 1.580445181003960586, -5.041949152542365198, 3.389704561770334301 ) ) ;
#14980=CARTESIAN_POINT ( 'NONE',  ( 2.351526912647309953, -5.373093220338979847, 4.606040641882800379 ) ) ;
#14981=CARTESIAN_POINT ( 'NONE',  ( 2.632194480419669080, -2.289578095837640159, 5.038623552414890128 ) ) ;
#14987=CARTESIAN_POINT ( 'NONE',  ( 2.199335452462550133, -3.733451969711520491, 3.862342996790889771 ) ) ;
#14990=CARTESIAN_POINT ( 'NONE',  ( 1.094547058713730037, -2.844656138396588929, 7.117660114503893354 ) ) ;
#14993=CARTESIAN_POINT ( 'NONE',  ( 1.115198193348289957, -1.261052534792989954, 6.772457159276550342 ) ) ;
#14996=CARTESIAN_POINT ( 'NONE',  ( -2.270487904532170198, -5.537711864406779760, 4.080813552109679776 ) ) ;
#14999=CARTESIAN_POINT ( 'NONE',  ( 1.477796163681079689, -5.117584745762709275, 6.531563725478138238 ) ) ;
#15001=CARTESIAN_POINT ( 'NONE',  ( 0.009037091307168881177, -0.3067697551340939910, 2.399753621991609798 ) ) ;
#15006=CARTESIAN_POINT ( 'NONE',  ( 1.866416942370620058, -3.962493976234419790, 3.266391446483460026 ) ) ;
#15007=CARTESIAN_POINT ( 'NONE',  ( -2.345900685764729765, -5.528813559322030002, 4.512231114381339836 ) ) ;
#15010=CARTESIAN_POINT ( 'NONE',  ( 0.9719602541832789155, -2.844656138396589817, 6.843370931913530519 ) ) ;
#15012=CARTESIAN_POINT ( 'NONE',  ( -2.052909741356249373, -1.773394877135329839, 4.721527574705180363 ) ) ;
#15015=CIRCLE ( 'NONE', #12643, 0.1500000000000000777 ) ;
#15016=CARTESIAN_POINT ( 'NONE',  ( -1.685497504775380850, -0.2673043920988010802, 2.637581209070348987 ) ) ;
#15018=CARTESIAN_POINT ( 'NONE',  ( 1.579711282809380002, -5.089528081836459883, 3.120288717190609962 ) ) ;
#15021=CARTESIAN_POINT ( 'NONE',  ( -2.325590009395030133, -4.870737219477670799, 5.061077271074069905 ) ) ;
#15028=CARTESIAN_POINT ( 'NONE',  ( -1.936998685628559258, -4.758136654396199816, 3.363294429306560751 ) ) ;
#15029=CARTESIAN_POINT ( 'NONE',  ( 1.791574935211219799, -5.108686440677970175, 6.226029630577610163 ) ) ;
#15034=CARTESIAN_POINT ( 'NONE',  ( 1.626408692231650077, -0.8922807985403480302, 6.401040991074950171 ) ) ;
#15038=CARTESIAN_POINT ( 'NONE',  ( 0.2818998297622880012, -1.354205687946139935, 7.036509827384409554 ) ) ;
#15042=CARTESIAN_POINT ( 'NONE',  ( 2.088297318559229954, -0.09788135593220401165, 5.785136623276629919 ) ) ;
#15048=CARTESIAN_POINT ( 'NONE',  ( 2.203023580853990193, -0.05783898305084790581, 3.872235369154280349 ) ) ;
#15053=CARTESIAN_POINT ( 'NONE',  ( -0.1824815401349519361, -1.101875393134940317, 7.046368721022736814 ) ) ;
#15054=CARTESIAN_POINT ( 'NONE',  ( -0.8244235255442939891, -0.5829339996946389935, 2.492493020344019872 ) ) ;
#15055=CARTESIAN_POINT ( 'NONE',  ( 0.04351999560419626129, -1.078587104846650213, 7.353529668759038351 ) ) ;
#15059=CARTESIAN_POINT ( 'NONE',  ( 1.552749016687789974, -4.036199717459258984, 6.468535037441730751 ) ) ;
#15060=CARTESIAN_POINT ( 'NONE',  ( 2.370419177058800120, -4.241953435693877061, 5.893409660608535994 ) ) ;
#15064=CARTESIAN_POINT ( 'NONE',  ( -0.2047443300700520219, -3.407415933675483899, 2.657212296411530783 ) ) ;
#15067=CARTESIAN_POINT ( 'NONE',  ( -0.1526488871098711508, -1.847100618360169699, 2.652660223633551251 ) ) ;
#15072=CARTESIAN_POINT ( 'NONE',  ( 0.2451610102875899921, -0.3251990024832500104, 2.350791033861340029 ) ) ;
#15073=CARTESIAN_POINT ( 'NONE',  ( 0.6015868932280445947, -2.592325843585391532, 7.284803068494412948 ) ) ;
#15076=CARTESIAN_POINT ( 'NONE',  ( -1.505092429369619955, -5.128627060139309357, 2.879659483602799774 ) ) ;
#15077=CARTESIAN_POINT ( 'NONE',  ( -1.248294325655370018, -5.273305084745760318, 2.704938983774309857 ) ) ;
#15085=CARTESIAN_POINT ( 'NONE',  ( 0.06264882350516240428, -5.448728813559320372, 7.052569299041220319 ) ) ;
#15086=CARTESIAN_POINT ( 'NONE',  ( 1.752195476665078688, -4.036199717459260761, 6.693219682964302031 ) ) ;
#15087=CARTESIAN_POINT ( 'NONE',  ( 0.2451610102875898256, -0.3251990024832499548, 2.350791033861340029 ) ) ;
#15090=CARTESIAN_POINT ( 'NONE',  ( 1.881914957835459923, -3.663587104846649734, 3.286797332666310023 ) ) ;
#15094=CARTESIAN_POINT ( 'NONE',  ( 1.524497189778211581, -2.798079561820010941, 6.872331008700157007 ) ) ;
#15099=CARTESIAN_POINT ( 'NONE',  ( -1.881914957835490121, -1.936412895153350133, 3.286797332666350435 ) ) ;
#15102=CARTESIAN_POINT ( 'NONE',  ( -0.2189795514005259958, -5.595550847457629651, 2.356806637999020015 ) ) ;
#15103=VERTEX_POINT ( 'NONE', #11984 ) ;
#15106=CARTESIAN_POINT ( 'NONE',  ( -0.009340024727881909850, -0.5980314830687609717, 2.378874508206480165 ) ) ;
#15109=CARTESIAN_POINT ( 'NONE',  ( -2.326448859701059746, -3.380286769027220029, 4.344498395672320434 ) ) ;
#15110=CARTESIAN_POINT ( 'NONE',  ( -1.549742865090599997, -5.484322033898309634, 6.471102547561460305 ) ) ;
#15113=CARTESIAN_POINT ( 'NONE',  ( 2.126557263589630153, -2.448755237495689574, 3.691783806836010040 ) ) ;
#15115=CARTESIAN_POINT ( 'NONE',  ( 0.4365326870214371602, -1.330917399657850497, 6.706076034398976482 ) ) ;
#15126=CARTESIAN_POINT ( 'NONE',  ( 1.661700935788380074, -5.037500000000000533, 3.038299064211610112 ) ) ;
#15130=CARTESIAN_POINT ( 'NONE',  ( -2.651429253058529945, -4.618406924666464519, 4.585822029124955179 ) ) ;
#15132=CARTESIAN_POINT ( 'NONE',  ( -1.503462833636818541, -5.095857339597785973, 3.304888304972901647 ) ) ;
#15133=CARTESIAN_POINT ( 'NONE',  ( 1.057242234132090175, -0.02224576271186469792, 2.597442975781520058 ) ) ;
#15135=CARTESIAN_POINT ( 'NONE',  ( -1.641808337277740115, -0.4868644067796619734, 6.386111670537629514 ) ) ;
#15137=CARTESIAN_POINT ( 'NONE',  ( -2.586172839791708533, -0.2358050847457631438, 4.104546363490954697 ) ) ;
#15140=CARTESIAN_POINT ( 'NONE',  ( 1.722199153441389852, -0.5041426604022090086, 3.099360556065540173 ) ) ;
#15141=CARTESIAN_POINT ( 'NONE',  ( -2.340070819011249803, -5.519915254237290014, 4.950151441910549899 ) ) ;
#15143=CARTESIAN_POINT ( 'NONE',  ( 2.589817782457058737, -0.6361096273691766445, 4.120381550729950604 ) ) ;
#15145=CARTESIAN_POINT ( 'NONE',  ( 0.009452110982653675123, -5.000192044704546035, 2.649999999999998579 ) ) ;
#15147=CARTESIAN_POINT ( 'NONE',  ( 1.886482464143609095, -0.5895330507926000996, 3.890008792968652429 ) ) ;
#15151=CARTESIAN_POINT ( 'NONE',  ( 1.942813984510739056, -1.074746228486680000, 5.363608065214415355 ) ) ;
#15153=ORIENTED_EDGE ( 'NONE', *, *, #14000, .T. ) ;
#15157=CARTESIAN_POINT ( 'NONE',  ( 0.8400312909773258729, -2.569037555297099651, 7.217431453521787610 ) ) ;
#15161=CARTESIAN_POINT ( 'NONE',  ( 2.034805890357269220, -5.368644067796615182, 4.427518626519221456 ) ) ;
#15170=CARTESIAN_POINT ( 'NONE',  ( -2.203023580853999963, -5.542161016949149754, 3.872235369154300333 ) ) ;
#15172=CARTESIAN_POINT ( 'NONE',  ( -0.8001094918299070935, -4.292370888630430592, 7.230402832373842514 ) ) ;
#15173=CARTESIAN_POINT ( 'NONE',  ( 0.9866023595736961305, -5.020626044399128851, 2.560054107758460873 ) ) ;
#15174=CARTESIAN_POINT ( 'NONE',  ( -0.04661003995944364847, -3.729611093351542284, 2.046522810126899294 ) ) ;
#15176=CARTESIAN_POINT ( 'NONE',  ( -1.652654650382400003, -4.804713230972780025, 3.029252778805629820 ) ) ;
#15182=CARTESIAN_POINT ( 'NONE',  ( 2.180207327701309872, -0.3934322033898309812, 5.586116916730190063 ) ) ;
#15183=CARTESIAN_POINT ( 'NONE',  ( 2.023259452208809872, -2.425466949207399914, 3.497849062500220096 ) ) ;
#15184=CARTESIAN_POINT ( 'NONE',  ( -0.008236272907986450995, -5.280537951349149495, 2.272810616177459941 ) ) ;
#15186=CARTESIAN_POINT ( 'NONE',  ( -2.386628511786350160, -5.546610169491530407, 3.539457309197792778 ) ) ;
#15189=CARTESIAN_POINT ( 'NONE',  ( 2.234315482767909700, -5.059745762711858497, 3.960850823455320580 ) ) ;
#15194=CARTESIAN_POINT ( 'NONE',  ( 0.6096110657044089276, -3.799475958216410376, 2.426869991387509806 ) ) ;
#15196=CARTESIAN_POINT ( 'NONE',  ( -1.750316316486840051, -5.559957627118639500, 3.126818518378589928 ) ) ;
#15198=CARTESIAN_POINT ( 'NONE',  ( 0.8748826269292639957, -2.262448931189380286, 2.515205712983200392 ) ) ;
#15200=CARTESIAN_POINT ( 'NONE',  ( -2.352190863465239978, -4.917313796054239461, 4.622903765856379188 ) ) ;
#15201=CARTESIAN_POINT ( 'NONE',  ( -1.238036348455400670, -2.006277760018210898, 3.062267469172299528 ) ) ;
#15206=CARTESIAN_POINT ( 'NONE',  ( -2.033393610350109793, -4.777584066324510381, 5.884928737465370041 ) ) ;
#15211=ORIENTED_EDGE ( 'NONE', *, *, #1873, .F. ) ;
#15213=CARTESIAN_POINT ( 'NONE',  ( -0.7983658734557950165, -5.166525423728809407, 6.913847129767330735 ) ) ;
#15216=CARTESIAN_POINT ( 'NONE',  ( -2.584100759211431786, -4.664983501243040287, 4.095403473953163953 ) ) ;
#15219=CARTESIAN_POINT ( 'NONE',  ( 1.480680413335799805, -1.214475958216410190, 6.529298007719799735 ) ) ;
#15220=CARTESIAN_POINT ( 'NONE',  ( -2.191755591049691532, -0.2536016949152540834, 3.203650300307721466 ) ) ;
#15222=CARTESIAN_POINT ( 'NONE',  ( -0.7093417302541390468, -0.4646186440677970153, 6.943956659919700236 ) ) ;
#15224=CARTESIAN_POINT ( 'NONE',  ( -0.5609751937345790473, -0.1601694915254239793, 7.293870047334757523 ) ) ;
#15228=CARTESIAN_POINT ( 'NONE',  ( 2.219956784870649180, -2.173136654396200740, 3.918630970161570026 ) ) ;
#15229=CARTESIAN_POINT ( 'NONE',  ( 2.328217775191430139, -5.381991525423729605, 5.043379051721160522 ) ) ;
#15230=CARTESIAN_POINT ( 'NONE',  ( 0.2908063684825958894, -1.055298816558370101, 7.337905485238597869 ) ) ;
#15232=CARTESIAN_POINT ( 'NONE',  ( -0.8298945877350979439, -5.211074464177370302, 2.494426474263899962 ) ) ;
#15233=CARTESIAN_POINT ( 'NONE',  ( 1.703239418290648732, -0.5429564742160235546, 3.553755118148703929 ) ) ;
#15235=CARTESIAN_POINT ( 'NONE',  ( 2.051568858000881068, -0.5196681859277345605, 3.016498023208322277 ) ) ;
#15239=CARTESIAN_POINT ( 'NONE',  ( 2.050994839075679366, -0.9815930753335269099, 4.608774933727144862 ) ) ;
#15245=CARTESIAN_POINT ( 'NONE',  ( 2.632194480419669080, -2.289578095837640159, 5.038623552414890128 ) ) ;
#15249=CARTESIAN_POINT ( 'NONE',  ( 1.289141334274990447, -5.417584745762705545, 6.297747079672416426 ) ) ;
#15254=CARTESIAN_POINT ( 'NONE',  ( 1.112838723655040107, -5.426483050847459744, 6.773667561836210105 ) ) ;
#15255=CARTESIAN_POINT ( 'NONE',  ( 2.325590009395039903, -0.7292627805223299564, 5.061077271074021056 ) ) ;
#15256=CARTESIAN_POINT ( 'NONE',  ( 2.105672170043351166, -3.962493976234419790, 3.084680091961101045 ) ) ;
#15259=CARTESIAN_POINT ( 'NONE',  ( -0.8967027089122764361, -1.195028546288099625, 6.546842195331652903 ) ) ;
#15266=CARTESIAN_POINT ( 'NONE',  ( 1.685353174447271840, -5.039854330134263094, 3.014646825552728782 ) ) ;
#15267=CARTESIAN_POINT ( 'NONE',  ( 2.560337424259670591, -0.3622881355932213721, 4.001768473655590519 ) ) ;
#15269=CARTESIAN_POINT ( 'NONE',  ( 0.3949552299394610277, -3.776187669928119828, 2.379923265530350385 ) ) ;
#15273=CARTESIAN_POINT ( 'NONE',  ( -1.554165089654128584, -5.479872881355935199, 6.851145244874527584 ) ) ;
#15276=CARTESIAN_POINT ( 'NONE',  ( -1.978267656359408821, -5.197669491525419794, 5.974740860598791947 ) ) ;
#15280=CARTESIAN_POINT ( 'NONE',  ( 2.260890494820590124, -4.055647129387580208, 4.046455925041149371 ) ) ;
#15282=CARTESIAN_POINT ( 'NONE',  ( 0.1969988207263408952, -5.304612347394259686, 2.648915996644538584 ) ) ;
#15285=CARTESIAN_POINT ( 'NONE',  ( 0.5570002967656469961, -2.891232714973159812, 6.986590552960210587 ) ) ;
#15288=CARTESIAN_POINT ( 'NONE',  ( -2.049636678546640667, -3.356998480738929924, 4.582138519505405405 ) ) ;
#15293=CARTESIAN_POINT ( 'NONE',  ( 0.4360591020457930123, -0.3088983050847460277, 2.387347919655840034 ) ) ;
#15303=CARTESIAN_POINT ( 'NONE',  ( -0.5137283630188880235, -5.162076271186444743, 6.687652957477222770 ) ) ;
#15304=CARTESIAN_POINT ( 'NONE',  ( -0.9250303514741213817, -1.777235753495299608, 2.212544966868041474 ) ) ;
#15314=CARTESIAN_POINT ( 'NONE',  ( 2.226511124464869873, -1.074746228486680000, 5.462491901673799610 ) ) ;
#15316=CARTESIAN_POINT ( 'NONE',  ( -2.020286629067959971, -0.1913135593220339215, 6.420841923842841581 ) ) ;
#15321=CARTESIAN_POINT ( 'NONE',  ( -1.873832970144350130, -0.2625000000000002331, 2.826167029855650270 ) ) ;
#15326=CARTESIAN_POINT ( 'NONE',  ( -0.6096110657044611081, -1.800524041783590157, 2.426869991387521353 ) ) ;
#15328=CARTESIAN_POINT ( 'NONE',  ( -0.2189795514005259958, -5.595550847457629651, 2.356806637999020015 ) ) ;
#15332=CARTESIAN_POINT ( 'NONE',  ( 2.145694642186089851, -1.098034516774969882, 5.666819626392539888 ) ) ;
#15333=CARTESIAN_POINT ( 'NONE',  ( -1.480680413335760059, -4.385524041783589233, 6.529298007719829933 ) ) ;
#15335=AXIS2_PLACEMENT_3D ( 'NONE', #2835, #4126, #1264 ) ;
#15339=CARTESIAN_POINT ( 'NONE',  ( 1.292934267244360447, -1.214475958216409746, 6.294748514096617065 ) ) ;
#15345=CARTESIAN_POINT ( 'NONE',  ( -1.679950111053631900, -0.1957627118644069686, 5.880020650119711867 ) ) ;
#15347=CARTESIAN_POINT ( 'NONE',  ( 0.2266049403549809660, -3.453992510252061887, 2.055805624767989226 ) ) ;
#15348=CARTESIAN_POINT ( 'NONE',  ( -0.1686436619862690112, -4.981295943764799894, 2.349239845786320391 ) ) ;
#15349=CARTESIAN_POINT ( 'NONE',  ( 0.2453710345350221533, -5.144279661016955885, 6.738252723719333481 ) ) ;
#15353=CARTESIAN_POINT ( 'NONE',  ( 1.713314936023349944, -5.338983050847460277, 3.089913064446569546 ) ) ;
#15356=CARTESIAN_POINT ( 'NONE',  ( -1.428515267734880023, -5.568855932203390147, 2.829745655876930055 ) ) ;
#15359=CARTESIAN_POINT ( 'NONE',  ( 2.334748642087659753, -0.6593979156574649725, 4.403867486184820379 ) ) ;
#15360=CARTESIAN_POINT ( 'NONE',  ( 0.2010642693393740188, -3.752899381639833720, 2.053740970237999619 ) ) ;
#15362=CARTESIAN_POINT ( 'NONE',  ( 2.036910256464071090, -0.6593979156574641953, 4.443293066459086837 ) ) ;
#15367=CARTESIAN_POINT ( 'NONE',  ( 0.7322514394120266390, -0.3133474576271193524, 2.149183891723918993 ) ) ;
#15368=CARTESIAN_POINT ( 'NONE',  ( 1.526791597786429922, -2.774791273531720392, 6.490992212270249695 ) ) ;
#15371=CARTESIAN_POINT ( 'NONE',  ( -1.925836318347889931, -5.488771186440680516, 6.525927015348141680 ) ) ;
#15380=CARTESIAN_POINT ( 'NONE',  ( -2.349464193210359930, -3.356998480738930368, 4.563019372514619754 ) ) ;
#15383=CARTESIAN_POINT ( 'NONE',  ( 1.449568901432419343, -5.337500000000000355, 3.250431098567584165 ) ) ;
#15389=CARTESIAN_POINT ( 'NONE',  ( 1.728413393879709936, -4.311818300558750039, 6.297289212178290185 ) ) ;
#15391=CARTESIAN_POINT ( 'NONE',  ( -0.9976707306414490661, -3.077539021279473097, 6.494311833503151554 ) ) ;
#15396=CARTESIAN_POINT ( 'NONE',  ( -1.626408692231610109, -4.707719201459649838, 6.401040991074980369 ) ) ;
#15403=CARTESIAN_POINT ( 'NONE',  ( -0.8731223871104993872, -5.170974576271189171, 6.558046933601121786 ) ) ;
#15404=CARTESIAN_POINT ( 'NONE',  ( 2.008025181017630167, -2.079983501243050981, 2.964791492240490101 ) ) ;
#15412=CARTESIAN_POINT ( 'NONE',  ( 1.704669856830330010, -0.8030495317899829510, 3.080704711052640210 ) ) ;
#15413=CARTESIAN_POINT ( 'NONE',  ( 0.8259795455966094657, -2.545749267008810435, 6.579537079411867495 ) ) ;
#15414=CARTESIAN_POINT ( 'NONE',  ( 1.647941990407678636, -0.04449152542372906277, 3.475676388127089123 ) ) ;
#15416=CARTESIAN_POINT ( 'NONE',  ( -2.224278379903029901, -0.5091101694915259879, 5.468825643806110470 ) ) ;
#15418=CARTESIAN_POINT ( 'NONE',  ( 0.3743405594629510280, -0.1423728813559329842, 7.023440622744399953 ) ) ;
#15419=CARTESIAN_POINT ( 'NONE',  ( 1.115198193348289957, -1.261052534792989954, 6.772457159276550342 ) ) ;
#15423=CARTESIAN_POINT ( 'NONE',  ( 2.237394498046679558, -2.336154672414219924, 5.429939413646329704 ) ) ;
#15425=CARTESIAN_POINT ( 'NONE',  ( 2.020286629067969297, -5.408686440677975327, 6.420841923842827370 ) ) ;
#15428=CARTESIAN_POINT ( 'NONE',  ( -2.255259958075430227, -1.703530012270459970, 5.372717034856060003 ) ) ;
#15429=CARTESIAN_POINT ( 'NONE',  ( -1.949083719010310078, -0.5402542372881364852, 4.055210292801460170 ) ) ;
#15434=CARTESIAN_POINT ( 'NONE',  ( -2.021195349941399044, -1.819971453711898945, 4.339901124684693912 ) ) ;
#15439=CARTESIAN_POINT ( 'NONE',  ( 2.644456467089558949, -3.803316834576382366, 4.476474416072626639 ) ) ;
#15441=CARTESIAN_POINT ( 'NONE',  ( -0.1881942810071039751, -5.280843314568230085, 2.350674491507239949 ) ) ;
#15442=CARTESIAN_POINT ( 'NONE',  ( 1.880631435828169939, -5.355296610169490101, 3.876649216148224220 ) ) ;
#15444=CARTESIAN_POINT ( 'NONE',  ( 2.306642602145299925, -0.08453389830508534208, 5.166805192608479480 ) ) ;
#15450=CARTESIAN_POINT ( 'NONE',  ( -1.724579595320040015, -1.660794312053859967, 3.098572228637930248 ) ) ;
#15452=CARTESIAN_POINT ( 'NONE',  ( -2.329383452786330189, -4.571830348089889640, 5.035735636132879556 ) ) ;
#15456=CARTESIAN_POINT ( 'NONE',  ( 2.268288188848061715, -0.3489406779661023417, 3.322421079292310786 ) ) ;
#15457=CARTESIAN_POINT ( 'NONE',  ( -1.097561405233230092, -3.613169651910099756, 2.618148744692269769 ) ) ;
#15460=CARTESIAN_POINT ( 'NONE',  ( 2.191755591049679541, -5.046398305084744962, 3.203650300307709475 ) ) ;
#15463=CARTESIAN_POINT ( 'NONE',  ( -0.2189795514005259958, -5.295550847457628940, 2.356806637999020015 ) ) ;
#15466=CARTESIAN_POINT ( 'NONE',  ( -2.239137794397029868, -4.987178660919110662, 3.975425900939220103 ) ) ;
#15467=CARTESIAN_POINT ( 'NONE',  ( 1.526064881623949931, -0.7763906680874419486, 2.903976516638540062 ) ) ;
#15469=CARTESIAN_POINT ( 'NONE',  ( 0.2134934900267039248, -5.004947479095229745, 2.650814970067049803 ) ) ;
#15472=CARTESIAN_POINT ( 'NONE',  ( -1.917298190932639868, -3.496728210468659892, 3.335187436117939885 ) ) ;
#15474=CARTESIAN_POINT ( 'NONE',  ( 1.366362128262241571, -3.915917399657852904, 3.167695729602394206 ) ) ;
#15484=UNCERTAINTY_MEASURE_WITH_UNIT (LENGTH_MEASURE( 1.000000000000000082E-05 ), #10944, 'distance_accuracy_value', 'NONE');
#15487=CARTESIAN_POINT ( 'NONE',  ( -1.725722849164588624, -5.197669491525426011, 5.812007984777676661 ) ) ;
#15489=CARTESIAN_POINT ( 'NONE',  ( 1.681140935901590083, -0.7917284067793100011, 3.001197262379470043 ) ) ;
#15492=CARTESIAN_POINT ( 'NONE',  ( 1.444955263746720009, -2.332313796054249710, 2.842353646881480511 ) ) ;
#15493=CARTESIAN_POINT ( 'NONE',  ( -1.854389246811851022, -3.151244762504313179, 3.819010576716904026 ) ) ;
#15494=CARTESIAN_POINT ( 'NONE',  ( 2.046424002475610404, -0.07118644067796651986, 4.536201610417760044 ) ) ;
#15497=CARTESIAN_POINT ( 'NONE',  ( 1.851073041990159984, -0.4067796610169499560, 6.153284478378259870 ) ) ;
#15502=CARTESIAN_POINT ( 'NONE',  ( 1.194742379459969861, -0.1245762711864410038, 6.727584234649759409 ) ) ;
#15503=CARTESIAN_POINT ( 'NONE',  ( 1.794646911016580137, -1.167899381639829981, 6.222494056560660347 ) ) ;
#15510=CARTESIAN_POINT ( 'NONE',  ( 0.4790341583531377845, -1.916965483225030020, 2.395814251711721354 ) ) ;
#15512=CARTESIAN_POINT ( 'NONE',  ( -1.554165089654128584, -5.479872881355935199, 6.851145244874527584 ) ) ;
#15514=CARTESIAN_POINT ( 'NONE',  ( 2.291237445532070094, -0.9350164987569499209, 4.162434510291790346 ) ) ;
#15515=CARTESIAN_POINT ( 'NONE',  ( 2.046424002475610404, -0.3711864406779670222, 4.536201610417760044 ) ) ;
#15521=CARTESIAN_POINT ( 'NONE',  ( -0.3681613504765444134, -2.122719201459649874, 2.680257674196191431 ) ) ;
#15523=CARTESIAN_POINT ( 'NONE',  ( 2.087380238839969593, -0.4067796610169500116, 6.338810156469096846 ) ) ;
#15527=CARTESIAN_POINT ( 'NONE',  ( 1.042222075699120287, -0.4245762711864407013, 6.468743694056166227 ) ) ;
#15531=CARTESIAN_POINT ( 'NONE',  ( 0.6187874668174475623, -5.135381355932194580, 6.657494107589526422 ) ) ;
#15534=CARTESIAN_POINT ( 'NONE',  ( 2.350067830300900162, -5.377542372881360500, 4.825253242917690422 ) ) ;
#15538=CARTESIAN_POINT ( 'NONE',  ( 0.8986180677147459495, -1.963542059801610229, 2.524860635301609868 ) ) ;
#15541=CARTESIAN_POINT ( 'NONE',  ( 0.5972539422562040956, -1.008722239981790558, 6.664227474374466276 ) ) ;
#15546=CARTESIAN_POINT ( 'NONE',  ( -2.328217775191430139, -0.5180084745762719711, 5.043379051721170292 ) ) ;
#15549=CARTESIAN_POINT ( 'NONE',  ( -1.747582379783008788, -5.484322033898315851, 6.697200745122486865 ) ) ;
#15552=CARTESIAN_POINT ( 'NONE',  ( -1.750316316486840051, -5.259957627118649448, 3.126818518378589928 ) ) ;
#15556=CARTESIAN_POINT ( 'NONE',  ( -1.132648842710420656, -1.493935417675870791, 7.100045893750492887 ) ) ;
#15559=CARTESIAN_POINT ( 'NONE',  ( -2.626509418457480649, -4.571830348089889640, 5.080213055741825023 ) ) ;
#15561=CARTESIAN_POINT ( 'NONE',  ( 0.8242394280877100021, -4.428259742000189902, 6.904399023015010073 ) ) ;
#15563=CARTESIAN_POINT ( 'NONE',  ( 0.1086361371091010830, -2.937809291549738688, 6.750146344128172160 ) ) ;
#15566=CARTESIAN_POINT ( 'NONE',  ( -0.4037348727536037574, -0.5906145504024216120, 2.679104755345550704 ) ) ;
#15574=CARTESIAN_POINT ( 'NONE',  ( -1.614765845140348821, -5.193220338983044471, 5.967758800287426446 ) ) ;
#15575=CARTESIAN_POINT ( 'NONE',  ( -1.769056124370508964, -1.684082600342149627, 2.721729512470790979 ) ) ;
#15580=CLOSED_SHELL ( 'NONE', ( #1312, #10491, #13595, #439, #239, #14220, #7090, #6511, #12546, #17713, #15936, #11638, #3348, #8036, #7061, #2667 ) ) ;
#15585=CARTESIAN_POINT ( 'NONE',  ( -2.349464193210359930, -3.356998480738930368, 4.563019372514619754 ) ) ;
#15586=CARTESIAN_POINT ( 'NONE',  ( 0.1781895581254300809, -3.453992510252061887, 2.654724878163539969 ) ) ;
#15587=CARTESIAN_POINT ( 'NONE',  ( 1.980638384804650931, -0.06228813559322075172, 4.159858630563753934 ) ) ;
#15588=CARTESIAN_POINT ( 'NONE',  ( -0.0009602353114128930152, -5.165218916585829767, 2.501032900279580140 ) ) ;
#15591=CARTESIAN_POINT ( 'NONE',  ( -0.6343239990445920240, -2.099430913171359769, 2.433641963034089972 ) ) ;
#15597=CARTESIAN_POINT ( 'NONE',  ( -0.1768565782246519502, -1.847100618360170365, 2.353200596935780098 ) ) ;
#15599=CARTESIAN_POINT ( 'NONE',  ( -2.087380238839969593, -5.493220338983046069, 6.338810156469112833 ) ) ;
#15603=CARTESIAN_POINT ( 'NONE',  ( 2.046174187462399985, -1.121322805063259986, 5.862719605943959245 ) ) ;
#15605=CARTESIAN_POINT ( 'NONE',  ( -1.869504824896970119, -0.5046610169491535514, 5.548311746956866131 ) ) ;
#15613=CARTESIAN_POINT ( 'NONE',  ( 1.181710496343130190, -2.798079561820010941, 6.378827610405712001 ) ) ;
#15625=CARTESIAN_POINT ( 'NONE',  ( -1.965557623688110933, -5.511016949152534927, 5.292675575926340414 ) ) ;
#15628=CARTESIAN_POINT ( 'NONE',  ( 2.180207327701309428, -0.09343220338983103390, 5.586116916730190063 ) ) ;
#15629=CARTESIAN_POINT ( 'NONE',  ( 1.641808337277750107, -5.413135593220339103, 6.386111670537619744 ) ) ;
#15635=CARTESIAN_POINT ( 'NONE',  ( -2.313035575219740014, -1.427911429170980018, 5.134294963419759661 ) ) ;
#15638=CARTESIAN_POINT ( 'NONE',  ( 1.124021676335459796, -2.010118636378181112, 2.982013645643220023 ) ) ;
#15645=CARTESIAN_POINT ( 'NONE',  ( 2.601107615185130673, -0.08453389830508521718, 5.226397344856369642 ) ) ;
#15646=CARTESIAN_POINT ( 'NONE',  ( -2.334032080503389839, -3.310421904162350160, 5.001728246382240783 ) ) ;
#15649=CARTESIAN_POINT ( 'NONE',  ( -0.4221287159901280228, -5.157627118644064979, 7.320050063945812369 ) ) ;
#15656=CARTESIAN_POINT ( 'NONE',  ( 2.510208264419000468, -1.074746228486680000, 5.561375738133185642 ) ) ;
#15659=CARTESIAN_POINT ( 'NONE',  ( 0.009452110982655399438, -5.000192044704546035, 2.649999999999998579 ) ) ;
#15661=CARTESIAN_POINT ( 'NONE',  ( 2.137408332595949645, -2.149848366107910191, 3.714996798363940034 ) ) ;
#15663=CARTESIAN_POINT ( 'NONE',  ( -0.2620510901103649815, -3.706322805063249959, 2.361180871966390260 ) ) ;
#15666=CARTESIAN_POINT ( 'NONE',  ( 2.016543577558679079, -4.078935417675856101, 4.314702916654005627 ) ) ;
#15676=CARTESIAN_POINT ( 'NONE',  ( 1.994315313497110997, -5.386440677966105817, 5.187224322759965922 ) ) ;
#15683=CARTESIAN_POINT ( 'NONE',  ( -1.236334101859210000, -2.029566048306499670, 2.697445712080720259 ) ) ;
#15684=CARTESIAN_POINT ( 'NONE',  ( -0.1086361371090530797, -2.662190708450249854, 6.750146344128172160 ) ) ;
#15689=CARTESIAN_POINT ( 'NONE',  ( 1.392553072310509510, -0.03559322033898333626, 3.191531554476519261 ) ) ;
#15690=CARTESIAN_POINT ( 'NONE',  ( -1.586727176531439909, -1.982989471729919906, 2.961885344765640138 ) ) ;
#15693=CARTESIAN_POINT ( 'NONE',  ( 2.255259958075439553, -3.896469987729530349, 5.372717034855999607 ) ) ;
#15694=CARTESIAN_POINT ( 'NONE',  ( -2.268288188848061715, -5.551059322033894183, 3.322421079292323665 ) ) ;
#15697=CARTESIAN_POINT ( 'NONE',  ( -0.05465110135555984600, -0.4512711864406789841, 6.752241303418941243 ) ) ;
#15701=CARTESIAN_POINT ( 'NONE',  ( -1.238036348455400670, -2.006277760018210898, 3.062267469172299528 ) ) ;
#15703=CARTESIAN_POINT ( 'NONE',  ( 0.9664230948141925293, -0.3177966101694921219, 2.228384861502251457 ) ) ;
#15710=CARTESIAN_POINT ( 'NONE',  ( -1.246151616534680651, -5.568855932203385706, 3.068501529594771071 ) ) ;
#15712=CARTESIAN_POINT ( 'NONE',  ( -2.351526912647309953, -0.2269067796610170218, 4.606040641882809261 ) ) ;
#15718=CARTESIAN_POINT ( 'NONE',  ( 2.137408332595949645, -2.149848366107910191, 3.714996798363940034 ) ) ;
#15721=CARTESIAN_POINT ( 'NONE',  ( 1.698651900122530867, -2.406019537279079579, 5.853032334688926142 ) ) ;
#15726=CARTESIAN_POINT ( 'NONE',  ( 2.230812463554230352, -0.4023305084745772420, 6.137473736419911674 ) ) ;
#15727=CARTESIAN_POINT ( 'NONE',  ( -2.352190863465239978, -4.917313796054239461, 4.622903765856379188 ) ) ;
#15730=CARTESIAN_POINT ( 'NONE',  ( -2.614198783383141045, -5.233262711864406391, 4.243032045539295360 ) ) ;
#15738=CARTESIAN_POINT ( 'NONE',  ( -1.951437470830620136, -5.057043525783970317, 3.384463041838880137 ) ) ;
#15741=CARTESIAN_POINT ( 'NONE',  ( 0.09706517602699299418, -2.638902420161969520, 7.051451474958980725 ) ) ;
#15742=CARTESIAN_POINT ( 'NONE',  ( 0.2570708662023959423, -5.304612347394245475, 2.048876625919409111 ) ) ;
#15743=CARTESIAN_POINT ( 'NONE',  ( 2.313035575219750228, -4.172088570829020071, 5.134294963419709923 ) ) ;
#15745=CARTESIAN_POINT ( 'NONE',  ( 0.5381211601353905749, -4.451548030288480895, 6.681243917250638376 ) ) ;
#15749=EDGE_LOOP ( 'NONE', ( #16223, #8880 ) ) ;
#15755=CARTESIAN_POINT ( 'NONE',  ( -2.012177589105470066, -5.515466101694915579, 5.107213040360599088 ) ) ;
#15756=CARTESIAN_POINT ( 'NONE',  ( 2.327043743583509627, -2.382731248990799244, 5.975923629552606364 ) ) ;
#15759=CARTESIAN_POINT ( 'NONE',  ( -1.864786684738369837, -4.804713230972779137, 2.817120744449669978 ) ) ;
#15763=CARTESIAN_POINT ( 'NONE',  ( -1.948278411993560111, -3.193980462720909852, 6.020210936496040333 ) ) ;
#15764=CARTESIAN_POINT ( 'NONE',  ( 1.616473591439308688, -3.989623140882693875, 5.965667796385536903 ) ) ;
#15768=CARTESIAN_POINT ( 'NONE',  ( -0.5134687485629449988, -3.384127645387192018, 2.096259702418250104 ) ) ;
#15770=CARTESIAN_POINT ( 'NONE',  ( -1.949083719010310078, -0.2402542372881359412, 4.055210292801460170 ) ) ;
#15771=CARTESIAN_POINT ( 'NONE',  ( 1.444955263746720009, -2.332313796054249710, 2.842353646881480511 ) ) ;
#15775=CARTESIAN_POINT ( 'NONE',  ( 1.710920205120059823, -4.012911429170970656, 6.316012914303540171 ) ) ;
#15777=CARTESIAN_POINT ( 'NONE',  ( 2.416676968769261080, -5.095338983050850423, 5.796598111919825769 ) ) ;
#15779=CARTESIAN_POINT ( 'NONE',  ( 0.8570167067220200163, -0.3177966101694920664, 2.508190348879349774 ) ) ;
#15784=CARTESIAN_POINT ( 'NONE',  ( -1.313542260532420292, -3.124115597856051085, 6.277817661335885369 ) ) ;
#15785=CARTESIAN_POINT ( 'NONE',  ( 1.255262969126039558E-16, -0.3000000000000002665, 2.050000000000001155 ) ) ;
#15791=CARTESIAN_POINT ( 'NONE',  ( 1.713314936023349944, -5.338983050847460277, 3.089913064446569546 ) ) ;
#15793=CARTESIAN_POINT ( 'NONE',  ( -0.9193620247240871235, -0.2831443699174389095, 2.206709149717571261 ) ) ;
#15795=CARTESIAN_POINT ( 'NONE',  ( -3.408368997776849933E-15, -5.599999999999999645, 2.350000000000000089 ) ) ;
#15796=CARTESIAN_POINT ( 'NONE',  ( -0.6096110657044609971, -1.800524041783589935, 2.426869991387519576 ) ) ;
#15798=CARTESIAN_POINT ( 'NONE',  ( -1.736825397686170502, -1.614217735477279536, 3.605313112995154334 ) ) ;
#15804=CARTESIAN_POINT ( 'NONE',  ( 0.2469343877495150108, -0.004449152542373164231, 2.057675570509529539 ) ) ;
#15805=CARTESIAN_POINT ( 'NONE',  ( 1.026235786675480099, -4.404971453711899798, 6.817920158464540137 ) ) ;
#15808=CARTESIAN_POINT ( 'NONE',  ( -3.188875856275119715E-15, -5.300000000000000711, 2.050000000000001155 ) ) ;
#15816=CARTESIAN_POINT ( 'NONE',  ( 1.923406176634910203, -0.8030495317899833951, 2.875176962145290727 ) ) ;
#15820=CARTESIAN_POINT ( 'NONE',  ( 1.507201387236020151, -2.475884402143949892, 6.507509243627189299 ) ) ;
#15823=CARTESIAN_POINT ( 'NONE',  ( 0.2270348434643680025, -5.304612347394249916, 2.348896311281980065 ) ) ;
#15824=CARTESIAN_POINT ( 'NONE',  ( -2.296954468777729463, -4.963890372630819670, 4.187412587068699565 ) ) ;
#15828=CARTESIAN_POINT ( 'NONE',  ( -1.802718065953990978, -5.033755237495684653, 3.717600174934233781 ) ) ;
#15832=CARTESIAN_POINT ( 'NONE',  ( -0.2812789908084309953, -0.4557203389830509765, 7.036533610117280624 ) ) ;
#15840=CARTESIAN_POINT ( 'NONE',  ( 1.494593880360790550, -5.338983050847455836, 3.295456077495951153 ) ) ;
#15842=CARTESIAN_POINT ( 'NONE',  ( 1.292937800126339631, -2.522460978720530989, 7.017633607369027082 ) ) ;
#15848=CARTESIAN_POINT ( 'NONE',  ( -1.145304265383870090, -3.077539021279469988, 6.755972720436099088 ) ) ;
#15849=CARTESIAN_POINT ( 'NONE',  ( -0.05638445020225820586, -4.222506023765566496, 6.752248190741917178 ) ) ;
#15853=CARTESIAN_POINT ( 'NONE',  ( -1.032615103526609568, -4.315659176918716255, 7.144753513336388195 ) ) ;
#15854=CARTESIAN_POINT ( 'NONE',  ( -1.134881315981510541, -0.1779661016949160846, 6.410767520434657918 ) ) ;
#15855=CARTESIAN_POINT ( 'NONE',  ( 1.167621112247380077, -2.821367850108300157, 6.743381174846749815 ) ) ;
#15860=CARTESIAN_POINT ( 'NONE',  ( -0.8748826269293140667, -3.337551068810609145, 2.515205712983220820 ) ) ;
#15861=CARTESIAN_POINT ( 'NONE',  ( 2.586172839791708533, -5.064194915254235596, 4.104546363490936045 ) ) ;
#15871=CARTESIAN_POINT ( 'NONE',  ( -2.035869680587120811, -3.310421904162345719, 4.964832940349540813 ) ) ;
#15873=CARTESIAN_POINT ( 'NONE',  ( 2.540842781840729536, -0.3889830508474575455, 5.466141598148674952 ) ) ;
#15880=CARTESIAN_POINT ( 'NONE',  ( -2.022304719220918479, -5.533262711864405325, 4.346496488058700258 ) ) ;
#15881=CARTESIAN_POINT ( 'NONE',  ( -2.155845792290839391, -0.2447033898305089883, 3.756158857535781159 ) ) ;
#15884=CARTESIAN_POINT ( 'NONE',  ( 1.152986057739970205, -3.846052534792983923, 2.309657588616410351 ) ) ;
#15886=CARTESIAN_POINT ( 'NONE',  ( -1.764807890102220167, -3.221109627369169726, 3.143016121304770039 ) ) ;
#15890=CARTESIAN_POINT ( 'NONE',  ( -0.7128755192781907057, -1.777235753495299608, 2.774718115017459130 ) ) ;
#15899=CARTESIAN_POINT ( 'NONE',  ( 0.04351999560419626129, -1.078587104846650213, 7.353529668759038351 ) ) ;
#15900=CARTESIAN_POINT ( 'NONE',  ( 1.994983296312400123, -4.265241723982169830, 5.948514050749290405 ) ) ;
#15903=CARTESIAN_POINT ( 'NONE',  ( 1.031876288691629506, -5.130932203389829915, 7.145012538880298081 ) ) ;
#15911=CARTESIAN_POINT ( 'NONE',  ( -2.380466601827099016, -1.889836318576769036, 3.526759849567179916 ) ) ;
#15913=CARTESIAN_POINT ( 'NONE',  ( 0.9930264841371569950, -0.4076464065212260235, 2.562902636367419884 ) ) ;
#15915=CARTESIAN_POINT ( 'NONE',  ( 0.8986180677147459495, -1.963542059801610229, 2.524860635301609868 ) ) ;
#15916=CARTESIAN_POINT ( 'NONE',  ( 1.484081582636959551, -5.328211948015596278, 2.487334927317659705 ) ) ;
#15918=CARTESIAN_POINT ( 'NONE',  ( -2.091881088960070745, -1.610376859117309767, 6.333140288723886790 ) ) ;
#15921=CARTESIAN_POINT ( 'NONE',  ( -2.028464043723881005, -4.870737219477664581, 5.016599851465114668 ) ) ;
#15924=CARTESIAN_POINT ( 'NONE',  ( 2.340070819011249803, -0.3800847457627120063, 4.950151441910540129 ) ) ;
#15936=ADVANCED_FACE ( 'NONE', ( #7403 ), #13387, .T. ) ;
#15937=CARTESIAN_POINT ( 'NONE',  ( -1.042222075699109407, -5.475423728813556323, 6.468743694056166227 ) ) ;
#15940=CARTESIAN_POINT ( 'NONE',  ( -1.381042549632419902, -1.540511994252449890, 6.605640880016140137 ) ) ;
#15941=CARTESIAN_POINT ( 'NONE',  ( -1.315254646989760134, -2.778632149891700376, 7.005042061779727547 ) ) ;
#15947=CARTESIAN_POINT ( 'NONE',  ( -1.381042549632419902, -1.540511994252449890, 6.605640880016140137 ) ) ;
#15949=CARTESIAN_POINT ( 'NONE',  ( -2.218077401483159683, -4.824160642901089702, 5.486688202856539576 ) ) ;
#15950=CARTESIAN_POINT ( 'NONE',  ( -2.033547680391670998, -4.641695212954759064, 4.417890669792460479 ) ) ;
#15952=CARTESIAN_POINT ( 'NONE',  ( 0.009417288784632644669, -5.000743947056720096, 2.370019840861731897 ) ) ;
#15956=CARTESIAN_POINT ( 'NONE',  ( 1.351903350398191206, -0.1156779661016950206, 6.245004350000406212 ) ) ;
#15957=CARTESIAN_POINT ( 'NONE',  ( 0.5570002967656469961, -2.891232714973159812, 6.986590552960210587 ) ) ;
#15964=CARTESIAN_POINT ( 'NONE',  ( -1.794646911016549495, -4.432100618360158784, 6.222494056560700315 ) ) ;
#15966=CARTESIAN_POINT ( 'NONE',  ( -0.4917262214559124933, -5.591101694915256104, 2.092115739186370948 ) ) ;
#15969=CARTESIAN_POINT ( 'NONE',  ( -2.143090896833110381, -0.5046610169491529962, 5.672454929438350391 ) ) ;
#15973=CARTESIAN_POINT ( 'NONE',  ( 1.741179788930650840, -4.265241723982168942, 5.787747574231955738 ) ) ;
#15974=CARTESIAN_POINT ( 'NONE',  ( -1.254903241568450900, -0.4735169491525429986, 7.038391080368498365 ) ) ;
#15978=CARTESIAN_POINT ( 'NONE',  ( 0.0003104168811371160069, -0.4450801552861859967, 2.198280450787269746 ) ) ;
#15979=CARTESIAN_POINT ( 'NONE',  ( -0.5889081234606770021, -5.462076271186440124, 6.978529000034869867 ) ) ;
#15982=CARTESIAN_POINT ( 'NONE',  ( -2.350067830300900162, -0.2224576271186440024, 4.825253242917700192 ) ) ;
#15984=CARTESIAN_POINT ( 'NONE',  ( 2.107551805806971323, -4.288530012270460823, 6.312866726931170902 ) ) ;
#15986=CARTESIAN_POINT ( 'NONE',  ( 2.062913653388430024, -2.382731248990799688, 5.832754583370790336 ) ) ;
#15989=CARTESIAN_POINT ( 'NONE',  ( 1.454969160282001406, -2.452596113855660676, 6.148435909958180901 ) ) ;
#15996=CARTESIAN_POINT ( 'NONE',  ( 2.293791554891360551, -0.8224159336754829353, 6.034778631725497000 ) ) ;
#15998=CARTESIAN_POINT ( 'NONE',  ( -0.4735094604798580353, -4.567989471729919870, 7.005327412390699671 ) ) ;
#16001=CARTESIAN_POINT ( 'NONE',  ( -1.554165089654128584, -5.179872881355935377, 6.851145244874527584 ) ) ;
#16011=CARTESIAN_POINT ( 'NONE',  ( -1.392767620582729293, -2.029566048306499670, 2.440948861123721780 ) ) ;
#16014=CARTESIAN_POINT ( 'NONE',  ( -1.962536940652960027, -2.895073591333140239, 5.998920491814800471 ) ) ;
#16015=CARTESIAN_POINT ( 'NONE',  ( 1.319613955262860072, -5.028306595106929677, 2.740497729816110173 ) ) ;
#16016=CARTESIAN_POINT ( 'NONE',  ( 2.651429253058529945, -0.9815930753335269099, 4.585822029124893895 ) ) ;
#16018=CARTESIAN_POINT ( 'NONE',  ( -0.5972539422561604638, -4.591277760018214416, 6.664227474374482263 ) ) ;
#16027=CARTESIAN_POINT ( 'NONE',  ( -1.044181395669830259, -2.052854336594790219, 2.590869634085910089 ) ) ;
#16029=CARTESIAN_POINT ( 'NONE',  ( 2.328217775191430139, -5.381991525423729605, 5.043379051721160522 ) ) ;
#16032=CARTESIAN_POINT ( 'NONE',  ( 2.102728310581320148, -4.241953435693879726, 5.757014351541050345 ) ) ;
#16033=CARTESIAN_POINT ( 'NONE',  ( 2.013199450439951299, -3.873181699441240244, 5.102405038954985095 ) ) ;
#16038=CARTESIAN_POINT ( 'NONE',  ( 1.042222075699120287, -0.1245762711864410871, 6.468743694056166227 ) ) ;
#16039=CARTESIAN_POINT ( 'NONE',  ( -1.145304265383870090, -3.077539021279469988, 6.755972720436099088 ) ) ;
#16044=CARTESIAN_POINT ( 'NONE',  ( -0.4539185741479769276, -3.384127645387189354, 2.390735265170451207 ) ) ;
#16046=CARTESIAN_POINT ( 'NONE',  ( 2.171642826483958899, -5.104237288135595740, 6.225392547715717484 ) ) ;
#16054=CARTESIAN_POINT ( 'NONE',  ( 2.016543577558679079, -4.078935417675856101, 4.314702916654005627 ) ) ;
#16056=CARTESIAN_POINT ( 'NONE',  ( 1.747582379783020778, -0.1156779661016950206, 6.697200745122486865 ) ) ;
#16061=CARTESIAN_POINT ( 'NONE',  ( 1.661700935665417544, -5.037501140877957084, 3.038299064334577082 ) ) ;
#16062=CARTESIAN_POINT ( 'NONE',  ( -0.5385843327681574255, -3.683034516774964295, 2.101338688959530465 ) ) ;
#16064=CARTESIAN_POINT ( 'NONE',  ( 0.2023972492402060230, -3.453992510252060111, 2.355265251465770149 ) ) ;
#16068=CARTESIAN_POINT ( 'NONE',  ( 1.642659730162729925, -3.663587104846653730, 3.468508687188663675 ) ) ;
#16071=CARTESIAN_POINT ( 'NONE',  ( 1.124021676335459796, -2.010118636378181112, 2.982013645643220023 ) ) ;
#16076=CARTESIAN_POINT ( 'NONE',  ( 1.233489123281660715, -0.9621456634052125700, 7.049812391606558037 ) ) ;
#16078=CARTESIAN_POINT ( 'NONE',  ( -2.281778813005780115, -4.847448931189379806, 5.276394947932169899 ) ) ;
#16081=CARTESIAN_POINT ( 'NONE',  ( -2.306642602145299925, -5.215466101694909540, 5.166805192608490138 ) ) ;
#16086=EDGE_LOOP ( 'NONE', ( #11724, #12594, #9013, #12424 ) ) ;
#16089=B_SPLINE_CURVE_WITH_KNOTS ( 'NONE', 3,
 ( #3720, #9379, #5081, #9531, #6845, #4988, #15189, #2498, #17930, #6565, #8063, #3595, #10642, #1015, #3683, #14903, #2214, #2315, #9331, #14999, #10926, #16572, #13705, #9616, #826, #12402, #7858, #5171, #10821, #9442, #2416, #6652, #12306, #2582, #18022, #5369, #11009, #15276, #16657, #8232, #13880, #1196, #1475, #165, #5640, #8600, #5545, #2771, #7030, #9988, #14247, #15552, #9893, #11190, #1647, #14327, #11283, #2678, #12488, #15463, #4145, #1285 ),
 .UNSPECIFIED., .F., .F.,
 ( 4, 1, 1, 1, 1, 1, 1, 1, 1, 1, 1, 1, 1, 1, 1, 1, 1, 1, 1, 1, 1, 1, 1, 1, 1, 1, 1, 1, 1, 1, 1, 1, 1, 1, 1, 1, 1, 1, 1, 1, 1, 1, 1, 1, 1, 1, 1, 1, 1, 1, 1, 1, 1, 1, 1, 1, 1, 1, 1, 4 ),
 ( 0.7853981633974479459, 0.8785809963429079827, 0.9717638292883680196, 1.064946662233830166, 1.158129495179289981, 1.251312328124750017, 1.344495161070210054, 1.437677994015669869, 1.530860826961129906, 1.624043659906589943, 1.717226492852049979, 1.810409325797509794, 1.903592158742969609, 1.996774991688429868, 2.089957824633889683, 2.183140657579349941, 2.276323490524809756, 2.369506323470270015, 2.462689156415730274, 2.555871989361190089, 2.649054822306649903, 2.742237655252109718, 2.835420488197569977, 2.928603321143030236, 3.021786154088490051, 3.114968987033949865, 3.208151819979410124, 3.301334652924869939, 3.394517485870330198, 3.487700318815790013, 3.580883151761249827, 3.674065984706710086, 3.767248817652169901, 3.860431650597620390, 3.953614483543079761, 4.046797316488540019, 4.139980149433999834, 4.233162982379460537, 4.326345815324920352, 4.419528648270380167, 4.512711481215839981, 4.605894314161299796, 4.699077147106760499, 4.792259980052219426, 4.885442812997680129, 4.978625645943139943, 5.071808478888599758, 5.164991311834059573, 5.258174144779520276, 5.351356977724980091, 5.444539810670439905, 5.537722643615899720, 5.630905476561360423, 5.724088309506820238, 5.817271142452280053, 5.910453975397739868, 6.003636808343199682, 6.096819641288659497, 6.190002474234119312, 6.283185307179590673 ),
 .UNSPECIFIED. ) ;
#16090=CARTESIAN_POINT ( 'NONE',  ( -2.121170185508219230, -1.936412895153350133, 3.105085978143999448 ) ) ;
#16091=CARTESIAN_POINT ( 'NONE',  ( 0.4904671284965613776, -0.6606104644819267291, 2.692290850878278796 ) ) ;
#16093=CARTESIAN_POINT ( 'NONE',  ( -2.276802572547989900, -3.104668185927729862, 4.104251954998810348 ) ) ;
#16094=CARTESIAN_POINT ( 'NONE',  ( 1.449568901432419343, -5.037500000000000533, 3.250431098567584165 ) ) ;
#16096=CARTESIAN_POINT ( 'NONE',  ( -1.722199153441400066, -5.095857339597789526, 3.099360556065549943 ) ) ;
#16100=CARTESIAN_POINT ( 'NONE',  ( 2.191755591049679541, -5.346398305084745672, 3.203650300307709475 ) ) ;
#16102=CARTESIAN_POINT ( 'NONE',  ( 1.315859850362970151, -5.328211948015590060, 2.737664967889629875 ) ) ;
#16107=CARTESIAN_POINT ( 'NONE',  ( -0.8429265834919730249, -2.076142624883080323, 2.502678798553459760 ) ) ;
#16112=CARTESIAN_POINT ( 'NONE',  ( -0.03714311608457869507, -4.521412895153340550, 7.053160869216429596 ) ) ;
#16113=CARTESIAN_POINT ( 'NONE',  ( 0.1352600594606461204, -4.199217735477280833, 6.748562071049542865 ) ) ;
#16118=CARTESIAN_POINT ( 'NONE',  ( 1.614765845140360589, -0.1067796610169500227, 5.967758800287426446 ) ) ;
#16119=CARTESIAN_POINT ( 'NONE',  ( -0.7435598031058080482, -3.030962444702889780, 6.932904947974540377 ) ) ;
#16126=CARTESIAN_POINT ( 'NONE',  ( -2.130266475405059090, -5.255508474576275901, 3.117337770017961418 ) ) ;
#16131=CARTESIAN_POINT ( 'NONE',  ( 1.065036425888030713, -4.381683165423609694, 6.455163597548602361 ) ) ;
#16132=CARTESIAN_POINT ( 'NONE',  ( 1.925836318347889931, -0.1112288135593229726, 6.525927015348126581 ) ) ;
#16134=CARTESIAN_POINT ( 'NONE',  ( 1.057242234132090175, -0.3222457627118650025, 2.597442975781520058 ) ) ;
#16135=CARTESIAN_POINT ( 'NONE',  ( -0.9707742057416274273, -0.4735169491525429986, 6.508944043303927174 ) ) ;
#16136=CARTESIAN_POINT ( 'NONE',  ( -2.578017356471871135, -0.5135593220338985354, 5.329826563567776176 ) ) ;
#16138=CARTESIAN_POINT ( 'NONE',  ( -2.180207327701300102, -5.506567796610169374, 5.586116916730199833 ) ) ;
#16144=CARTESIAN_POINT ( 'NONE',  ( 1.945845091385960401, -3.939205687946139900, 2.895339208235789830 ) ) ;
#16147=CARTESIAN_POINT ( 'NONE',  ( -2.337178851518210365, -3.011515032774580103, 4.976298214796809560 ) ) ;
#16151=CARTESIAN_POINT ( 'NONE',  ( 2.045969882616350155, -3.803316834576382366, 4.529973290172005562 ) ) ;
#16154=CARTESIAN_POINT ( 'NONE',  ( 0.7778405029480717214, -0.9854339516935015642, 6.599964735094206780 ) ) ;
#16155=EDGE_LOOP ( 'NONE', ( #13055, #7348 ) ) ;
#16158=CARTESIAN_POINT ( 'NONE',  ( -1.947945325730720434, -1.288181699441250050, 6.502393603230366637 ) ) ;
#16164=CARTESIAN_POINT ( 'NONE',  ( -1.707817112497179934, -5.188771186440679806, 6.319218296629480314 ) ) ;
#16175=CARTESIAN_POINT ( 'NONE',  ( 0.5803392541454069908, -5.011796459788057767, 2.403119802722881282 ) ) ;
#16176=CARTESIAN_POINT ( 'NONE',  ( 1.901407128523888934, -2.751502985243430288, 6.551422324754781812 ) ) ;
#16179=CARTESIAN_POINT ( 'NONE',  ( -0.8748826269293140667, -3.337551068810609589, 2.515205712983220376 ) ) ;
#16182=CARTESIAN_POINT ( 'NONE',  ( 1.032615103526660416, -1.284340823081270733, 7.144753513336372208 ) ) ;
#16190=CARTESIAN_POINT ( 'NONE',  ( 2.651721837666119796, -5.373093220338980736, 4.594045830208265180 ) ) ;
#16199=CARTESIAN_POINT ( 'NONE',  ( -2.316639661709700260, -1.819971453711900056, 4.285359956977770501 ) ) ;
#16201=CARTESIAN_POINT ( 'NONE',  ( -1.194742379459959869, -5.475423728813559876, 6.727584234649759409 ) ) ;
#16203=CARTESIAN_POINT ( 'NONE',  ( -2.353343516942199898, -1.773394877135329839, 4.722803042560189901 ) ) ;
#16204=CARTESIAN_POINT ( 'NONE',  ( 1.026235786675480099, -4.404971453711899798, 6.817920158464540137 ) ) ;
#16206=CARTESIAN_POINT ( 'NONE',  ( 0.8014931112107362976, -1.284340823081270733, 6.590108630558003000 ) ) ;
#16208=CARTESIAN_POINT ( 'NONE',  ( 1.000896394980339998, -0.4290254237288140260, 6.829956240957369751 ) ) ;
#16212=CARTESIAN_POINT ( 'NONE',  ( 1.557365740149800226, -0.6207580293448360376, 3.145669832173699998 ) ) ;
#16214=CARTESIAN_POINT ( 'NONE',  ( 1.401708661791409849, -4.358394877135329359, 6.590491606684049763 ) ) ;
#16220=CIRCLE ( 'NONE', #9420, 0.1500000000000000777 ) ;
#16221=CARTESIAN_POINT ( 'NONE',  ( -1.192209327851089240, -5.277754237288146300, 2.329031440774910422 ) ) ;
#16222=CARTESIAN_POINT ( 'NONE',  ( -1.477796163681079911, -0.4824152542372879826, 6.531563725478150673 ) ) ;
#16223=ORIENTED_EDGE ( 'NONE', *, *, #874, .T. ) ;
#16225=CARTESIAN_POINT ( 'NONE',  ( -1.865240315818168959, -3.450151633892079239, 3.842223568244830467 ) ) ;
#16226=CARTESIAN_POINT ( 'NONE',  ( -0.7998959936908373036, -0.4646186440677965712, 7.230419212249866945 ) ) ;
#16228=CARTESIAN_POINT ( 'NONE',  ( 1.428515267734870031, -0.3311440677966109858, 2.829745655876919841 ) ) ;
#16229=CARTESIAN_POINT ( 'NONE',  ( 1.596341326794969984, -0.3355932203389830337, 2.970780074643809776 ) ) ;
#16232=CARTESIAN_POINT ( 'NONE',  ( -0.3171869470818471370, -0.4557203389830515317, 7.334814496515233095 ) ) ;
#16234=CARTESIAN_POINT ( 'NONE',  ( 0.9150601050661639757, -5.430932203389830626, 6.868218666554230190 ) ) ;
#16237=CARTESIAN_POINT ( 'NONE',  ( 0.7093417302541469294, -5.435381355932199732, 6.943956659919690466 ) ) ;
#16238=CARTESIAN_POINT ( 'NONE',  ( -2.574214976178951009, -3.403575057315514130, 4.054607910322786779 ) ) ;
#16240=CARTESIAN_POINT ( 'NONE',  ( -0.4446501070882830087, -4.952022267818760426, 2.379695998155090031 ) ) ;
#16242=CARTESIAN_POINT ( 'NONE',  ( 0.3159454637157339540, -2.615614131873679860, 7.032150113402090064 ) ) ;
#16245=CARTESIAN_POINT ( 'NONE',  ( 1.203420131881999477, -4.059488005747546424, 6.363334551077796775 ) ) ;
#16248=CARTESIAN_POINT ( 'NONE',  ( 1.937109463115360253, -2.173136654396201184, 4.019920026366761157 ) ) ;
#16252=CARTESIAN_POINT ( 'NONE',  ( -0.009452110982655099330, -0.5998079552954631577, 2.649999999999998579 ) ) ;
#16253=CARTESIAN_POINT ( 'NONE',  ( 2.501774541437309374, -0.7758393570989061683, 5.585572039315881199 ) ) ;
#16260=CARTESIAN_POINT ( 'NONE',  ( -1.889104232906369862, -5.255508474576269684, 3.296507079072529933 ) ) ;
#16267=CARTESIAN_POINT ( 'NONE',  ( -1.526871680339578541, -5.559957627118640389, 3.327650196883449762 ) ) ;
#16268=CARTESIAN_POINT ( 'NONE',  ( -1.524497189778160289, -2.801920438179980710, 6.872331008700187205 ) ) ;
#16269=CARTESIAN_POINT ( 'NONE',  ( 1.319613955262859850, -5.028306595106927901, 2.740497729816110173 ) ) ;
#16270=CARTESIAN_POINT ( 'NONE',  ( 2.647661051184980519, -2.541908390648840665, 4.518328177639069132 ) ) ;
#16274=CARTESIAN_POINT ( 'NONE',  ( 0.3752419433107369584, -4.175929447188989840, 7.023346545710360544 ) ) ;
#16277=CARTESIAN_POINT ( 'NONE',  ( 1.315254646989809872, -2.821367850108300157, 7.005042061779697349 ) ) ;
#16281=CARTESIAN_POINT ( 'NONE',  ( 0.4360591020457930123, -0.3088983050847460277, 2.387347919655840034 ) ) ;
#16283=CARTESIAN_POINT ( 'NONE',  ( 0.2818998297622880012, -1.354205687946139935, 7.036509827384409554 ) ) ;
#16284=CARTESIAN_POINT ( 'NONE',  ( -1.661700935788390066, -0.5625000000000000000, 3.038299064211610112 ) ) ;
#16294=CARTESIAN_POINT ( 'NONE',  ( 0.7678268402137939930, -2.867944426684879922, 6.924676972266129660 ) ) ;
#16297=CARTESIAN_POINT ( 'NONE',  ( -0.8570167067220350043, -5.582203389830509899, 2.508190348879359988 ) ) ;
#16299=CARTESIAN_POINT ( 'NONE',  ( 0.3413183941262679655, -2.914521003261450360, 7.028571974690709823 ) ) ;
#16300=CARTESIAN_POINT ( 'NONE',  ( 2.260890494820590124, -4.055647129387580208, 4.046455925041149371 ) ) ;
#16301=CARTESIAN_POINT ( 'NONE',  ( 2.052456847059610734, -2.565196678937129438, 4.748194746458525017 ) ) ;
#16307=CARTESIAN_POINT ( 'NONE',  ( 2.100188519621589922, -4.009070552810999999, 3.637948273607370275 ) ) ;
#16315=CARTESIAN_POINT ( 'NONE',  ( -0.2469343877495291661, -5.295550847457634269, 2.057675570509529539 ) ) ;
#16320=CARTESIAN_POINT ( 'NONE',  ( 1.632144308286169965, -4.288530012270460823, 5.945394234592866312 ) ) ;
#16321=CARTESIAN_POINT ( 'NONE',  ( 1.128670402850170174, -0.4290254237288141370, 7.101865548313628373 ) ) ;
#16324=CARTESIAN_POINT ( 'NONE',  ( -2.578017356471871135, -0.2135593220338991571, 5.329826563567776176 ) ) ;
#16326=CARTESIAN_POINT ( 'NONE',  ( -0.3743405594629430344, -5.457627118644070130, 7.023440622744399953 ) ) ;
#16327=CARTESIAN_POINT ( 'NONE',  ( 1.670747152266691016, -0.4963810343603142217, 3.047345280935851441 ) ) ;
#16328=CARTESIAN_POINT ( 'NONE',  ( -0.009452110982655708218, -0.5998079552954630467, 2.350000000000000089 ) ) ;
#16329=CARTESIAN_POINT ( 'NONE',  ( 1.882879255550339082, -0.4963798976394455664, 2.835213315261639000 ) ) ;
#16333=CARTESIAN_POINT ( 'NONE',  ( -1.928817277882840076, -4.455388906648449776, 6.048484184565969812 ) ) ;
#16336=CARTESIAN_POINT ( 'NONE',  ( 1.043047520545210105, -4.082776294035843634, 6.468319459971126228 ) ) ;
#16339=CARTESIAN_POINT ( 'NONE',  ( 0.2302241296434710538, -1.893677194936738806, 2.659926792304259990 ) ) ;
#16343=CARTESIAN_POINT ( 'NONE',  ( 0.1953673232040119001, -0.6247245358507567126, 2.648920247487680513 ) ) ;
#16344=CARTESIAN_POINT ( 'NONE',  ( -0.6265155281652096120, -2.708767285026830951, 7.278874170247493502 ) ) ;
#16345=ORIENTED_EDGE ( 'NONE', *, *, #4313, .F. ) ;
#16347=CARTESIAN_POINT ( 'NONE',  ( -1.197297565406129971, -1.517223705964160008, 6.726135293448209929 ) ) ;
#16348=CARTESIAN_POINT ( 'NONE',  ( -1.670747221194380128, -5.103620102360550526, 3.047345349617600174 ) ) ;
#16350=CARTESIAN_POINT ( 'NONE',  ( 0.2812789908084389889, -5.144279661016950556, 7.036533610117280624 ) ) ;
#16357=CARTESIAN_POINT ( 'NONE',  ( -2.180207327701300102, -5.506567796610169374, 5.586116916730199833 ) ) ;
#16358=CARTESIAN_POINT ( 'NONE',  ( 1.392767620582681332, -3.570433951693503527, 2.440948861123688474 ) ) ;
#16359=CARTESIAN_POINT ( 'NONE',  ( 1.327748599278329777, -0.4480353997208160188, 2.745754414290000334 ) ) ;
#16360=CARTESIAN_POINT ( 'NONE',  ( -0.7785957873162068221, -3.659746228486683073, 2.162894899107379754 ) ) ;
#16362=MECHANICAL_DESIGN_GEOMETRIC_PRESENTATION_REPRESENTATION('',(#6009),#3028);
#16365=CARTESIAN_POINT ( 'NONE',  ( -1.265407828724339989, -3.290974492234040483, 2.715689360385570073 ) ) ;
#16368=CARTESIAN_POINT ( 'NONE',  ( 2.065789008933020199, -2.728214696955149510, 6.366022047745297563 ) ) ;
#16371=CARTESIAN_POINT ( 'NONE',  ( 0.07299321914061039640, -0.3014830508474579673, 2.350000000000000089 ) ) ;
#16372=CARTESIAN_POINT ( 'NONE',  ( -1.854177340199669954, -1.610376859117309989, 6.149404042554720284 ) ) ;
#16373=CARTESIAN_POINT ( 'NONE',  ( -2.286166334984490067, -0.5135593220338989795, 5.258525443163870605 ) ) ;
#16374=CARTESIAN_POINT ( 'NONE',  ( -0.4478021372196528960, -0.2909039927201509945, 2.380136890750930156 ) ) ;
#16375=CARTESIAN_POINT ( 'NONE',  ( 2.416676968769261080, -5.395338983050850246, 5.796598111919825769 ) ) ;
#16383=CARTESIAN_POINT ( 'NONE',  ( -1.741913176380149864, -1.959701183441629802, 3.117443785062560035 ) ) ;
#16390=CARTESIAN_POINT ( 'NONE',  ( 2.301223891756920104, -2.611773255513699876, 5.193066210047949660 ) ) ;
#16392=CARTESIAN_POINT ( 'NONE',  ( -0.8735826871841183561, -1.493935417675870791, 6.557889967484691773 ) ) ;
#16394=CARTESIAN_POINT ( 'NONE',  ( -1.687197751398160861, -0.5672554343907065810, 2.639290338773708999 ) ) ;
#16396=CARTESIAN_POINT ( 'NONE',  ( 1.635135312535000107, -0.5029574999466160934, 3.082160985277540011 ) ) ;
#16403=CARTESIAN_POINT ( 'NONE',  ( -2.287919158821179799, -4.548542059801598647, 5.251517552016938595 ) ) ;
#16404=CARTESIAN_POINT ( 'NONE',  ( 1.943632316591230147, -5.046398305084740521, 3.373048379518159834 ) ) ;
#16407=CARTESIAN_POINT ( 'NONE',  ( -2.035218756299248977, -4.781424942684484591, 2.996768277952679860 ) ) ;
#16409=CARTESIAN_POINT ( 'NONE',  ( -2.308170020371289599, -1.726818300558750074, 5.159452766389659217 ) ) ;
#16410=CARTESIAN_POINT ( 'NONE',  ( 1.750316316486830059, -0.04004237288135630013, 3.126818518378580158 ) ) ;
#16413=CARTESIAN_POINT ( 'NONE',  ( -0.7998959936908373036, -0.1646186440677970542, 7.230419212249866945 ) ) ;
#16417=CARTESIAN_POINT ( 'NONE',  ( 2.239137794397009440, -0.6128213390808880945, 3.975425900939169921 ) ) ;
#16418=CARTESIAN_POINT ( 'NONE',  ( -0.1565249325564300187, -5.453177966101690366, 7.048192310558509810 ) ) ;
#16420=CARTESIAN_POINT ( 'NONE',  ( -2.159308672244651284, -4.754295778036219389, 6.242886823772542115 ) ) ;
#16424=CARTESIAN_POINT ( 'NONE',  ( -2.350542563031990273, -4.595118636378179744, 4.817027120179790067 ) ) ;
#16425=CARTESIAN_POINT ( 'NONE',  ( -2.632587027711260852, -4.940602084342534894, 4.364441905910590336 ) ) ;
#16428=CARTESIAN_POINT ( 'NONE',  ( -1.436030008293460503, -4.408812330071866015, 6.167214932417466322 ) ) ;
#16431=CARTESIAN_POINT ( 'NONE',  ( 2.002297259025890064, -2.312866384125929820, 5.153549919110900213 ) ) ;
#16437=CARTESIAN_POINT ( 'NONE',  ( 2.623186471072028514, -2.219713230972778728, 4.297499775172036962 ) ) ;
#16438=EDGE_LOOP ( 'NONE', ( #13678, #7740, #11209, #6033 ) ) ;
#16441=CARTESIAN_POINT ( 'NONE',  ( 1.432215783582721613, -5.113135593220339281, 6.170863372171116801 ) ) ;
#16447=CARTESIAN_POINT ( 'NONE',  ( 2.286166334984490067, -5.386440677966100488, 5.258525443163859947 ) ) ;
#16448=CARTESIAN_POINT ( 'NONE',  ( 2.644456467089558949, -3.803316834576382366, 4.476474416072626639 ) ) ;
#16453=CARTESIAN_POINT ( 'NONE',  ( -1.074829861819750043, -3.314262780522330143, 2.606322265575609975 ) ) ;
#16457=CARTESIAN_POINT ( 'NONE',  ( 0.2683982510036849733, -2.192584066324520187, 2.059720455735791322 ) ) ;
#16461=CARTESIAN_POINT ( 'NONE',  ( 2.126557263589630153, -2.448755237495689574, 3.691783806836010040 ) ) ;
#16463=CARTESIAN_POINT ( 'NONE',  ( 0.009303514085960742572, -5.002547179689483592, 2.316528937223460982 ) ) ;
#16465=CARTESIAN_POINT ( 'NONE',  ( -1.596341326794979976, -5.564406779661021041, 2.970780074643819990 ) ) ;
#16472=CARTESIAN_POINT ( 'NONE',  ( -1.286937324407759986, -3.589881363621809651, 2.729584305145209999 ) ) ;
#16479=CARTESIAN_POINT ( 'NONE',  ( -1.236334101859210000, -2.029566048306499670, 2.697445712080720259 ) ) ;
#16482=CARTESIAN_POINT ( 'NONE',  ( -1.616473591439278712, -1.610376859117309767, 5.965667796385567101 ) ) ;
#16486=CARTESIAN_POINT ( 'NONE',  ( -0.4478021372196530070, -0.2909039927201509945, 2.380136890750930156 ) ) ;
#16500=CARTESIAN_POINT ( 'NONE',  ( -1.194742379459959869, -5.175423728813560054, 6.727584234649759409 ) ) ;
#16504=CARTESIAN_POINT ( 'NONE',  ( 2.135041058613650122, -0.7991276453871950514, 5.690123914223769397 ) ) ;
#16507=CARTESIAN_POINT ( 'NONE',  ( 2.351212046067109984, -0.9815930753335269099, 4.597298481426010497 ) ) ;
#16508=CARTESIAN_POINT ( 'NONE',  ( -1.851400890972779045, -0.1868644067796610686, 6.601359968904141340 ) ) ;
#16511=CARTESIAN_POINT ( 'NONE',  ( 2.318251751302029984, -0.3667372881355940306, 4.294764266798990704 ) ) ;
#16512=CARTESIAN_POINT ( 'NONE',  ( -1.713314936023349944, -0.5610169491525430763, 3.089913064446579760 ) ) ;
#16514=CARTESIAN_POINT ( 'NONE',  ( -1.031876288691620625, -0.1690677966101698793, 7.145012538880312292 ) ) ;
#16521=CARTESIAN_POINT ( 'NONE',  ( -2.260890494820599450, -1.544352870612419881, 4.046455925041200885 ) ) ;
#16523=CARTESIAN_POINT ( 'NONE',  ( 0.9150601050661639757, -5.430932203389830626, 6.868218666554230190 ) ) ;
#16524=CARTESIAN_POINT ( 'NONE',  ( -2.524473153133541814, -4.987178660919110662, 3.881373716577405819 ) ) ;
#16528=CARTESIAN_POINT ( 'NONE',  ( 2.255259958075439997, -3.896469987729530349, 5.372717034855999607 ) ) ;
#16529=CARTESIAN_POINT ( 'NONE',  ( -2.573461662271331551, -4.847448931189385135, 5.348389362822530302 ) ) ;
#16533=CARTESIAN_POINT ( 'NONE',  ( -1.790316459643189972, -4.734848366107908824, 3.695177221627210074 ) ) ;
#16539=CARTESIAN_POINT ( 'NONE',  ( -1.449568901432419343, -0.2625000000000002331, 3.250431098567584165 ) ) ;
#16542=CARTESIAN_POINT ( 'NONE',  ( -0.8642983280852033490, -2.732055573315119723, 7.209203477813437289 ) ) ;
#16545=CARTESIAN_POINT ( 'NONE',  ( -3.503171016405825766E-15, -5.300000000000000711, 2.649999999999998579 ) ) ;
#16548=CARTESIAN_POINT ( 'NONE',  ( 2.293398556041700065, -5.364194915254239859, 4.171956209133470317 ) ) ;
#16552=CARTESIAN_POINT ( 'NONE',  ( -2.353194804772640314, -5.524364406779660008, 4.731327187377240229 ) ) ;
#16553=CARTESIAN_POINT ( 'NONE',  ( 1.722199153441390074, -0.5041426604022090086, 3.099360556065540173 ) ) ;
#16556=CARTESIAN_POINT ( 'NONE',  ( -2.018065005288401270, -1.427911429170979352, 5.077247235985114848 ) ) ;
#16559=CARTESIAN_POINT ( 'NONE',  ( 2.594645788401200637, -2.611773255513701653, 5.257608218854235460 ) ) ;
#16563=CARTESIAN_POINT ( 'NONE',  ( 0.009452039534070141164, -0.3001931771041043140, 2.350000000173209092 ) ) ;
#16564=CARTESIAN_POINT ( 'NONE',  ( 2.345900685764729765, -0.3711864406779670222, 4.512231114381330066 ) ) ;
#16565=CARTESIAN_POINT ( 'NONE',  ( 2.211317922628870392, -2.472043525783979678, 3.894507149290419967 ) ) ;
#16566=CARTESIAN_POINT ( 'NONE',  ( 0.008535039157538009888, -5.014726856582200298, 2.281464080633750058 ) ) ;
#16568=CARTESIAN_POINT ( 'NONE',  ( -0.08231150243516484333, -5.598516949152545941, 2.050000000000001155 ) ) ;
#16572=CARTESIAN_POINT ( 'NONE',  ( 1.112838723655039885, -5.126483050847459033, 6.773667561836209217 ) ) ;
#16574=CARTESIAN_POINT ( 'NONE',  ( -0.005674314996646560166, -0.5399330878477630602, 2.472195840738689920 ) ) ;
#16578=CARTESIAN_POINT ( 'NONE',  ( 2.342931736853870017, -4.102223705964150646, 4.477701633099130163 ) ) ;
#16580=CARTESIAN_POINT ( 'NONE',  ( 1.112838723655040107, -5.426483050847459744, 6.773667561836210105 ) ) ;
#16582=CARTESIAN_POINT ( 'NONE',  ( -1.948278411993560111, -3.193980462720909852, 6.020210936496040333 ) ) ;
#16586=CARTESIAN_POINT ( 'NONE',  ( -0.9290506585603975909, -0.5829339996946386604, 2.210445150547709403 ) ) ;
#16589=SURFACE_STYLE_USAGE ( .BOTH. , #2338 ) ;
#16594=( BOUNDED_SURFACE ( )  B_SPLINE_SURFACE ( 3, 3, ( 
 ( #11861, #10278, #4891, #17206, #4529, #9056, #4799, #9155, #8804, #17479, #14456, #7687, #464, #7422, #13063, #3408, #383, #8890, #14541, #1938, #1857, #17560, #11771, #7504, #14713, #7777, #2032, #6023, #3331, #11668, #13151, #14623, #13332, #15947, #6107, #8976, #17398, #4716, #645, #10365, #7589, #6283, #11943, #16203, #3512, #14818, #5379, #2427, #6762, #12038, #17661, #9254, #3605, #3794, #16479, #12139, #8249, #12320, #12412, #17759, #14913, #6662, #5184, #16667, #15198, #18034, #2222, #1025, #5090, #5001, #6372, #17939, #15113, #11018, #7869, #5284, #737, #7976, #10742, #16390, #13624, #13520, #838, #3973, #6480, #1117, #3692, #9625, #9340, #15010, #10652, #15285, #16299, #2327, #935, #6573, #12227, #2597, #10935, #17846, #10833, #9451, #8072, #13712, #16582, #3888, #9542, #2506, #8153, #13792, #17016, #13891, #5464, #11102, #18115, #14168, #1206, #15472, #1487, #3049, #1379, #2780, #16749, #4333, #5557, #12863, #15663, #2869, #1575, #7045, #10000, #6854, #12500, #12781, #7221, #14061, #175, #17108, #5822, #12585, #11473, #7144, #16932, #4063, #9720, #4242, #15743, #4432, #5652, #8424, #8519, #9904, #15389, #10091, #12688, #2687, #18200, #15561, #95, #11296, #2972, #8340, #6938, #5738, #13973, #10, #1294, #11383, #8613, #14256, #11202, #16847, #4158, #9814, #13217, #7666, #4592, #4873, #1756, #11645, #15824, #3229, #539, #8961, #2011, #14693, #16096, #17272 ),
 ( #278, #10519, #1921, #1844, #17190, #14433, #13311, #7404, #3127, #16016, #11841, #10433, #7487, #13043, #13135, #6185, #11925, #17464, #4783, #10164, #8874, #3391, #16182, #8691, #9036, #14605, #8779, #364, #6002, #6089, #10350, #11742, #17376, #7305, #12953, #10251, #15918, #14523, #7570, #5919, #627, #11559, #6266, #447, #17543, #4697, #14337, #3317, #1656, #4514, #916, #12121, #6455, #9320, #5160, #12016, #10810, #10915, #17740, #6639, #717, #16457, #4974, #2106, #7956, #5068, #3672, #13402, #10720, #6554, #815, #3582, #12207, #9229, #1002, #3868, #3488, #3770, #17823, #16559, #9133, #9430, #14792, #13694, #16368, #6351, #10629, #15094, #16277, #14990, #2303, #2405, #13601, #5261, #8052, #12296, #17916, #7757, #17636, #14891, #2204, #7848, #13498, #10402, #10485, #14495, #7460, #4751, #419, #3287, #14754, #8848, #6055, #16238, #4840, #11704, #7722, #13182, #6318, #3360, #13366, #13014, #337, #10218, #4562, #16062, #17433, #13105, #9191, #13278, #679, #17336, #15884, #7632, #6149, #17592, #16144, #11980, #3195, #1970, #4666, #5972, #7375, #596, #9003, #4930, #1817, #6235, #1723, #8930, #10321, #15984, #14575, #1891, #7538, #10585, #498, #2068, #11808, #3544, #14656, #11895, #11616, #17243, #17514, #3445, #9093, #10686, #2169, #2534, #13559, #16420, #9572, #3634, #875, #11048, #17979, #6514, #8184, #8011, #1153, #16524, #13834, #7810, #13457, #5030, #17698, #17879 ),
 ( #16329, #2454, #965, #12448, #10970, #6800, #9285, #15143, #7911, #774, #6406, #8101, #10874, #18065, #14948, #1058, #14853, #3726, #12171, #17788, #9387, #2258, #5125, #5408, #10775, #15230, #15055, #16697, #2361, #13655, #12077, #4006, #6603, #12261, #5216, #3834, #9482, #13740, #6698, #12356, #5324, #16615, #3916, #5477, #12600, #9741, #12707, #18220, #6953, #2795, #16949, #13909, #15575, #5392, #5575, #9638, #15304, #2887, #11117, #8267, #1399, #16864, #4172, #1223, #8439, #24, #14073, #16764, #5669, #15404, #2709, #11311, #14187, #1503, #6343, #10712, #7235, #708, #14981, #9218, #1771, #12879, #15756, #12007, #3063, #4526, #10178, #3479, #15842, #804, #13059, #3140, #2097, #3664, #17626, #192, #17287, #8707, #8799, #15941, #16268, #1675, #12969, #10270, #4612, #293, #5837, #4965, #6445, #5931, #14349, #13394, #11662, #5061, #3571, #12112, #7324, #7748, #11571, #11489, #17121, #10620, #9125, #17732, #17202, #14882, #4445, #14450, #7418, #378, #6018, #14781, #2196, #16358, #7840, #13487, #9312, #10105, #2396, #17909, #6546, #8314, #7947, #16448, #10908, #3759, #13593, #13952, #1180, #13762, #18173, #6631, #2661, #15086, #2482, #12288, #2560, #8126, #9513, #18006, #6828, #9422, #18090, #16819, #15172, #6913, #5152, #5437, #8045, #12199, #9599, #1084, #12386, #17815, #6731, #8215, #3860, #994, #13863, #5251, #1269, #9788, #2293, #11078, #12472, #5524, #908, #16721 ),
 ( #13686, #16553, #5350, #10994, #4032, #9687, #12561, #11169, #15359, #16642, #3946, #15255, #4131, #10802, #2759, #12753, #7008, #17246, #14313, #8584, #5625, #2839, #3104, #8487, #9879, #4406, #251, #17167, #14229, #14134, #1549, #1634, #339, #12924, #5891, #16910, #9970, #7280, #4565, #1353, #10064, #15635, #7196, #12659, #2943, #3021, #16993, #1459, #11533, #7114, #14400, #15450, #8401, #4486, #10140, #5975, #14038, #15796, #18281, #8751, #12837, #11268, #4219, #1728, #15538, #68, #5714, #11441, #11360, #7379, #150, #4306, #15718, #11618, #13017, #5797, #17078, #6057, #500, #599, #681, #4670, #15986, #13281, #8932, #11811, #4934, #17338, #14579, #6410, #13369, #1895, #16242, #3363, #14857, #11897, #3547, #3199, #8851, #421, #13108, #6238, #7635, #3289, #17702, #3447, #9194, #7540, #11706, #16147, #14658, #7814, #6320, #2173, #10325, #10488, #13184, #14497, #15886, #9096, #17516, #13460, #6152, #14758, #10220, #17436, #4753, #10404, #16064, #9006, #1972, #777, #4842, #10588, #2070, #12082, #7725, #11983, #1819, #7462, #17596, #880, #13658, #6517, #10689, #11052, #3921, #16528, #2640, #9391, #5413, #17792, #5220, #15059, #5328, #10877, #12264, #2458, #9575, #12174, #2537, #1247, #17882, #9661, #7914, #8187, #5128, #3838, #15333, #6702, #16700, #16333, #3637, #13564, #10778, #8104, #13743, #16424, #12537, #16619, #4009, #3729, #2366, #10973, #9486, #8291, #1157, #13930 ),
 ( #1061, #6890, #8016, #15233, #5033, #15147, #969, #6606, #12360, #17982, #13837, #9289, #6804, #14951, #12451, #2261, #18068, #4850, #11817, #13574, #13191, #3369, #16154, #9012, #508, #888, #6421, #690, #5135, #11902, #7923, #1979, #7731, #17521, #7822, #13375, #14764, #4943, #12091, #14664, #5040, #3738, #2077, #12180, #10409, #10696, #7641, #17441, #14864, #6326, #17606, #4759, #11990, #13467, #9104, #6243, #785, #10495, #6524, #15067, #7545, #16339, #17709, #10786, #6161, #3643, #16071, #9294, #10596, #13286, #604, #14960, #3454, #16248, #3553, #9200, #2179, #17798, #2269, #16431, #9399, #17129, #14194, #2375, #12715, #16776, #11227, #11321, #11405, #15413, #8362, #5677, #1314, #4180, #15684, #9748, #6961, #4454, #5763, #12610, #8634, #1512, #8024, #32, #4089, #16872, #16957, #17037, #2717, #13995, #4265, #18232, #9839, #2994, #5583, #15493, #10112, #4363, #2802, #14279, #14081, #7246, #9924, #1602, #13664, #976, #10884, #5229, #15586, #2899, #8447, #6613, #7165, #12886, #1411, #7073, #8547, #12803, #203, #10025, #5848, #117, #11498, #12270, #17890, #3071, #16033, #11774, #7689, #11577, #1940, #15764, #4622, #14459, #8808, #10282, #17209, #4532, #647, #10184, #16113, #15849, #2034, #3151, #13066, #1683, #3410, #8715, #1778, #6026, #7426, #14359, #9059, #14625, #8894, #13335, #386, #14716, #11671, #15950, #17294, #3333, #3250, #14543, #13152, #7592, #1859, #13243 ),
 ( #7333, #4718, #7506, #466, #12978, #6110, #8978, #17400, #10368, #564, #6208, #6285, #4893, #300, #11864, #17481, #11945, #5939, #4801, #10452, #17562, #5092, #16206, #739, #15115, #6374, #7871, #13524, #6575, #842, #3890, #16392, #6482, #5187, #6766, #12229, #16482, #2331, #6665, #12041, #3608, #2429, #9544, #15012, #3514, #9342, #12141, #10937, #2508, #9157, #17664, #1120, #8074, #15201, #17761, #12414, #9257, #10744, #5003, #3695, #13714, #10835, #8155, #13796, #17942, #7978, #13626, #937, #18036, #10544, #14820, #17848, #2135, #7778, #3798, #9454, #10654, #16301, #13425, #14915, #2224, #1027, #12322, #5288, #4160, #16751, #9816, #9906, #8615, #2872, #8521, #6856, #18203, #15563, #12865, #5381, #14171, #5655, #18117, #15391, #4066, #2783, #7048, #8426, #14063, #3975, #9627, #8342, #2689, #11104, #16934, #15288, #4244, #2602, #8253, #16851, #1489, #11020, #13893, #1208, #12502, #11298, #16670, #6940, #7146, #5466, #11206, #12587, #9725, #12784, #13975, #4336, #97, #12692, #11385, #15474, #5740, #1296, #5560, #17018, #10002, #1381, #15666, #14258, #2974, #12, #1579, #7223, #3232, #178, #4435, #8876, #7670, #5824, #10253, #13046, #13137, #14526, #15745, #11475, #366, #10093, #4516, #3051, #16018, #3319, #1659, #6004, #4700, #8696, #14339, #10352, #449, #12955, #10167, #11561, #15921, #1846, #7489, #6091, #7307, #282, #3129, #15828, #5921, #11747, #17192, #17379 ),
 ( #8782, #14436, #11648, #1759, #17274, #4596, #8963, #14608, #1923, #13219, #8637, #1688, #9932, #1784, #9141, #17642, #12125, #4979, #14801, #9524, #2409, #14993, #1095, #7852, #3872, #16283, #3677, #13503, #3776, #9324, #10726, #920, #8056, #10634, #1009, #18015, #16372, #8139, #6356, #6645, #3588, #7763, #10814, #2311, #13606, #721, #7961, #9436, #5075, #2208, #15099, #821, #2491, #3494, #2111, #12300, #13698, #6744, #13408, #17921, #12021, #5267, #6558, #9233, #14896, #10920, #6461, #17744, #12213, #17829, #5163, #15183, #16461, #16565, #13774, #5362, #12396, #16652, #8410, #12482, #6922, #7022, #7127, #11088, #4046, #1362, #15368, #18182, #11367, #5447, #2671, #12845, #1468, #8324, #4316, #9797, #2953, #9887, #5805, #76, #11184, #3958, #6838, #2850, #18100, #13959, #1279, #12669, #12569, #15646, #4139, #5536, #11277, #159, #8497, #9608, #14046, #16729, #16829, #10040, #12763, #9701, #15457, #5634, #2765, #16918, #17000, #4227, #14147, #15269, #5721, #8593, #14240, #1558, #7203, #2574, #8227, #13874, #1189, #1641, #14321, #14507, #8859, #4495, #611, #4681, #4765, #10150, #7288, #17352, #15900, #9019, #7551, #10417, #12934, #11719, #15805, #10075, #17089, #10335, #7471, #3375, #263, #15998, #11454, #348, #3111, #8763, #5987, #5900, #11542, #14669, #17175, #11824, #14413, #16078, #1738, #7388, #15727, #17447, #4416, #13025, #11627, #17257, #3032, #1988, #3301, #4573 ) ),
 .UNSPECIFIED., .T., .F., .F. ) 
 B_SPLINE_SURFACE_WITH_KNOTS ( ( 4, 3, 4 ),
 ( 4, 1, 1, 1, 1, 1, 1, 1, 1, 1, 1, 1, 1, 1, 1, 1, 1, 1, 1, 1, 1, 1, 1, 1, 1, 1, 1, 1, 1, 1, 1, 1, 1, 1, 1, 1, 1, 1, 1, 1, 1, 1, 1, 1, 1, 1, 1, 1, 1, 1, 1, 1, 1, 1, 1, 1, 1, 1, 1, 1, 1, 1, 1, 1, 1, 1, 1, 1, 1, 1, 1, 1, 1, 1, 1, 1, 1, 1, 1, 1, 1, 1, 1, 1, 1, 1, 1, 1, 1, 1, 1, 1, 1, 1, 1, 1, 1, 1, 1, 1, 1, 1, 1, 1, 1, 1, 1, 1, 1, 1, 1, 1, 1, 1, 1, 1, 1, 1, 1, 1, 1, 1, 1, 1, 1, 1, 1, 1, 1, 1, 1, 1, 1, 1, 1, 1, 1, 1, 1, 1, 1, 1, 1, 1, 1, 1, 1, 1, 1, 1, 1, 1, 1, 1, 1, 1, 1, 1, 1, 1, 1, 1, 1, 1, 1, 1, 1, 1, 1, 1, 1, 1, 1, 1, 1, 1, 1, 1, 1, 1, 1, 1, 1, 1, 1, 4 ),
 ( 0.000000000000000000, 3.141592653589790007, 6.283185307179590673 ),
 ( 0.7853981633974479459, 0.8787968639095770085, 0.9721955644217059600, 1.065594264933839908, 1.158992965445959866, 1.252391665958090039, 1.345790366470219990, 1.439189066982349940, 1.532587767494480113, 1.625986468006610064, 1.719385168518740015, 1.812783869030869965, 1.906182569543000138, 1.999581270055129867, 2.092979970567249826, 2.186378671079379998, 2.279777371591510171, 2.373176072103639900, 2.466574772615769628, 2.559973473127900245, 2.653372173640029974, 2.746770874152160147, 2.840169574664289875, 2.933568275176409834, 3.026966975688540007, 3.120365676200670180, 3.213764376712799908, 3.307163077224930081, 3.400561777737059810, 3.493960478249190427, 3.587359178761320155, 3.680757879273439670, 3.774156579785570287, 3.867555280297700016, 3.960953980809830188, 4.054352681321960361, 4.147751381834090090, 4.241150082346219818, 4.334548782858350435, 4.427947483370480164, 4.521346183882600123, 4.614744884394729851, 4.708143584906859580, 4.801542285418989309, 4.894940985931119926, 4.988339686443250542, 5.081738386955380271, 5.175137087467510000, 5.268535787979639728, 5.361934488491760575, 5.455333189003890304, 5.548731889516020033, 5.642130590028149761, 5.735529290540279490, 5.828927991052410107, 5.922326691564539836, 6.015725392076670452, 6.109124092588789523, 6.202522793100920140, 6.295921493613049869, 6.389320194125180485, 6.482718894637310214, 6.576117595149439943, 6.669516295661569671, 6.762914996173699400, 6.856313696685830017, 6.949712397197949976, 7.043111097710079704, 7.136509798222209433, 7.229908498734340050, 7.323307199246470667, 7.416705899758600395, 7.510104600270730124, 7.603503300782859853, 7.696902001294989581, 7.790300701807110428, 7.883699402319240157, 7.977098102831369886, 8.070496803343500503, 8.163895503855631119, 8.257294204367759960, 8.350692904879890577, 8.444091605392019417, 8.537490305904139376, 8.630889006416269993, 8.724287706928398833, 8.817686407440529450, 8.911085107952660067, 9.004483808464788908, 9.097882508976921301, 9.191281209489050141, 9.284679910001178982, 9.378078610513298941, 9.471477311025429557, 9.564876011537560174, 9.658274712049690791, 9.751673412561819632, 9.845072113073950248, 9.938470813586080865, 10.03186951409819905, 10.12526821461029947, 10.21866691512249936, 10.31206561563459978, 10.40546431614669842, 10.49886301665890009, 10.59226171717100051, 10.68566041768310093, 10.77905911819519957, 10.87245781870739947, 10.96585651921949989, 11.05925521973160031, 11.15265392024380020, 11.24605262075590062, 11.33945132126800104, 11.43285002178009968, 11.52624872229229958, 11.61964742280439999, 11.71304612331650041, 11.80644482382869853, 11.89984352434079895, 11.99324222485290115, 12.08664092536500156, 12.18003962587719968, 12.27343832638930010, 12.36683702690140052, 12.46023572741360042, 12.55363442792569906, 12.64703312843779948, 12.74043182894989990, 12.83383052946209979, 12.92722922997419843, 13.02062793048630063, 13.11402663099850052, 13.20742533151059916, 13.30082403202269958, 13.39422273253480000, 13.48762143304700167, 13.58102013355910032, 13.67441883407120073, 13.76781753458340063, 13.86121623509549927, 13.95461493560759969, 14.04801363611970011, 14.14141233663190000, 14.23481103714399865, 14.32820973765609907, 14.42160843816829896, 14.51500713868040116, 14.60840583919249980, 14.70180453970460022, 14.79520324021680011, 14.88860194072889875, 14.98200064124100095, 15.07539934175320084, 15.16879804226530126, 15.26219674277739990, 15.35559544328959980, 15.44899414380170022, 15.54239284431380064, 15.63579154482589928, 15.72919024533809917, 15.82258894585019959, 15.91598764636230001, 16.00938634687449991, 16.10278504738660033, 16.19618374789869719, 16.28958244841080116, 16.38298114892299751, 16.47637984943510148, 16.56977854994720190, 16.66317725045940179, 16.75657595097149866, 16.84997465148359908, 16.94337335199570305, 17.03677205250789939, 17.13017075301999981, 17.22356945353210023, 17.31696815404430012, 17.41036685455640054, 17.50376555506850096, 17.59716425558059782, 17.69056295609280127, 17.78396165660489814, 17.87736035711699856, 17.97075905762920200, 18.06415775814129887 ),
 .UNSPECIFIED. ) 
 GEOMETRIC_REPRESENTATION_ITEM ( )  RATIONAL_B_SPLINE_SURFACE ( (
 ( 1.000000000000000000, 1.000000000000000000, 1.000000000000000000, 1.000000000000000000, 1.000000000000000000, 1.000000000000000000, 1.000000000000000000, 1.000000000000000000, 1.000000000000000000, 1.000000000000000000, 1.000000000000000000, 1.000000000000000000, 1.000000000000000000, 1.000000000000000000, 1.000000000000000000, 1.000000000000000000, 1.000000000000000000, 1.000000000000000000, 1.000000000000000000, 1.000000000000000000, 1.000000000000000000, 1.000000000000000000, 1.000000000000000000, 1.000000000000000000, 1.000000000000000000, 1.000000000000000000, 1.000000000000000000, 1.000000000000000000, 1.000000000000000000, 1.000000000000000000, 1.000000000000000000, 1.000000000000000000, 1.000000000000000000, 1.000000000000000000, 1.000000000000000000, 1.000000000000000000, 1.000000000000000000, 1.000000000000000000, 1.000000000000000000, 1.000000000000000000, 1.000000000000000000, 1.000000000000000000, 1.000000000000000000, 1.000000000000000000, 1.000000000000000000, 1.000000000000000000, 1.000000000000000000, 1.000000000000000000, 1.000000000000000000, 1.000000000000000000, 1.000000000000000000, 1.000000000000000000, 1.000000000000000000, 1.000000000000000000, 1.000000000000000000, 1.000000000000000000, 1.000000000000000000, 1.000000000000000000, 1.000000000000000000, 1.000000000000000000, 1.000000000000000000, 1.000000000000000000, 1.000000000000000000, 1.000000000000000000, 1.000000000000000000, 1.000000000000000000, 1.000000000000000000, 1.000000000000000000, 1.000000000000000000, 1.000000000000000000, 1.000000000000000000, 1.000000000000000000, 1.000000000000000000, 1.000000000000000000, 1.000000000000000000, 1.000000000000000000, 1.000000000000000000, 1.000000000000000000, 1.000000000000000000, 1.000000000000000000, 1.000000000000000000, 1.000000000000000000, 1.000000000000000000, 1.000000000000000000, 1.000000000000000000, 1.000000000000000000, 1.000000000000000000, 1.000000000000000000, 1.000000000000000000, 1.000000000000000000, 1.000000000000000000, 1.000000000000000000, 1.000000000000000000, 1.000000000000000000, 1.000000000000000000, 1.000000000000000000, 1.000000000000000000, 1.000000000000000000, 1.000000000000000000, 1.000000000000000000, 1.000000000000000000, 1.000000000000000000, 1.000000000000000000, 1.000000000000000000, 1.000000000000000000, 1.000000000000000000, 1.000000000000000000, 1.000000000000000000, 1.000000000000000000, 1.000000000000000000, 1.000000000000000000, 1.000000000000000000, 1.000000000000000000, 1.000000000000000000, 1.000000000000000000, 1.000000000000000000, 1.000000000000000000, 1.000000000000000000, 1.000000000000000000, 1.000000000000000000, 1.000000000000000000, 1.000000000000000000, 1.000000000000000000, 1.000000000000000000, 1.000000000000000000, 1.000000000000000000, 1.000000000000000000, 1.000000000000000000, 1.000000000000000000, 1.000000000000000000, 1.000000000000000000, 1.000000000000000000, 1.000000000000000000, 1.000000000000000000, 1.000000000000000000, 1.000000000000000000, 1.000000000000000000, 1.000000000000000000, 1.000000000000000000, 1.000000000000000000, 1.000000000000000000, 1.000000000000000000, 1.000000000000000000, 1.000000000000000000, 1.000000000000000000, 1.000000000000000000, 1.000000000000000000, 1.000000000000000000, 1.000000000000000000, 1.000000000000000000, 1.000000000000000000, 1.000000000000000000, 1.000000000000000000, 1.000000000000000000, 1.000000000000000000, 1.000000000000000000, 1.000000000000000000, 1.000000000000000000, 1.000000000000000000, 1.000000000000000000, 1.000000000000000000, 1.000000000000000000, 1.000000000000000000, 1.000000000000000000, 1.000000000000000000, 1.000000000000000000, 1.000000000000000000, 1.000000000000000000, 1.000000000000000000, 1.000000000000000000, 1.000000000000000000, 1.000000000000000000, 1.000000000000000000, 1.000000000000000000, 1.000000000000000000, 1.000000000000000000, 1.000000000000000000, 1.000000000000000000, 1.000000000000000000, 1.000000000000000000, 1.000000000000000000, 1.000000000000000000, 1.000000000000000000, 1.000000000000000000, 1.000000000000000000, 1.000000000000000000, 1.000000000000000000, 1.000000000000000000),
 ( 0.3333333333333329818, 0.3333333333333329818, 0.3333333333333329818, 0.3333333333333329818, 0.3333333333333329818, 0.3333333333333329818, 0.3333333333333329818, 0.3333333333333329818, 0.3333333333333329818, 0.3333333333333329818, 0.3333333333333329818, 0.3333333333333329818, 0.3333333333333329818, 0.3333333333333329818, 0.3333333333333329818, 0.3333333333333329818, 0.3333333333333329818, 0.3333333333333329818, 0.3333333333333329818, 0.3333333333333329818, 0.3333333333333329818, 0.3333333333333329818, 0.3333333333333329818, 0.3333333333333329818, 0.3333333333333329818, 0.3333333333333329818, 0.3333333333333329818, 0.3333333333333329818, 0.3333333333333329818, 0.3333333333333329818, 0.3333333333333329818, 0.3333333333333329818, 0.3333333333333329818, 0.3333333333333329818, 0.3333333333333329818, 0.3333333333333329818, 0.3333333333333329818, 0.3333333333333329818, 0.3333333333333329818, 0.3333333333333329818, 0.3333333333333329818, 0.3333333333333329818, 0.3333333333333329818, 0.3333333333333329818, 0.3333333333333329818, 0.3333333333333329818, 0.3333333333333329818, 0.3333333333333329818, 0.3333333333333329818, 0.3333333333333329818, 0.3333333333333329818, 0.3333333333333329818, 0.3333333333333329818, 0.3333333333333329818, 0.3333333333333329818, 0.3333333333333329818, 0.3333333333333329818, 0.3333333333333329818, 0.3333333333333329818, 0.3333333333333329818, 0.3333333333333329818, 0.3333333333333329818, 0.3333333333333329818, 0.3333333333333329818, 0.3333333333333329818, 0.3333333333333329818, 0.3333333333333329818, 0.3333333333333329818, 0.3333333333333329818, 0.3333333333333329818, 0.3333333333333329818, 0.3333333333333329818, 0.3333333333333329818, 0.3333333333333329818, 0.3333333333333329818, 0.3333333333333329818, 0.3333333333333329818, 0.3333333333333329818, 0.3333333333333329818, 0.3333333333333329818, 0.3333333333333329818, 0.3333333333333329818, 0.3333333333333329818, 0.3333333333333329818, 0.3333333333333329818, 0.3333333333333329818, 0.3333333333333329818, 0.3333333333333329818, 0.3333333333333329818, 0.3333333333333329818, 0.3333333333333329818, 0.3333333333333329818, 0.3333333333333329818, 0.3333333333333329818, 0.3333333333333329818, 0.3333333333333329818, 0.3333333333333329818, 0.3333333333333329818, 0.3333333333333329818, 0.3333333333333329818, 0.3333333333333329818, 0.3333333333333329818, 0.3333333333333329818, 0.3333333333333329818, 0.3333333333333329818, 0.3333333333333329818, 0.3333333333333329818, 0.3333333333333329818, 0.3333333333333329818, 0.3333333333333329818, 0.3333333333333329818, 0.3333333333333329818, 0.3333333333333329818, 0.3333333333333329818, 0.3333333333333329818, 0.3333333333333329818, 0.3333333333333329818, 0.3333333333333329818, 0.3333333333333329818, 0.3333333333333329818, 0.3333333333333329818, 0.3333333333333329818, 0.3333333333333329818, 0.3333333333333329818, 0.3333333333333329818, 0.3333333333333329818, 0.3333333333333329818, 0.3333333333333329818, 0.3333333333333329818, 0.3333333333333329818, 0.3333333333333329818, 0.3333333333333329818, 0.3333333333333329818, 0.3333333333333329818, 0.3333333333333329818, 0.3333333333333329818, 0.3333333333333329818, 0.3333333333333329818, 0.3333333333333329818, 0.3333333333333329818, 0.3333333333333329818, 0.3333333333333329818, 0.3333333333333329818, 0.3333333333333329818, 0.3333333333333329818, 0.3333333333333329818, 0.3333333333333329818, 0.3333333333333329818, 0.3333333333333329818, 0.3333333333333329818, 0.3333333333333329818, 0.3333333333333329818, 0.3333333333333329818, 0.3333333333333329818, 0.3333333333333329818, 0.3333333333333329818, 0.3333333333333329818, 0.3333333333333329818, 0.3333333333333329818, 0.3333333333333329818, 0.3333333333333329818, 0.3333333333333329818, 0.3333333333333329818, 0.3333333333333329818, 0.3333333333333329818, 0.3333333333333329818, 0.3333333333333329818, 0.3333333333333329818, 0.3333333333333329818, 0.3333333333333329818, 0.3333333333333329818, 0.3333333333333329818, 0.3333333333333329818, 0.3333333333333329818, 0.3333333333333329818, 0.3333333333333329818, 0.3333333333333329818, 0.3333333333333329818, 0.3333333333333329818, 0.3333333333333329818, 0.3333333333333329818, 0.3333333333333329818, 0.3333333333333329818, 0.3333333333333329818, 0.3333333333333329818, 0.3333333333333329818, 0.3333333333333329818, 0.3333333333333329818),
 ( 0.3333333333333329818, 0.3333333333333329818, 0.3333333333333329818, 0.3333333333333329818, 0.3333333333333329818, 0.3333333333333329818, 0.3333333333333329818, 0.3333333333333329818, 0.3333333333333329818, 0.3333333333333329818, 0.3333333333333329818, 0.3333333333333329818, 0.3333333333333329818, 0.3333333333333329818, 0.3333333333333329818, 0.3333333333333329818, 0.3333333333333329818, 0.3333333333333329818, 0.3333333333333329818, 0.3333333333333329818, 0.3333333333333329818, 0.3333333333333329818, 0.3333333333333329818, 0.3333333333333329818, 0.3333333333333329818, 0.3333333333333329818, 0.3333333333333329818, 0.3333333333333329818, 0.3333333333333329818, 0.3333333333333329818, 0.3333333333333329818, 0.3333333333333329818, 0.3333333333333329818, 0.3333333333333329818, 0.3333333333333329818, 0.3333333333333329818, 0.3333333333333329818, 0.3333333333333329818, 0.3333333333333329818, 0.3333333333333329818, 0.3333333333333329818, 0.3333333333333329818, 0.3333333333333329818, 0.3333333333333329818, 0.3333333333333329818, 0.3333333333333329818, 0.3333333333333329818, 0.3333333333333329818, 0.3333333333333329818, 0.3333333333333329818, 0.3333333333333329818, 0.3333333333333329818, 0.3333333333333329818, 0.3333333333333329818, 0.3333333333333329818, 0.3333333333333329818, 0.3333333333333329818, 0.3333333333333329818, 0.3333333333333329818, 0.3333333333333329818, 0.3333333333333329818, 0.3333333333333329818, 0.3333333333333329818, 0.3333333333333329818, 0.3333333333333329818, 0.3333333333333329818, 0.3333333333333329818, 0.3333333333333329818, 0.3333333333333329818, 0.3333333333333329818, 0.3333333333333329818, 0.3333333333333329818, 0.3333333333333329818, 0.3333333333333329818, 0.3333333333333329818, 0.3333333333333329818, 0.3333333333333329818, 0.3333333333333329818, 0.3333333333333329818, 0.3333333333333329818, 0.3333333333333329818, 0.3333333333333329818, 0.3333333333333329818, 0.3333333333333329818, 0.3333333333333329818, 0.3333333333333329818, 0.3333333333333329818, 0.3333333333333329818, 0.3333333333333329818, 0.3333333333333329818, 0.3333333333333329818, 0.3333333333333329818, 0.3333333333333329818, 0.3333333333333329818, 0.3333333333333329818, 0.3333333333333329818, 0.3333333333333329818, 0.3333333333333329818, 0.3333333333333329818, 0.3333333333333329818, 0.3333333333333329818, 0.3333333333333329818, 0.3333333333333329818, 0.3333333333333329818, 0.3333333333333329818, 0.3333333333333329818, 0.3333333333333329818, 0.3333333333333329818, 0.3333333333333329818, 0.3333333333333329818, 0.3333333333333329818, 0.3333333333333329818, 0.3333333333333329818, 0.3333333333333329818, 0.3333333333333329818, 0.3333333333333329818, 0.3333333333333329818, 0.3333333333333329818, 0.3333333333333329818, 0.3333333333333329818, 0.3333333333333329818, 0.3333333333333329818, 0.3333333333333329818, 0.3333333333333329818, 0.3333333333333329818, 0.3333333333333329818, 0.3333333333333329818, 0.3333333333333329818, 0.3333333333333329818, 0.3333333333333329818, 0.3333333333333329818, 0.3333333333333329818, 0.3333333333333329818, 0.3333333333333329818, 0.3333333333333329818, 0.3333333333333329818, 0.3333333333333329818, 0.3333333333333329818, 0.3333333333333329818, 0.3333333333333329818, 0.3333333333333329818, 0.3333333333333329818, 0.3333333333333329818, 0.3333333333333329818, 0.3333333333333329818, 0.3333333333333329818, 0.3333333333333329818, 0.3333333333333329818, 0.3333333333333329818, 0.3333333333333329818, 0.3333333333333329818, 0.3333333333333329818, 0.3333333333333329818, 0.3333333333333329818, 0.3333333333333329818, 0.3333333333333329818, 0.3333333333333329818, 0.3333333333333329818, 0.3333333333333329818, 0.3333333333333329818, 0.3333333333333329818, 0.3333333333333329818, 0.3333333333333329818, 0.3333333333333329818, 0.3333333333333329818, 0.3333333333333329818, 0.3333333333333329818, 0.3333333333333329818, 0.3333333333333329818, 0.3333333333333329818, 0.3333333333333329818, 0.3333333333333329818, 0.3333333333333329818, 0.3333333333333329818, 0.3333333333333329818, 0.3333333333333329818, 0.3333333333333329818, 0.3333333333333329818, 0.3333333333333329818, 0.3333333333333329818, 0.3333333333333329818, 0.3333333333333329818, 0.3333333333333329818, 0.3333333333333329818, 0.3333333333333329818, 0.3333333333333329818, 0.3333333333333329818, 0.3333333333333329818),
 ( 1.000000000000000000, 1.000000000000000000, 1.000000000000000000, 1.000000000000000000, 1.000000000000000000, 1.000000000000000000, 1.000000000000000000, 1.000000000000000000, 1.000000000000000000, 1.000000000000000000, 1.000000000000000000, 1.000000000000000000, 1.000000000000000000, 1.000000000000000000, 1.000000000000000000, 1.000000000000000000, 1.000000000000000000, 1.000000000000000000, 1.000000000000000000, 1.000000000000000000, 1.000000000000000000, 1.000000000000000000, 1.000000000000000000, 1.000000000000000000, 1.000000000000000000, 1.000000000000000000, 1.000000000000000000, 1.000000000000000000, 1.000000000000000000, 1.000000000000000000, 1.000000000000000000, 1.000000000000000000, 1.000000000000000000, 1.000000000000000000, 1.000000000000000000, 1.000000000000000000, 1.000000000000000000, 1.000000000000000000, 1.000000000000000000, 1.000000000000000000, 1.000000000000000000, 1.000000000000000000, 1.000000000000000000, 1.000000000000000000, 1.000000000000000000, 1.000000000000000000, 1.000000000000000000, 1.000000000000000000, 1.000000000000000000, 1.000000000000000000, 1.000000000000000000, 1.000000000000000000, 1.000000000000000000, 1.000000000000000000, 1.000000000000000000, 1.000000000000000000, 1.000000000000000000, 1.000000000000000000, 1.000000000000000000, 1.000000000000000000, 1.000000000000000000, 1.000000000000000000, 1.000000000000000000, 1.000000000000000000, 1.000000000000000000, 1.000000000000000000, 1.000000000000000000, 1.000000000000000000, 1.000000000000000000, 1.000000000000000000, 1.000000000000000000, 1.000000000000000000, 1.000000000000000000, 1.000000000000000000, 1.000000000000000000, 1.000000000000000000, 1.000000000000000000, 1.000000000000000000, 1.000000000000000000, 1.000000000000000000, 1.000000000000000000, 1.000000000000000000, 1.000000000000000000, 1.000000000000000000, 1.000000000000000000, 1.000000000000000000, 1.000000000000000000, 1.000000000000000000, 1.000000000000000000, 1.000000000000000000, 1.000000000000000000, 1.000000000000000000, 1.000000000000000000, 1.000000000000000000, 1.000000000000000000, 1.000000000000000000, 1.000000000000000000, 1.000000000000000000, 1.000000000000000000, 1.000000000000000000, 1.000000000000000000, 1.000000000000000000, 1.000000000000000000, 1.000000000000000000, 1.000000000000000000, 1.000000000000000000, 1.000000000000000000, 1.000000000000000000, 1.000000000000000000, 1.000000000000000000, 1.000000000000000000, 1.000000000000000000, 1.000000000000000000, 1.000000000000000000, 1.000000000000000000, 1.000000000000000000, 1.000000000000000000, 1.000000000000000000, 1.000000000000000000, 1.000000000000000000, 1.000000000000000000, 1.000000000000000000, 1.000000000000000000, 1.000000000000000000, 1.000000000000000000, 1.000000000000000000, 1.000000000000000000, 1.000000000000000000, 1.000000000000000000, 1.000000000000000000, 1.000000000000000000, 1.000000000000000000, 1.000000000000000000, 1.000000000000000000, 1.000000000000000000, 1.000000000000000000, 1.000000000000000000, 1.000000000000000000, 1.000000000000000000, 1.000000000000000000, 1.000000000000000000, 1.000000000000000000, 1.000000000000000000, 1.000000000000000000, 1.000000000000000000, 1.000000000000000000, 1.000000000000000000, 1.000000000000000000, 1.000000000000000000, 1.000000000000000000, 1.000000000000000000, 1.000000000000000000, 1.000000000000000000, 1.000000000000000000, 1.000000000000000000, 1.000000000000000000, 1.000000000000000000, 1.000000000000000000, 1.000000000000000000, 1.000000000000000000, 1.000000000000000000, 1.000000000000000000, 1.000000000000000000, 1.000000000000000000, 1.000000000000000000, 1.000000000000000000, 1.000000000000000000, 1.000000000000000000, 1.000000000000000000, 1.000000000000000000, 1.000000000000000000, 1.000000000000000000, 1.000000000000000000, 1.000000000000000000, 1.000000000000000000, 1.000000000000000000, 1.000000000000000000, 1.000000000000000000, 1.000000000000000000, 1.000000000000000000, 1.000000000000000000, 1.000000000000000000, 1.000000000000000000, 1.000000000000000000, 1.000000000000000000, 1.000000000000000000, 1.000000000000000000, 1.000000000000000000),
 ( 0.3333333333333329818, 0.3333333333333329818, 0.3333333333333329818, 0.3333333333333329818, 0.3333333333333329818, 0.3333333333333329818, 0.3333333333333329818, 0.3333333333333329818, 0.3333333333333329818, 0.3333333333333329818, 0.3333333333333329818, 0.3333333333333329818, 0.3333333333333329818, 0.3333333333333329818, 0.3333333333333329818, 0.3333333333333329818, 0.3333333333333329818, 0.3333333333333329818, 0.3333333333333329818, 0.3333333333333329818, 0.3333333333333329818, 0.3333333333333329818, 0.3333333333333329818, 0.3333333333333329818, 0.3333333333333329818, 0.3333333333333329818, 0.3333333333333329818, 0.3333333333333329818, 0.3333333333333329818, 0.3333333333333329818, 0.3333333333333329818, 0.3333333333333329818, 0.3333333333333329818, 0.3333333333333329818, 0.3333333333333329818, 0.3333333333333329818, 0.3333333333333329818, 0.3333333333333329818, 0.3333333333333329818, 0.3333333333333329818, 0.3333333333333329818, 0.3333333333333329818, 0.3333333333333329818, 0.3333333333333329818, 0.3333333333333329818, 0.3333333333333329818, 0.3333333333333329818, 0.3333333333333329818, 0.3333333333333329818, 0.3333333333333329818, 0.3333333333333329818, 0.3333333333333329818, 0.3333333333333329818, 0.3333333333333329818, 0.3333333333333329818, 0.3333333333333329818, 0.3333333333333329818, 0.3333333333333329818, 0.3333333333333329818, 0.3333333333333329818, 0.3333333333333329818, 0.3333333333333329818, 0.3333333333333329818, 0.3333333333333329818, 0.3333333333333329818, 0.3333333333333329818, 0.3333333333333329818, 0.3333333333333329818, 0.3333333333333329818, 0.3333333333333329818, 0.3333333333333329818, 0.3333333333333329818, 0.3333333333333329818, 0.3333333333333329818, 0.3333333333333329818, 0.3333333333333329818, 0.3333333333333329818, 0.3333333333333329818, 0.3333333333333329818, 0.3333333333333329818, 0.3333333333333329818, 0.3333333333333329818, 0.3333333333333329818, 0.3333333333333329818, 0.3333333333333329818, 0.3333333333333329818, 0.3333333333333329818, 0.3333333333333329818, 0.3333333333333329818, 0.3333333333333329818, 0.3333333333333329818, 0.3333333333333329818, 0.3333333333333329818, 0.3333333333333329818, 0.3333333333333329818, 0.3333333333333329818, 0.3333333333333329818, 0.3333333333333329818, 0.3333333333333329818, 0.3333333333333329818, 0.3333333333333329818, 0.3333333333333329818, 0.3333333333333329818, 0.3333333333333329818, 0.3333333333333329818, 0.3333333333333329818, 0.3333333333333329818, 0.3333333333333329818, 0.3333333333333329818, 0.3333333333333329818, 0.3333333333333329818, 0.3333333333333329818, 0.3333333333333329818, 0.3333333333333329818, 0.3333333333333329818, 0.3333333333333329818, 0.3333333333333329818, 0.3333333333333329818, 0.3333333333333329818, 0.3333333333333329818, 0.3333333333333329818, 0.3333333333333329818, 0.3333333333333329818, 0.3333333333333329818, 0.3333333333333329818, 0.3333333333333329818, 0.3333333333333329818, 0.3333333333333329818, 0.3333333333333329818, 0.3333333333333329818, 0.3333333333333329818, 0.3333333333333329818, 0.3333333333333329818, 0.3333333333333329818, 0.3333333333333329818, 0.3333333333333329818, 0.3333333333333329818, 0.3333333333333329818, 0.3333333333333329818, 0.3333333333333329818, 0.3333333333333329818, 0.3333333333333329818, 0.3333333333333329818, 0.3333333333333329818, 0.3333333333333329818, 0.3333333333333329818, 0.3333333333333329818, 0.3333333333333329818, 0.3333333333333329818, 0.3333333333333329818, 0.3333333333333329818, 0.3333333333333329818, 0.3333333333333329818, 0.3333333333333329818, 0.3333333333333329818, 0.3333333333333329818, 0.3333333333333329818, 0.3333333333333329818, 0.3333333333333329818, 0.3333333333333329818, 0.3333333333333329818, 0.3333333333333329818, 0.3333333333333329818, 0.3333333333333329818, 0.3333333333333329818, 0.3333333333333329818, 0.3333333333333329818, 0.3333333333333329818, 0.3333333333333329818, 0.3333333333333329818, 0.3333333333333329818, 0.3333333333333329818, 0.3333333333333329818, 0.3333333333333329818, 0.3333333333333329818, 0.3333333333333329818, 0.3333333333333329818, 0.3333333333333329818, 0.3333333333333329818, 0.3333333333333329818, 0.3333333333333329818, 0.3333333333333329818, 0.3333333333333329818, 0.3333333333333329818, 0.3333333333333329818, 0.3333333333333329818, 0.3333333333333329818, 0.3333333333333329818),
 ( 0.3333333333333329818, 0.3333333333333329818, 0.3333333333333329818, 0.3333333333333329818, 0.3333333333333329818, 0.3333333333333329818, 0.3333333333333329818, 0.3333333333333329818, 0.3333333333333329818, 0.3333333333333329818, 0.3333333333333329818, 0.3333333333333329818, 0.3333333333333329818, 0.3333333333333329818, 0.3333333333333329818, 0.3333333333333329818, 0.3333333333333329818, 0.3333333333333329818, 0.3333333333333329818, 0.3333333333333329818, 0.3333333333333329818, 0.3333333333333329818, 0.3333333333333329818, 0.3333333333333329818, 0.3333333333333329818, 0.3333333333333329818, 0.3333333333333329818, 0.3333333333333329818, 0.3333333333333329818, 0.3333333333333329818, 0.3333333333333329818, 0.3333333333333329818, 0.3333333333333329818, 0.3333333333333329818, 0.3333333333333329818, 0.3333333333333329818, 0.3333333333333329818, 0.3333333333333329818, 0.3333333333333329818, 0.3333333333333329818, 0.3333333333333329818, 0.3333333333333329818, 0.3333333333333329818, 0.3333333333333329818, 0.3333333333333329818, 0.3333333333333329818, 0.3333333333333329818, 0.3333333333333329818, 0.3333333333333329818, 0.3333333333333329818, 0.3333333333333329818, 0.3333333333333329818, 0.3333333333333329818, 0.3333333333333329818, 0.3333333333333329818, 0.3333333333333329818, 0.3333333333333329818, 0.3333333333333329818, 0.3333333333333329818, 0.3333333333333329818, 0.3333333333333329818, 0.3333333333333329818, 0.3333333333333329818, 0.3333333333333329818, 0.3333333333333329818, 0.3333333333333329818, 0.3333333333333329818, 0.3333333333333329818, 0.3333333333333329818, 0.3333333333333329818, 0.3333333333333329818, 0.3333333333333329818, 0.3333333333333329818, 0.3333333333333329818, 0.3333333333333329818, 0.3333333333333329818, 0.3333333333333329818, 0.3333333333333329818, 0.3333333333333329818, 0.3333333333333329818, 0.3333333333333329818, 0.3333333333333329818, 0.3333333333333329818, 0.3333333333333329818, 0.3333333333333329818, 0.3333333333333329818, 0.3333333333333329818, 0.3333333333333329818, 0.3333333333333329818, 0.3333333333333329818, 0.3333333333333329818, 0.3333333333333329818, 0.3333333333333329818, 0.3333333333333329818, 0.3333333333333329818, 0.3333333333333329818, 0.3333333333333329818, 0.3333333333333329818, 0.3333333333333329818, 0.3333333333333329818, 0.3333333333333329818, 0.3333333333333329818, 0.3333333333333329818, 0.3333333333333329818, 0.3333333333333329818, 0.3333333333333329818, 0.3333333333333329818, 0.3333333333333329818, 0.3333333333333329818, 0.3333333333333329818, 0.3333333333333329818, 0.3333333333333329818, 0.3333333333333329818, 0.3333333333333329818, 0.3333333333333329818, 0.3333333333333329818, 0.3333333333333329818, 0.3333333333333329818, 0.3333333333333329818, 0.3333333333333329818, 0.3333333333333329818, 0.3333333333333329818, 0.3333333333333329818, 0.3333333333333329818, 0.3333333333333329818, 0.3333333333333329818, 0.3333333333333329818, 0.3333333333333329818, 0.3333333333333329818, 0.3333333333333329818, 0.3333333333333329818, 0.3333333333333329818, 0.3333333333333329818, 0.3333333333333329818, 0.3333333333333329818, 0.3333333333333329818, 0.3333333333333329818, 0.3333333333333329818, 0.3333333333333329818, 0.3333333333333329818, 0.3333333333333329818, 0.3333333333333329818, 0.3333333333333329818, 0.3333333333333329818, 0.3333333333333329818, 0.3333333333333329818, 0.3333333333333329818, 0.3333333333333329818, 0.3333333333333329818, 0.3333333333333329818, 0.3333333333333329818, 0.3333333333333329818, 0.3333333333333329818, 0.3333333333333329818, 0.3333333333333329818, 0.3333333333333329818, 0.3333333333333329818, 0.3333333333333329818, 0.3333333333333329818, 0.3333333333333329818, 0.3333333333333329818, 0.3333333333333329818, 0.3333333333333329818, 0.3333333333333329818, 0.3333333333333329818, 0.3333333333333329818, 0.3333333333333329818, 0.3333333333333329818, 0.3333333333333329818, 0.3333333333333329818, 0.3333333333333329818, 0.3333333333333329818, 0.3333333333333329818, 0.3333333333333329818, 0.3333333333333329818, 0.3333333333333329818, 0.3333333333333329818, 0.3333333333333329818, 0.3333333333333329818, 0.3333333333333329818, 0.3333333333333329818, 0.3333333333333329818, 0.3333333333333329818, 0.3333333333333329818, 0.3333333333333329818, 0.3333333333333329818, 0.3333333333333329818, 0.3333333333333329818),
 ( 1.000000000000000000, 1.000000000000000000, 1.000000000000000000, 1.000000000000000000, 1.000000000000000000, 1.000000000000000000, 1.000000000000000000, 1.000000000000000000, 1.000000000000000000, 1.000000000000000000, 1.000000000000000000, 1.000000000000000000, 1.000000000000000000, 1.000000000000000000, 1.000000000000000000, 1.000000000000000000, 1.000000000000000000, 1.000000000000000000, 1.000000000000000000, 1.000000000000000000, 1.000000000000000000, 1.000000000000000000, 1.000000000000000000, 1.000000000000000000, 1.000000000000000000, 1.000000000000000000, 1.000000000000000000, 1.000000000000000000, 1.000000000000000000, 1.000000000000000000, 1.000000000000000000, 1.000000000000000000, 1.000000000000000000, 1.000000000000000000, 1.000000000000000000, 1.000000000000000000, 1.000000000000000000, 1.000000000000000000, 1.000000000000000000, 1.000000000000000000, 1.000000000000000000, 1.000000000000000000, 1.000000000000000000, 1.000000000000000000, 1.000000000000000000, 1.000000000000000000, 1.000000000000000000, 1.000000000000000000, 1.000000000000000000, 1.000000000000000000, 1.000000000000000000, 1.000000000000000000, 1.000000000000000000, 1.000000000000000000, 1.000000000000000000, 1.000000000000000000, 1.000000000000000000, 1.000000000000000000, 1.000000000000000000, 1.000000000000000000, 1.000000000000000000, 1.000000000000000000, 1.000000000000000000, 1.000000000000000000, 1.000000000000000000, 1.000000000000000000, 1.000000000000000000, 1.000000000000000000, 1.000000000000000000, 1.000000000000000000, 1.000000000000000000, 1.000000000000000000, 1.000000000000000000, 1.000000000000000000, 1.000000000000000000, 1.000000000000000000, 1.000000000000000000, 1.000000000000000000, 1.000000000000000000, 1.000000000000000000, 1.000000000000000000, 1.000000000000000000, 1.000000000000000000, 1.000000000000000000, 1.000000000000000000, 1.000000000000000000, 1.000000000000000000, 1.000000000000000000, 1.000000000000000000, 1.000000000000000000, 1.000000000000000000, 1.000000000000000000, 1.000000000000000000, 1.000000000000000000, 1.000000000000000000, 1.000000000000000000, 1.000000000000000000, 1.000000000000000000, 1.000000000000000000, 1.000000000000000000, 1.000000000000000000, 1.000000000000000000, 1.000000000000000000, 1.000000000000000000, 1.000000000000000000, 1.000000000000000000, 1.000000000000000000, 1.000000000000000000, 1.000000000000000000, 1.000000000000000000, 1.000000000000000000, 1.000000000000000000, 1.000000000000000000, 1.000000000000000000, 1.000000000000000000, 1.000000000000000000, 1.000000000000000000, 1.000000000000000000, 1.000000000000000000, 1.000000000000000000, 1.000000000000000000, 1.000000000000000000, 1.000000000000000000, 1.000000000000000000, 1.000000000000000000, 1.000000000000000000, 1.000000000000000000, 1.000000000000000000, 1.000000000000000000, 1.000000000000000000, 1.000000000000000000, 1.000000000000000000, 1.000000000000000000, 1.000000000000000000, 1.000000000000000000, 1.000000000000000000, 1.000000000000000000, 1.000000000000000000, 1.000000000000000000, 1.000000000000000000, 1.000000000000000000, 1.000000000000000000, 1.000000000000000000, 1.000000000000000000, 1.000000000000000000, 1.000000000000000000, 1.000000000000000000, 1.000000000000000000, 1.000000000000000000, 1.000000000000000000, 1.000000000000000000, 1.000000000000000000, 1.000000000000000000, 1.000000000000000000, 1.000000000000000000, 1.000000000000000000, 1.000000000000000000, 1.000000000000000000, 1.000000000000000000, 1.000000000000000000, 1.000000000000000000, 1.000000000000000000, 1.000000000000000000, 1.000000000000000000, 1.000000000000000000, 1.000000000000000000, 1.000000000000000000, 1.000000000000000000, 1.000000000000000000, 1.000000000000000000, 1.000000000000000000, 1.000000000000000000, 1.000000000000000000, 1.000000000000000000, 1.000000000000000000, 1.000000000000000000, 1.000000000000000000, 1.000000000000000000, 1.000000000000000000, 1.000000000000000000, 1.000000000000000000, 1.000000000000000000, 1.000000000000000000, 1.000000000000000000, 1.000000000000000000, 1.000000000000000000, 1.000000000000000000, 1.000000000000000000) ) ) 
 REPRESENTATION_ITEM ( '' )  SURFACE ( )  );
#16597=CARTESIAN_POINT ( 'NONE',  ( 0.4974685680287860290, -5.139830508474580562, 7.000224381598740386 ) ) ;
#16601=CARTESIAN_POINT ( 'NONE',  ( -1.571912189623050127, -1.264893411152959946, 6.451524409078659872 ) ) ;
#16605=CARTESIAN_POINT ( 'NONE',  ( -0.3752419433106839453, -1.424070552810999812, 7.023346545710370314 ) ) ;
#16606=CARTESIAN_POINT ( 'NONE',  ( 2.116444151961470066, -0.05338983050847490031, 3.670839500609349937 ) ) ;
#16608=CARTESIAN_POINT ( 'NONE',  ( 2.353194804772640314, -0.3756355932203400139, 4.731327187377229571 ) ) ;
#16612=CARTESIAN_POINT ( 'NONE',  ( 1.507201387236019263, -2.475884402143949004, 6.507509243627190187 ) ) ;
#16614=CARTESIAN_POINT ( 'NONE',  ( -1.707817112497179934, -5.488771186440679628, 6.319218296629480314 ) ) ;
#16615=CARTESIAN_POINT ( 'NONE',  ( -2.608006145151089861, -1.427911429170979352, 5.191342690854409803 ) ) ;
#16618=CARTESIAN_POINT ( 'NONE',  ( -1.229686204202100175, -5.164643153926309793, 2.674737924334550154 ) ) ;
#16619=CARTESIAN_POINT ( 'NONE',  ( -2.331386066015260106, -4.641695212954759953, 4.378465089518190467 ) ) ;
#16620=CARTESIAN_POINT ( 'NONE',  ( -2.199635523370571111, -5.057043525783965876, 3.215170965529011493 ) ) ;
#16626=CARTESIAN_POINT ( 'NONE',  ( -0.6965028529798926726, -1.470647129387581575, 6.631265289497783044 ) ) ;
#16631=CARTESIAN_POINT ( 'NONE',  ( 1.526871680339569659, -0.3400423728813561364, 3.327650196883443101 ) ) ;
#16632=CARTESIAN_POINT ( 'NONE',  ( -2.445954350973251312, -2.941650167909708458, 5.729767452368195180 ) ) ;
#16634=CARTESIAN_POINT ( 'NONE',  ( -0.009452110982656879157, -5.299807955295460005, 2.350000000000000089 ) ) ;
#16635=CARTESIAN_POINT ( 'NONE',  ( 1.580445181003960586, -5.341949152542365908, 3.389704561770334301 ) ) ;
#16638=CARTESIAN_POINT ( 'NONE',  ( 2.143090896833110381, -5.395338983050850246, 5.672454929438339732 ) ) ;
#16641=CARTESIAN_POINT ( 'NONE',  ( 1.300961508564179914, -5.422033898305079092, 6.661123742937279602 ) ) ;
#16642=CARTESIAN_POINT ( 'NONE',  ( 2.352190863465239978, -0.6826862039457530784, 4.622903765856330338 ) ) ;
#16643=CARTESIAN_POINT ( 'NONE',  ( -0.2938780505772099483, -3.706322805063249959, 2.062434951628528523 ) ) ;
#16646=CARTESIAN_POINT ( 'NONE',  ( 1.934380261529039080, -0.7758393570989061683, 5.387804366397126010 ) ) ;
#16651=CARTESIAN_POINT ( 'NONE',  ( -2.286166334984490067, -0.5135593220338989795, 5.258525443163870605 ) ) ;
#16652=CARTESIAN_POINT ( 'NONE',  ( 2.352760675243219968, -2.565196678937129882, 4.757121734156020132 ) ) ;
#16653=CARTESIAN_POINT ( 'NONE',  ( -2.293398556041709835, -0.5358050847457630494, 4.171956209133480975 ) ) ;
#16657=CARTESIAN_POINT ( 'NONE',  ( -2.088297318559229065, -5.202118644067799558, 5.785136623276640577 ) ) ;
#16659=CARTESIAN_POINT ( 'NONE',  ( -0.003440977838562779990, -0.5045365850187280010, 2.491636233962229774 ) ) ;
#16661=CARTESIAN_POINT ( 'NONE',  ( -1.460675875430050175, -4.684430913171359734, 6.545310725710059785 ) ) ;
#16663=CARTESIAN_POINT ( 'NONE',  ( 1.722095088963199405, -0.7763906680874423927, 2.675734922583239861 ) ) ;
#16667=CARTESIAN_POINT ( 'NONE',  ( 0.6673090596498160165, -2.239160642901090181, 2.443133963569570355 ) ) ;
#16670=CARTESIAN_POINT ( 'NONE',  ( -0.9588981328681495109, -3.613169651910099756, 2.884671871696449230 ) ) ;
#16679=CARTESIAN_POINT ( 'NONE',  ( 0.6187874668174475623, -5.135381355932194580, 6.657494107589526422 ) ) ;
#16683=CARTESIAN_POINT ( 'NONE',  ( -0.9345217207511814506, -5.211074464177369414, 2.212378604467589494 ) ) ;
#16685=CARTESIAN_POINT ( 'NONE',  ( -1.886482464143629967, -5.010466949207390108, 3.890008792968694618 ) ) ;
#16686=CARTESIAN_POINT ( 'NONE',  ( 0.8570167067220200163, -0.01779661016949179997, 2.508190348879349774 ) ) ;
#16691=CARTESIAN_POINT ( 'NONE',  ( 2.230812463554230352, -0.1023305084745770588, 6.137473736419911674 ) ) ;
#16695=CARTESIAN_POINT ( 'NONE',  ( 1.781655196750449255, -2.079983501243050092, 3.162323035427780482 ) ) ;
#16696=CARTESIAN_POINT ( 'NONE',  ( -1.750316316486840051, -5.559957627118639500, 3.126818518378589928 ) ) ;
#16697=CARTESIAN_POINT ( 'NONE',  ( -0.2041457401073759059, -1.101875393134940984, 7.346023093209487875 ) ) ;
#16700=CARTESIAN_POINT ( 'NONE',  ( -1.794646911016549939, -4.432100618360159672, 6.222494056560700315 ) ) ;
#16704=CARTESIAN_POINT ( 'NONE',  ( -1.823404397755031159, -1.656953435693890864, 5.643450181448764980 ) ) ;
#16708=CARTESIAN_POINT ( 'NONE',  ( -1.668426559427188982, -4.385524041783587457, 6.763847501343006385 ) ) ;
#16710=CARTESIAN_POINT ( 'NONE',  ( -0.3865907654992132292, -4.952022267818764867, 2.675656795012148592 ) ) ;
#16711=CARTESIAN_POINT ( 'NONE',  ( -2.052786957354850728, -5.224364406779660186, 4.727327971967373976 ) ) ;
#16714=CARTESIAN_POINT ( 'NONE',  ( 2.270487904532159540, -0.06228813559322070315, 4.080813552109670894 ) ) ;
#16720=CARTESIAN_POINT ( 'NONE',  ( -1.889104232906369862, -5.555508474576269506, 3.296507079072529933 ) ) ;
#16721=CARTESIAN_POINT ( 'NONE',  ( -1.864786684738369837, -4.804713230972779137, 2.817120744449669978 ) ) ;
#16723=CARTESIAN_POINT ( 'NONE',  ( -1.632144308286139989, -1.311469987729540376, 5.945394234592896510 ) ) ;
#16727=CARTESIAN_POINT ( 'NONE',  ( 1.768982498583140162, -5.182556448558739426, 2.931017501416850024 ) ) ;
#16728=CARTESIAN_POINT ( 'NONE',  ( -0.9150601050661559821, -0.4690677966101700069, 6.868218666554230190 ) ) ;
#16729=CARTESIAN_POINT ( 'NONE',  ( -1.917298190932639868, -3.496728210468659892, 3.335187436117939885 ) ) ;
#16732=CARTESIAN_POINT ( 'NONE',  ( -2.638803263991410741, -5.519915254237295343, 4.982085668537435730 ) ) ;
#16740=CARTESIAN_POINT ( 'NONE',  ( -0.009452173233711079481, -0.5998089419219779783, 2.358866582356790254 ) ) ;
#16745=CARTESIAN_POINT ( 'NONE',  ( 0.4005155088302400634, -4.474836318576759453, 7.019123328904770531 ) ) ;
#16746=CARTESIAN_POINT ( 'NONE',  ( 0.4944444514933294954, -5.311531839079339790, 2.693008931300498787 ) ) ;
#16749=CARTESIAN_POINT ( 'NONE',  ( -1.097561405233230092, -3.613169651910099756, 2.618148744692269769 ) ) ;
#16751=CARTESIAN_POINT ( 'NONE',  ( 1.472933559740161602, -2.751502985243430288, 6.130163826706326091 ) ) ;
#16754=CARTESIAN_POINT ( 'NONE',  ( -0.1641805561540918557, -0.5962015548080631389, 2.650681144176719961 ) ) ;
#16758=CARTESIAN_POINT ( 'NONE',  ( -2.218077401483159683, -4.824160642901089702, 5.486688202856539576 ) ) ;
#16763=CARTESIAN_POINT ( 'NONE',  ( -1.647941990407690627, -5.255508474576275901, 3.475676388127094896 ) ) ;
#16764=CARTESIAN_POINT ( 'NONE',  ( 1.650842931266089497, -2.033406924666469884, 2.622060802311419803 ) ) ;
#16773=CARTESIAN_POINT ( 'NONE',  ( 2.046174187462399985, -1.121322805063259986, 5.862719605943959245 ) ) ;
#16776=CARTESIAN_POINT ( 'NONE',  ( 1.454969160282001406, -2.452596113855660676, 6.148435909958180901 ) ) ;
#16778=CARTESIAN_POINT ( 'NONE',  ( 2.340070819011249803, -0.08008474576271229495, 4.950151441910540129 ) ) ;
#16783=CARTESIAN_POINT ( 'NONE',  ( 2.088297318559229954, -0.09788135593220401165, 5.785136623276629919 ) ) ;
#16789=CARTESIAN_POINT ( 'NONE',  ( -2.245209214543379961, -2.964938456198000782, 5.405536158119060630 ) ) ;
#16790=CARTESIAN_POINT ( 'NONE',  ( 2.321479326063749404, -5.350847457627126325, 3.414080590619961608 ) ) ;
#16794=CARTESIAN_POINT ( 'NONE',  ( 1.936998685628529948, -0.8418633456037969420, 3.363294429306519895 ) ) ;
#16795=CARTESIAN_POINT ( 'NONE',  ( -1.880631435828179265, -0.5447033898305090327, 3.876649216148230437 ) ) ;
#16800=CARTESIAN_POINT ( 'NONE',  ( -1.440522616026439495, -4.804713230972779137, 3.241384813161591438 ) ) ;
#16806=CARTESIAN_POINT ( 'NONE',  ( -1.949083719010310078, -0.2402542372881359412, 4.055210292801460170 ) ) ;
#16807=CARTESIAN_POINT ( 'NONE',  ( 2.612083973477990373, -3.780028546288090041, 4.230818789270793800 ) ) ;
#16808=CARTESIAN_POINT ( 'NONE',  ( -0.009452110982656879157, -5.299807955295460005, 2.350000000000000089 ) ) ;
#16809=CARTESIAN_POINT ( 'NONE',  ( 1.449568901432419343, -5.337500000000000355, 3.250431098567584165 ) ) ;
#16812=CARTESIAN_POINT ( 'NONE',  ( 1.428515267734869587, -0.03114406779661050076, 2.829745655876920285 ) ) ;
#16814=CARTESIAN_POINT ( 'NONE',  ( -1.873832970144350130, -0.5625000000000005551, 2.826167029855650270 ) ) ;
#16819=CARTESIAN_POINT ( 'NONE',  ( -0.5606293434988356417, -4.269082600342137823, 7.293994686233948421 ) ) ;
#16821=CARTESIAN_POINT ( 'NONE',  ( 1.117157304995380240, -0.9388573751169233539, 6.422457952614097465 ) ) ;
#16826=CARTESIAN_POINT ( 'NONE',  ( -1.661700935788390066, -4.954166666666670160, 3.038299064211620326 ) ) ;
#16827=CARTESIAN_POINT ( 'NONE',  ( -1.641808337277740115, -0.4868644067796619734, 6.386111670537629514 ) ) ;
#16829=CARTESIAN_POINT ( 'NONE',  ( -1.781655196750479897, -3.520016498756949996, 3.162323035427820450 ) ) ;
#16832=CARTESIAN_POINT ( 'NONE',  ( -1.610878918935079840, -5.568855932203385706, 2.590989782159090815 ) ) ;
#16836=DIRECTION ( 'NONE',  ( 0.000000000000000000, 0.000000000000000000, 1.000000000000000000 ) ) ;
#16837=FACE_OUTER_BOUND ( 'NONE', #16155, .T. ) ;
#16839=CARTESIAN_POINT ( 'NONE',  ( -0.2564439965878500538, -4.544701183441629766, 7.039440566481220074 ) ) ;
#16842=CARTESIAN_POINT ( 'NONE',  ( 0.9788656693287738353, -5.320452325212859712, 2.556357798777459944 ) ) ;
#16847=CARTESIAN_POINT ( 'NONE',  ( -1.914021115237000137, -4.754295778036220277, 6.069404563272239983 ) ) ;
#16851=CARTESIAN_POINT ( 'NONE',  ( -1.865240315818168959, -3.450151633892079239, 3.842223568244830467 ) ) ;
#16853=B_SPLINE_CURVE_WITH_KNOTS ( 'NONE', 3,
 ( #705, #6257, #14680, #4960, #1998, #7744, #13300 ),
 .UNSPECIFIED., .F., .F.,
 ( 4, 1, 1, 1, 4 ),
 ( 0.000000000000000000, 0.3003308066897660278, 0.4325493167368040237, 0.5576349185195599301, 0.7853981633974479459 ),
 .UNSPECIFIED. ) ;
#16863=CARTESIAN_POINT ( 'NONE',  ( -0.9222751404131093178, -5.277754237288146300, 2.865854510788139908 ) ) ;
#16864=CARTESIAN_POINT ( 'NONE',  ( 0.2938780505771511620, -1.893677194936738806, 2.062434951628520086 ) ) ;
#16871=CARTESIAN_POINT ( 'NONE',  ( -0.4201920264140019956, -2.122719201459649874, 2.384360920086639801 ) ) ;
#16872=CARTESIAN_POINT ( 'NONE',  ( -1.810994336139479133, -2.918361879621429011, 5.667058093962724641 ) ) ;
#16873=CARTESIAN_POINT ( 'NONE',  ( 0.06367493584606445656, -0.001483050847457929866, 2.649999999999998579 ) ) ;
#16875=CARTESIAN_POINT ( 'NONE',  ( 2.011500846714319835, -0.3489406779661020086, 3.478373409938460448 ) ) ;
#16876=CARTESIAN_POINT ( 'NONE',  ( 2.345900685764729765, -0.3711864406779670222, 4.512231114381330066 ) ) ;
#16879=CARTESIAN_POINT ( 'NONE',  ( -1.641808337277740115, -0.1868644067796620123, 6.386111670537629514 ) ) ;
#16880=CARTESIAN_POINT ( 'NONE',  ( 0.7109160811436110450, -1.307629111369560171, 6.943511536198400336 ) ) ;
#16884=CARTESIAN_POINT ( 'NONE',  ( -0.7678268402137429227, -2.732055573315121055, 6.924676972266150088 ) ) ;
#16886=CARTESIAN_POINT ( 'NONE',  ( -0.1765068388402301069, -5.453177966101685037, 7.347961541693632803 ) ) ;
#16888=CARTESIAN_POINT ( 'NONE',  ( 1.303621121494459967, -1.237764246504700072, 6.659417683669679455 ) ) ;
#16889=CARTESIAN_POINT ( 'NONE',  ( 0.6964468257805941365, -0.4334745762711874617, 6.631228347243847132 ) ) ;
#16895=CARTESIAN_POINT ( 'NONE',  ( -2.033547680391670998, -4.641695212954759064, 4.417890669792460479 ) ) ;
#16900=CARTESIAN_POINT ( 'NONE',  ( 2.022304719220918479, -0.3667372881355940861, 4.346496488058688712 ) ) ;
#16901=CARTESIAN_POINT ( 'NONE',  ( 2.358786130710011086, -3.943046564306109669, 5.916240799583690979 ) ) ;
#16903=CARTESIAN_POINT ( 'NONE',  ( -2.022304719220918479, -5.233262711864406391, 4.346496488058700258 ) ) ;
#16910=CARTESIAN_POINT ( 'NONE',  ( -1.728413393879669968, -1.288181699441249828, 6.297289212178331042 ) ) ;
#16912=CARTESIAN_POINT ( 'NONE',  ( 1.668733558229380520, -0.8457042219637719294, 5.895922302771890777 ) ) ;
#16917=CARTESIAN_POINT ( 'NONE',  ( -0.06264882350515391107, -0.4512711864406790396, 7.052569299041220319 ) ) ;
#16918=CARTESIAN_POINT ( 'NONE',  ( -0.4790341583531910197, -3.683034516774959855, 2.395814251711740006 ) ) ;
#16928=CARTESIAN_POINT ( 'NONE',  ( 2.579602008086750775, -1.051457940198389673, 5.323511966907245707 ) ) ;
#16930=CARTESIAN_POINT ( 'NONE',  ( -2.343457872958619959, -1.451199717459269900, 4.916681529328609912 ) ) ;
#16932=CARTESIAN_POINT ( 'NONE',  ( 2.311987889326980294, -4.078935417675859654, 4.260161748947079552 ) ) ;
#16934=CARTESIAN_POINT ( 'NONE',  ( -2.051695471449629160, -3.333710192450643373, 4.773807418740784847 ) ) ;
#16938=CARTESIAN_POINT ( 'NONE',  ( -1.496290472746829803, -0.5672554343907050267, 2.872674968141029961 ) ) ;
#16947=CARTESIAN_POINT ( 'NONE',  ( 2.000624272291700034, -5.064194915254235596, 4.239366054775996595 ) ) ;
#16949=CARTESIAN_POINT ( 'NONE',  ( -2.105672170043390246, -1.637506023765568530, 3.084680091961149007 ) ) ;
#16956=CARTESIAN_POINT ( 'NONE',  ( -0.9485663501270049647, -3.054250732991179440, 6.853826262002260528 ) ) ;
#16957=CARTESIAN_POINT ( 'NONE',  ( -1.893291846171410331, -2.941650167909708458, 5.493944474033886749 ) ) ;
#16958=CARTESIAN_POINT ( 'NONE',  ( 1.754713504580569960, -0.04894067796610205440, 3.634325740584615883 ) ) ;
#16959=CARTESIAN_POINT ( 'NONE',  ( 2.180207327701309872, -0.3934322033898309812, 5.586116916730190063 ) ) ;
#16964=CARTESIAN_POINT ( 'NONE',  ( 0.06367493584606445656, -0.001483050847457929866, 2.649999999999998579 ) ) ;
#16965=CARTESIAN_POINT ( 'NONE',  ( -0.5320716618283710675, -3.007674156414609890, 6.992519451207139802 ) ) ;
#16969=CARTESIAN_POINT ( 'NONE',  ( 1.286937324407709804, -2.010118636378180224, 2.729584305145181133 ) ) ;
#16970=CARTESIAN_POINT ( 'NONE',  ( -1.128670402850159737, -5.470974576271190770, 7.101865548313641696 ) ) ;
#16973=CARTESIAN_POINT ( 'NONE',  ( 0.8731223871105069367, -0.4290254237288141370, 6.558046933601105799 ) ) ;
#16978=CARTESIAN_POINT ( 'NONE',  ( 1.102492180652039577, -2.309025507765959606, 2.968118700883580541 ) ) ;
#16980=CARTESIAN_POINT ( 'NONE',  ( 2.484260633728970546, -0.3578389830508479363, 3.766563288620793593 ) ) ;
#16984=CARTESIAN_POINT ( 'NONE',  ( -1.229686204202100175, -5.164643153926309793, 2.674737924334550154 ) ) ;
#16985=CARTESIAN_POINT ( 'NONE',  ( 2.328217775191430139, -5.381991525423729605, 5.043379051721160522 ) ) ;
#16988=CARTESIAN_POINT ( 'NONE',  ( 2.353194804772640314, -0.07563559322033941434, 4.731327187377229571 ) ) ;
#16989=CARTESIAN_POINT ( 'NONE',  ( -0.3743405594629430344, -5.457627118644070130, 7.023440622744399953 ) ) ;
#16993=CARTESIAN_POINT ( 'NONE',  ( -2.260890494820599894, -1.544352870612419881, 4.046455925041199997 ) ) ;
#16995=CARTESIAN_POINT ( 'NONE',  ( 1.423520578776751533, -2.056695212954759100, 3.220645071516909930 ) ) ;
#16999=CARTESIAN_POINT ( 'NONE',  ( 2.638803263991410741, -0.08008474576271243373, 4.982085668537405532 ) ) ;
#17000=CARTESIAN_POINT ( 'NONE',  ( -0.2620510901103649815, -3.706322805063249959, 2.361180871966390260 ) ) ;
#17003=CARTESIAN_POINT ( 'NONE',  ( -0.08231150243516484333, -5.298516949152545230, 2.050000000000001155 ) ) ;
#17011=CARTESIAN_POINT ( 'NONE',  ( 1.864786684738361178, -0.7952867690272195089, 2.817120744449660652 ) ) ;
#17014=CARTESIAN_POINT ( 'NONE',  ( 0.6864473529425539899, -1.008722239981789892, 6.951118770549889803 ) ) ;
#17016=CARTESIAN_POINT ( 'NONE',  ( -2.351999299633229956, -3.333710192450639820, 4.782734406438290620 ) ) ;
#17018=CARTESIAN_POINT ( 'NONE',  ( 1.831349212334668852, -4.009070552811004440, 3.772065786216904026 ) ) ;
#17028=CARTESIAN_POINT ( 'NONE',  ( -2.046424002475610404, -5.228813559322024851, 4.536201610417774255 ) ) ;
#17032=CARTESIAN_POINT ( 'NONE',  ( -1.385366411767399608, -5.164643153926310681, 2.415423146782709640 ) ) ;
#17036=CARTESIAN_POINT ( 'NONE',  ( 2.075124426334590044, -2.681638120378570189, 5.810227140144509583 ) ) ;
#17037=CARTESIAN_POINT ( 'NONE',  ( -1.959085573314230055, -2.964938456198001671, 5.313910057793616026 ) ) ;
#17045=CARTESIAN_POINT ( 'NONE',  ( -2.351526912647309953, -0.2269067796610169940, 4.606040641882809261 ) ) ;
#17046=CARTESIAN_POINT ( 'NONE',  ( 2.301223891756920104, -2.611773255513699876, 5.193066210047949660 ) ) ;
#17048=AXIS2_PLACEMENT_3D ( 'NONE', #10364, #7685, #3330 ) ;
#17052=CARTESIAN_POINT ( 'NONE',  ( 2.340959815966380031, -3.849893411152960354, 4.942183458383420991 ) ) ;
#17054=CARTESIAN_POINT ( 'NONE',  ( 2.586172839791708533, -5.364194915254235418, 4.104546363490930716 ) ) ;
#17055=ORIENTED_EDGE ( 'NONE', *, *, #10868, .T. ) ;
#17056=CARTESIAN_POINT ( 'NONE',  ( -1.795861365445549973, -0.5491525423728815802, 3.705232155007899930 ) ) ;
#17062=CARTESIAN_POINT ( 'NONE',  ( -0.9123513484652393535, -2.052854336594789331, 2.860838000723768815 ) ) ;
#17072=CARTESIAN_POINT ( 'NONE',  ( -0.3803919826357066158, -5.591101694915256104, 2.682580100125310896 ) ) ;
#17074=CARTESIAN_POINT ( 'NONE',  ( 1.978267656359408821, -0.1023305084745769755, 5.974740860598791947 ) ) ;
#17078=CARTESIAN_POINT ( 'NONE',  ( 2.349464193210359930, -2.243001519261070165, 4.563019372514570016 ) ) ;
#17080=CARTESIAN_POINT ( 'NONE',  ( -1.058024172752510594, -1.730659176918718956, 2.940600473883360433 ) ) ;
#17088=CARTESIAN_POINT ( 'NONE',  ( -2.650076489488250697, -0.5224576271186435195, 4.841243018609314497 ) ) ;
#17089=CARTESIAN_POINT ( 'NONE',  ( 0.6150581927482109412, -4.451548030288480895, 6.971662190339319665 ) ) ;
#17092=CARTESIAN_POINT ( 'NONE',  ( 2.234315482767910144, -5.059745762711860273, 3.960850823455320580 ) ) ;
#17101=CARTESIAN_POINT ( 'NONE',  ( 2.516451517878131927, -0.9117282104686613708, 3.857037693030633818 ) ) ;
#17103=CARTESIAN_POINT ( 'NONE',  ( 1.882879255550339082, -0.4963798976394455664, 2.835213315261639000 ) ) ;
#17105=CARTESIAN_POINT ( 'NONE',  ( 2.349464193210359930, -2.243001519261070165, 4.563019372514570016 ) ) ;
#17108=CARTESIAN_POINT ( 'NONE',  ( 1.866416942370620058, -3.962493976234419790, 3.266391446483460026 ) ) ;
#17120=CARTESIAN_POINT ( 'NONE',  ( -1.725722849164588624, -5.497669491525425833, 5.812007984777676661 ) ) ;
#17121=CARTESIAN_POINT ( 'NONE',  ( -1.630703155447540631, -3.267686203945749490, 2.606218513833090000 ) ) ;
#17125=CARTESIAN_POINT ( 'NONE',  ( -0.9138909625329535436, -4.911779243796845051, 2.204775695797560164 ) ) ;
#17128=CARTESIAN_POINT ( 'NONE',  ( 1.764807890102179977, -2.378890372630820149, 3.143016121304719857 ) ) ;
#17129=CARTESIAN_POINT ( 'NONE',  ( 1.883235269974540937, -2.359442960702510472, 5.517512544583896172 ) ) ;
#17130=CARTESIAN_POINT ( 'NONE',  ( 0.004026115436751699292, -5.086189479527880586, 2.487698411374999807 ) ) ;
#17135=CARTESIAN_POINT ( 'NONE',  ( -2.350067830300900162, -0.2224576271186440024, 4.825253242917699303 ) ) ;
#17136=CARTESIAN_POINT ( 'NONE',  ( -2.182690844914350059, -1.680241723982170088, 5.580117243900479806 ) ) ;
#17140=CARTESIAN_POINT ( 'NONE',  ( -2.211317922628891264, -3.127956474216019966, 3.894507149290469705 ) ) ;
#17141=CARTESIAN_POINT ( 'NONE',  ( 2.519547246525509543, -5.059745762711855832, 3.866491354109194756 ) ) ;
#17145=CARTESIAN_POINT ( 'NONE',  ( 0.4360591020457930123, -0.3088983050847460277, 2.387347919655840034 ) ) ;
#17149=CARTESIAN_POINT ( 'NONE',  ( 0.8493734496528324573, -2.844656138396588929, 6.569081749323157915 ) ) ;
#17157=CARTESIAN_POINT ( 'NONE',  ( 1.925796468768800063, -5.404237288135590234, 6.052706598917719560 ) ) ;
#17160=CARTESIAN_POINT ( 'NONE',  ( -2.328217775191430139, -0.2180084745762720932, 5.043379051721168516 ) ) ;
#17167=CARTESIAN_POINT ( 'NONE',  ( -0.1824815401349519917, -1.101875393134939873, 7.046368721022739479 ) ) ;
#17170=CARTESIAN_POINT ( 'NONE',  ( 2.049636678546640667, -2.243001519261071053, 4.582138519505345009 ) ) ;
#17174=CARTESIAN_POINT ( 'NONE',  ( 0.9664230948141925293, -0.01779661016949178609, 2.228384861502251457 ) ) ;
#17175=CARTESIAN_POINT ( 'NONE',  ( -2.033393610350109793, -4.777584066324510381, 5.884928737465370041 ) ) ;
#17178=CARTESIAN_POINT ( 'NONE',  ( 2.155845792290829621, -5.055296610169490279, 3.756158857535770057 ) ) ;
#17180=ORIENTED_EDGE ( 'NONE', *, *, #11743, .T. ) ;
#17185=CARTESIAN_POINT ( 'NONE',  ( 1.853635285637830865, -1.191187669928120529, 6.599249831075482575 ) ) ;
#17188=CARTESIAN_POINT ( 'NONE',  ( -0.1226612266410539998, -2.662190708450249854, 7.050255286338659388 ) ) ;
#17190=CARTESIAN_POINT ( 'NONE',  ( 2.316126390218360420, -0.8651516338920848259, 3.404364157709320438 ) ) ;
#17192=CARTESIAN_POINT ( 'NONE',  ( -1.503462833636818541, -5.095857339597785973, 3.304888304972901647 ) ) ;
#17195=ORIENTED_EDGE ( 'NONE', *, *, #11912, .F. ) ;
#17201=CARTESIAN_POINT ( 'NONE',  ( 1.949083719010301197, -5.359745762711870753, 4.055210292801453953 ) ) ;
#17202=CARTESIAN_POINT ( 'NONE',  ( -0.7540633504678314614, -3.360839357098899693, 2.155495695330209127 ) ) ;
#17206=CARTESIAN_POINT ( 'NONE',  ( 1.936998685628529948, -0.8418633456037969420, 3.363294429306519895 ) ) ;
#17208=CARTESIAN_POINT ( 'NONE',  ( 0.1226612266411070129, -2.937809291549740021, 7.050255286338659388 ) ) ;
#17209=CARTESIAN_POINT ( 'NONE',  ( 0.8735826871841618768, -4.106064582324130185, 6.557889967484662463 ) ) ;
#17210=CARTESIAN_POINT ( 'NONE',  ( 1.921786527979010062, -0.05783898305084796132, 3.977907449687776431 ) ) ;
#17215=CARTESIAN_POINT ( 'NONE',  ( -0.5606293434988356417, -4.269082600342137823, 7.293994686233948421 ) ) ;
#17216=CARTESIAN_POINT ( 'NONE',  ( 2.052786957354850728, -0.07563559322033948373, 4.727327971967373976 ) ) ;
#17217=CARTESIAN_POINT ( 'NONE',  ( 1.962536940652990003, -2.704926408666860294, 5.998920491814760503 ) ) ;
#17220=CARTESIAN_POINT ( 'NONE',  ( 1.981271652668328720, -3.966334852594400662, 5.970160748022401265 ) ) ;
#17222=CARTESIAN_POINT ( 'NONE',  ( -2.540842781840720654, -5.211016949152535993, 5.466141598148674952 ) ) ;
#17227=CARTESIAN_POINT ( 'NONE',  ( -2.286166334984490067, -0.5135593220338989795, 5.258525443163870605 ) ) ;
#17231=CARTESIAN_POINT ( 'NONE',  ( -1.951270856817509003, -3.263845327585779277, 5.338313313320930398 ) ) ;
#17232=CARTESIAN_POINT ( 'NONE',  ( 2.614198783383141045, -0.3667372881355940861, 4.243032045539284702 ) ) ;
#17236=CARTESIAN_POINT ( 'NONE',  ( 1.489797906646480596, -0.4112288135593234473, 6.112509577910826941 ) ) ;
#17239=CARTESIAN_POINT ( 'NONE',  ( -2.012177589105470066, -5.515466101694915579, 5.107213040360599088 ) ) ;
#17241=CARTESIAN_POINT ( 'NONE',  ( -2.058670345754649134, -0.2491525423728820077, 3.559656372813929881 ) ) ;
#17242=CARTESIAN_POINT ( 'NONE',  ( -0.5058614788087384406, -0.2909039927201511055, 2.084176093893880921 ) ) ;
#17243=CARTESIAN_POINT ( 'NONE',  ( -0.5355577887185811736, -4.567989471729919870, 7.299286738308172318 ) ) ;
#17246=CARTESIAN_POINT ( 'NONE',  ( 1.777964140657680048, -0.8689925102520590361, 6.241943319976220650 ) ) ;
#17248=CARTESIAN_POINT ( 'NONE',  ( 1.313542260532459149, -2.475884402143949892, 6.277817661335856059 ) ) ;
#17255=CARTESIAN_POINT ( 'NONE',  ( 2.159308672244681482, -0.8457042219637719294, 6.242886823772496818 ) ) ;
#17257=CARTESIAN_POINT ( 'NONE',  ( -2.065623031241579977, -5.033755237495680213, 3.572193642975310279 ) ) ;
#17269=CARTESIAN_POINT ( 'NONE',  ( -1.991984774470509922, -1.614217735477279980, 3.446707398186049875 ) ) ;
#17270=CARTESIAN_POINT ( 'NONE',  ( 1.534924416212170017, -5.333856471232000018, 2.911460733964629899 ) ) ;
#17272=CARTESIAN_POINT ( 'NONE',  ( -1.670747221194380128, -5.103620102360550526, 3.047345349617600174 ) ) ;
#17274=CARTESIAN_POINT ( 'NONE',  ( 2.053221424930760097, -0.8651516338920849369, 3.549770689668250157 ) ) ;
#17284=CARTESIAN_POINT ( 'NONE',  ( 1.679950111053631900, -5.404237288135596451, 5.880020650119711867 ) ) ;
#17287=CARTESIAN_POINT ( 'NONE',  ( -0.6265155281652096120, -2.708767285026830951, 7.278874170247493502 ) ) ;
#17293=CARTESIAN_POINT ( 'NONE',  ( -2.135041058613629694, -4.800872354612799597, 5.690123914223820023 ) ) ;
#17294=CARTESIAN_POINT ( 'NONE',  ( -1.998374131852739266, -4.664983501243040287, 4.229465546630535755 ) ) ;
#17297=CARTESIAN_POINT ( 'NONE',  ( -0.007508403481304109714, -5.269001837275429700, 2.444053578789410430 ) ) ;
#17300=CARTESIAN_POINT ( 'NONE',  ( 0.7137241095604313079, -3.500569086828633658, 2.143887406933319362 ) ) ;
#17301=CARTESIAN_POINT ( 'NONE',  ( -1.994315313497099229, -0.2135593220338991571, 5.187224322759965922 ) ) ;
#17302=CARTESIAN_POINT ( 'NONE',  ( 2.352760675243219968, -2.565196678937129882, 4.757121734156020132 ) ) ;
#17309=CARTESIAN_POINT ( 'NONE',  ( 1.854177340199709478, -3.989623140882689434, 6.149404042554680316 ) ) ;
#17311=CARTESIAN_POINT ( 'NONE',  ( -2.230812463554230352, -5.197669491525426011, 6.137473736419926773 ) ) ;
#17316=CARTESIAN_POINT ( 'NONE',  ( -0.4974685680287780354, -0.4601694915254240237, 7.000224381598740386 ) ) ;
#17321=CARTESIAN_POINT ( 'NONE',  ( -0.2739924515130059968, -2.984385868126320673, 6.734657214162127481 ) ) ;
#17322=CARTESIAN_POINT ( 'NONE',  ( 2.653602652190420574, -0.07563559322033948373, 4.735326402787084277 ) ) ;
#17325=CARTESIAN_POINT ( 'NONE',  ( -1.670747221194377685, -5.103620102360557631, 3.047345349617607724 ) ) ;
#17332=CARTESIAN_POINT ( 'NONE',  ( 1.300961508564179914, -5.422033898305079092, 6.661123742937279602 ) ) ;
#17336=CARTESIAN_POINT ( 'NONE',  ( 0.9250303514740658706, -3.822764246504686270, 2.212544966868020602 ) ) ;
#17338=CARTESIAN_POINT ( 'NONE',  ( 1.332058588847409908, -2.499172690432239996, 6.640197310420189680 ) ) ;
#17342=CARTESIAN_POINT ( 'NONE',  ( 0.03895741673415010348, -1.870388906648449812, 2.647347042895590086 ) ) ;
#17350=CARTESIAN_POINT ( 'NONE',  ( -2.105672170043390246, -1.637506023765568530, 3.084680091961149007 ) ) ;
#17352=CARTESIAN_POINT ( 'NONE',  ( 2.102728310581320148, -4.241953435693879726, 5.757014351541050345 ) ) ;
#17355=CARTESIAN_POINT ( 'NONE',  ( 2.043308330018790198, -5.099788135593220417, 5.867646457774659652 ) ) ;
#17366=CARTESIAN_POINT ( 'NONE',  ( -1.788074174585561060, -1.982989471729918352, 2.738902236199820539 ) ) ;
#17372=CARTESIAN_POINT ( 'NONE',  ( -0.5570002967655939274, -2.708767285026830063, 6.986590552960220357 ) ) ;
#17374=CARTESIAN_POINT ( 'NONE',  ( 0.5803392541454069908, -5.011796459788059543, 2.403119802722879950 ) ) ;
#17376=CARTESIAN_POINT ( 'NONE',  ( -1.351547610267091581, -1.517223705964159786, 6.983951126925262542 ) ) ;
#17379=CARTESIAN_POINT ( 'NONE',  ( -1.458615186838411626, -5.103620102360555855, 3.259477383973569786 ) ) ;
#17392=CARTESIAN_POINT ( 'NONE',  ( -2.237394498046660019, -3.263845327585780165, 5.429939413646380331 ) ) ;
#17395=CARTESIAN_POINT ( 'NONE',  ( 2.293398556041700065, -5.364194915254239859, 4.171956209133470317 ) ) ;
#17398=CARTESIAN_POINT ( 'NONE',  ( -1.854177340199669954, -1.610376859117309989, 6.149404042554720284 ) ) ;
#17399=CARTESIAN_POINT ( 'NONE',  ( 1.866416942370620058, -3.962493976234419790, 3.266391446483460026 ) ) ;
#17400=CARTESIAN_POINT ( 'NONE',  ( 1.998374131852729940, -0.9350164987569505870, 4.229465546630494011 ) ) ;
#17404=CARTESIAN_POINT ( 'NONE',  ( 1.754713504580569960, -0.3489406779661023417, 3.634325740584615883 ) ) ;
#17405=CARTESIAN_POINT ( 'NONE',  ( -2.237394498046660019, -3.263845327585780165, 5.429939413646380331 ) ) ;
#17411=CARTESIAN_POINT ( 'NONE',  ( 0.8429265834919228428, -3.523857375116919766, 2.502678798553440220 ) ) ;
#17412=CARTESIAN_POINT ( 'NONE',  ( 0.7998959936908462964, -5.135381355932194580, 7.230419212249866945 ) ) ;
#17416=CARTESIAN_POINT ( 'NONE',  ( 2.253200202764420013, -0.3889830508474579895, 5.379408587037500133 ) ) ;
#17420=CARTESIAN_POINT ( 'NONE',  ( 1.503314099254039471, -3.939205687946139900, 3.301805249039985402 ) ) ;
#17422=CARTESIAN_POINT ( 'NONE',  ( -2.630358833876468960, -0.5313559322033900578, 4.347767980622416317 ) ) ;
#17424=CARTESIAN_POINT ( 'NONE',  ( 0.07299321914061039640, -0.3014830508474579673, 2.350000000000000089 ) ) ;
#17428=CARTESIAN_POINT ( 'NONE',  ( 0.009451942938127287294, -0.3001947080680037461, 2.339951117924002233 ) ) ;
#17433=CARTESIAN_POINT ( 'NONE',  ( -0.2938780505772099483, -3.706322805063249959, 2.062434951628528523 ) ) ;
#17436=CARTESIAN_POINT ( 'NONE',  ( -0.4539185741479770386, -3.384127645387189798, 2.390735265170449875 ) ) ;
#17439=CARTESIAN_POINT ( 'NONE',  ( -1.566607907718199577, -4.432100618360157007, 6.026891670824300107 ) ) ;
#17441=CARTESIAN_POINT ( 'NONE',  ( -1.909909196654771213, -1.567641158900710430, 3.946907241329710381 ) ) ;
#17444=CARTESIAN_POINT ( 'NONE',  ( 0.9724415447670879953, -0.7068739681193980662, 2.553509270169310064 ) ) ;
#17445=CARTESIAN_POINT ( 'NONE',  ( -2.471388659209118543, -1.381334852594401363, 5.667135868497515716 ) ) ;
#17447=CARTESIAN_POINT ( 'NONE',  ( -2.334748642087669523, -4.940602084342530453, 4.403867486184871005 ) ) ;
#17450=CARTESIAN_POINT ( 'NONE',  ( -1.378221871957430178, -5.179872881355930048, 6.607619368096279366 ) ) ;
#17458=CARTESIAN_POINT ( 'NONE',  ( -2.556942001999829905, -1.843259742000191048, 3.989253004641622358 ) ) ;
#17461=CARTESIAN_POINT ( 'NONE',  ( 1.465095039565329937, -2.033406924666469884, 2.858195935359850282 ) ) ;
#17462=CARTESIAN_POINT ( 'NONE',  ( 1.873832970144350130, -5.337500000000000355, 2.826167029855650270 ) ) ;
#17464=CARTESIAN_POINT ( 'NONE',  ( 2.022685914314938938, -1.167899381639830203, 6.418096442297061444 ) ) ;
#17466=CARTESIAN_POINT ( 'NONE',  ( 0.5889081234606849957, -0.4379237288135600092, 6.978529000034869867 ) ) ;
#17475=CARTESIAN_POINT ( 'NONE',  ( -2.267872052190610166, -1.843259742000189938, 4.071110468860649867 ) ) ;
#17479=CARTESIAN_POINT ( 'NONE',  ( 2.351212046067109984, -0.9815930753335269099, 4.597298481426010497 ) ) ;
#17480=CARTESIAN_POINT ( 'NONE',  ( -1.465095039565370127, -3.566593075333519991, 2.858195935359880480 ) ) ;
#17481=CARTESIAN_POINT ( 'NONE',  ( 1.785776242921180756, -1.121322805063259542, 5.712869711683790541 ) ) ;
#17488=CARTESIAN_POINT ( 'NONE',  ( 0.9222751404130974384, -0.3222457627118649470, 2.865854510788131027 ) ) ;
#17489=CARTESIAN_POINT ( 'NONE',  ( 0.1824815401350060040, -4.498124606865050445, 7.046368721022729709 ) ) ;
#17496=CARTESIAN_POINT ( 'NONE',  ( -1.704669856830349772, -4.796950468210010143, 3.080704711052660194 ) ) ;
#17498=CARTESIAN_POINT ( 'NONE',  ( -1.973760952634090238, -5.559957627118640389, 2.925986839873730982 ) ) ;
#17500=CARTESIAN_POINT ( 'NONE',  ( 0.1565249325564390115, -0.4468220338983060480, 7.048192310558509810 ) ) ;
#17501=VERTEX_POINT ( 'NONE', #3754 ) ;
#17504=CARTESIAN_POINT ( 'NONE',  ( 0.7128755192781456307, -3.822764246504686270, 2.774718115017441367 ) ) ;
#17505=CARTESIAN_POINT ( 'NONE',  ( 2.354888465609351389, -0.09788135593220394226, 5.923664702843856489 ) ) ;
#17507=FACE_OUTER_BOUND ( 'NONE', #10947, .T. ) ;
#17510=CARTESIAN_POINT ( 'NONE',  ( 2.638803263991410741, -0.3800847457627119508, 4.982085668537405532 ) ) ;
#17512=CARTESIAN_POINT ( 'NONE',  ( 1.112838723655040107, -5.426483050847459744, 6.773667561836210105 ) ) ;
#17513=CARTESIAN_POINT ( 'NONE',  ( -2.234315482767909700, -0.2402542372881359967, 3.960850823455329905 ) ) ;
#17514=CARTESIAN_POINT ( 'NONE',  ( -0.7756407636288503715, -4.591277760018214416, 7.238010066725332869 ) ) ;
#17516=CARTESIAN_POINT ( 'NONE',  ( -1.444955263746759977, -3.267686203945750378, 2.842353646881510265 ) ) ;
#17519=CARTESIAN_POINT ( 'NONE',  ( -1.404946080800599351, -3.244397915657463827, 3.202993536195951840 ) ) ;
#17521=CARTESIAN_POINT ( 'NONE',  ( -1.224086244040909488, -1.241605122864670285, 6.348185277745776567 ) ) ;
#17526=ORIENTED_EDGE ( 'NONE', *, *, #9832, .F. ) ;
#17530=CARTESIAN_POINT ( 'NONE',  ( -0.6493550500446439999, -5.286652542372879182, 2.437955526623099889 ) ) ;
#17538=CARTESIAN_POINT ( 'NONE',  ( -0.8400312909772689185, -3.030962444702889780, 7.217431453521816920 ) ) ;
#17541=CARTESIAN_POINT ( 'NONE',  ( 2.308170020371300257, -3.873181699441239800, 5.159452766389609479 ) ) ;
#17542=CARTESIAN_POINT ( 'NONE',  ( 0.009452110982655418520, -5.000192044704539818, 2.350000000000000089 ) ) ;
#17543=CARTESIAN_POINT ( 'NONE',  ( -2.644456467089570939, -1.796683165423619055, 4.476474416072687035 ) ) ;
#17550=ORIENTED_EDGE ( 'NONE', *, *, #3364, .F. ) ;
#17556=CARTESIAN_POINT ( 'NONE',  ( -1.507201387235980183, -3.124115597856050197, 6.507509243627219497 ) ) ;
#17557=CARTESIAN_POINT ( 'NONE',  ( 0.7093417302541469294, -5.435381355932199732, 6.943956659919690466 ) ) ;
#17560=CARTESIAN_POINT ( 'NONE',  ( 1.115198193348289957, -1.261052534792989954, 6.772457159276550342 ) ) ;
#17561=CARTESIAN_POINT ( 'NONE',  ( 1.397172971746949877, -3.892629111369559691, 2.806153814454899642 ) ) ;
#17562=CARTESIAN_POINT ( 'NONE',  ( 1.138568046961060176, -1.237764246504700072, 6.408380708468512488 ) ) ;
#17566=CARTESIAN_POINT ( 'NONE',  ( 0.06367493584606445656, -0.3014830508474583004, 2.649999999999998579 ) ) ;
#17567=CARTESIAN_POINT ( 'NONE',  ( 2.192143888961729736, -4.218665147405599392, 5.556300681753580051 ) ) ;
#17572=CARTESIAN_POINT ( 'NONE',  ( -2.351212046067109984, -4.618406924666470736, 4.597298481426070893 ) ) ;
#17573=CARTESIAN_POINT ( 'NONE',  ( 2.332582362116870200, -5.068644067796610031, 4.387643303570810005 ) ) ;
#17575=CARTESIAN_POINT ( 'NONE',  ( 1.000896394980339998, -0.4290254237288140260, 6.829956240957369751 ) ) ;
#17579=EDGE_CURVE ( 'NONE', #12508, #4345, #4956, .T. ) ;
#17580=CARTESIAN_POINT ( 'NONE',  ( -0.4114611322411360628, -4.567989471729919870, 6.711368086473216366 ) ) ;
#17582=CARTESIAN_POINT ( 'NONE',  ( -2.508228811380011081, -0.5091101694915260989, 5.566973598334550744 ) ) ;
#17584=CARTESIAN_POINT ( 'NONE',  ( 0.8570167067220200163, -0.3177966101694920664, 2.508190348879349774 ) ) ;
#17586=CARTESIAN_POINT ( 'NONE',  ( -0.07064654565474801085, -0.4512711864406789841, 7.352897294663512717 ) ) ;
#17588=CARTESIAN_POINT ( 'NONE',  ( -3.408368997776849933E-15, -5.599999999999999645, 2.350000000000000089 ) ) ;
#17589=AXIS2_PLACEMENT_3D ( 'NONE', #8026, #7571, #11647 ) ;
#17590=CARTESIAN_POINT ( 'NONE',  ( -1.219286470748950135, -1.218316834576380403, 6.712979431025679844 ) ) ;
#17591=CARTESIAN_POINT ( 'NONE',  ( -0.3897427956305680175, -0.2909039927201511055, 2.676097687607990938 ) ) ;
#17592=CARTESIAN_POINT ( 'NONE',  ( 1.769056124370469885, -3.915917399657852904, 2.721729512470748791 ) ) ;
#17595=CARTESIAN_POINT ( 'NONE',  ( -0.009452110982656853136, -5.299807955295470663, 2.649999999999998579 ) ) ;
#17596=CARTESIAN_POINT ( 'NONE',  ( 2.199335452462550133, -3.733451969711520491, 3.862342996790889771 ) ) ;
#17601=CARTESIAN_POINT ( 'NONE',  ( 1.079900583135640302, -3.570433951693503527, 2.953942563037689428 ) ) ;
#17606=CARTESIAN_POINT ( 'NONE',  ( -1.627161714697918704, -1.637506023765568530, 3.448102801005849649 ) ) ;
#17607=ORIENTED_EDGE ( 'NONE', *, *, #6435, .T. ) ;
#17610=CARTESIAN_POINT ( 'NONE',  ( -1.155768864438580179, -1.195028546288090743, 7.088998121597467339 ) ) ;
#17616=CARTESIAN_POINT ( 'NONE',  ( 1.880631435828169939, -5.055296610169490279, 3.876649216148224220 ) ) ;
#17624=CARTESIAN_POINT ( 'NONE',  ( -1.846259792136611066, -5.546610169491530407, 3.802221692020929744 ) ) ;
#17626=CARTESIAN_POINT ( 'NONE',  ( -0.1366863161730529075, -2.662190708450249854, 7.350364228549148393 ) ) ;
#17627=CARTESIAN_POINT ( 'NONE',  ( 1.428323476796560465, -2.309025507765959606, 2.463260019887501429 ) ) ;
#17632=CARTESIAN_POINT ( 'NONE',  ( 2.267872052190590182, -3.756740257999799937, 4.071110468860600129 ) ) ;
#17636=CARTESIAN_POINT ( 'NONE',  ( -1.071153154657450202, -3.054250732991181216, 7.128115444592631356 ) ) ;
#17642=CARTESIAN_POINT ( 'NONE',  ( 2.046174187462399985, -1.121322805063259986, 5.862719605943959245 ) ) ;
#17644=CARTESIAN_POINT ( 'NONE',  ( 2.321479326063749404, -5.350847457627126325, 3.414080590619961608 ) ) ;
#17655=CARTESIAN_POINT ( 'NONE',  ( -1.332058588847369940, -3.100827309567760537, 6.640197310420220767 ) ) ;
#17661=CARTESIAN_POINT ( 'NONE',  ( -1.881914957835490121, -1.936412895153350133, 3.286797332666350435 ) ) ;
#17662=CARTESIAN_POINT ( 'NONE',  ( 2.343457872958619959, -4.148800282540729967, 4.916681529328559286 ) ) ;
#17664=CARTESIAN_POINT ( 'NONE',  ( -1.642659730162759901, -1.936412895153350133, 3.468508687188699646 ) ) ;
#17670=CARTESIAN_POINT ( 'NONE',  ( -2.062913653388399826, -3.217268751009200400, 5.832754583370829415 ) ) ;
#17678=CARTESIAN_POINT ( 'NONE',  ( -1.707817112497179934, -5.188771186440679806, 6.319218296629480314 ) ) ;
#17681=AXIS2_PLACEMENT_3D ( 'NONE', #11191, #16836, #4146 ) ;
#17683=CARTESIAN_POINT ( 'NONE',  ( -0.9516466452860307124, -4.637854336594775084, 6.519140045500596337 ) ) ;
#17685=CARTESIAN_POINT ( 'NONE',  ( -0.5609751937345790473, -0.4601694915254239682, 7.293870047334757523 ) ) ;
#17687=CARTESIAN_POINT ( 'NONE',  ( 2.203023580853990193, -0.3578389830508479919, 3.872235369154280349 ) ) ;
#17689=CARTESIAN_POINT ( 'NONE',  ( -1.134881315981510541, -0.4779661016949154906, 6.410767520434657918 ) ) ;
#17690=CARTESIAN_POINT ( 'NONE',  ( -2.171642826483958899, -0.1957627118644069686, 6.225392547715731695 ) ) ;
#17694=CARTESIAN_POINT ( 'NONE',  ( 2.484260633728970546, -0.3578389830508479363, 3.766563288620793593 ) ) ;
#17695=CARTESIAN_POINT ( 'NONE',  ( 2.135041058613649234, -0.7991276453871951624, 5.690123914223770285 ) ) ;
#17697=CARTESIAN_POINT ( 'NONE',  ( 2.332582362116870200, -5.368644067796609853, 4.387643303570810005 ) ) ;
#17698=CARTESIAN_POINT ( 'NONE',  ( -1.940935473245981147, -5.095857339597785973, 2.893832807158200016 ) ) ;
#17702=CARTESIAN_POINT ( 'NONE',  ( -1.962536940652960027, -2.895073591333140239, 5.998920491814800471 ) ) ;
#17703=CARTESIAN_POINT ( 'NONE',  ( 2.107551805806971323, -4.288530012270460823, 6.312866726931170902 ) ) ;
#17706=CARTESIAN_POINT ( 'NONE',  ( 1.750352751699790987, -3.686875393134939394, 3.627075451280439733 ) ) ;
#17709=CARTESIAN_POINT ( 'NONE',  ( 0.4194839839381755975, -1.916965483225031130, 2.690289814463930895 ) ) ;
#17713=ADVANCED_FACE ( 'NONE', ( #9681 ), #14798, .T. ) ;
#17714=CARTESIAN_POINT ( 'NONE',  ( 0.4904671284965613776, -0.6606104644819267291, 2.692290850878278796 ) ) ;
#17715=CARTESIAN_POINT ( 'NONE',  ( 0.3578984759184136166, -2.615614131873680748, 7.329643012642057087 ) ) ;
#17719=CARTESIAN_POINT ( 'NONE',  ( 1.928817277882869829, -1.144611093351550091, 6.048484184565929844 ) ) ;
#17720=FACE_OUTER_BOUND ( 'NONE', #8788, .T. ) ;
#17721=CARTESIAN_POINT ( 'NONE',  ( 1.112838723655040107, -5.126483050847459921, 6.773667561836210105 ) ) ;
#17730=CARTESIAN_POINT ( 'NONE',  ( -1.754713504580578842, -5.551059322033894183, 3.634325740584633646 ) ) ;
#17732=CARTESIAN_POINT ( 'NONE',  ( -0.9880847989278745969, -3.337551068810613142, 2.236912075639700515 ) ) ;
#17733=CARTESIAN_POINT ( 'NONE',  ( 0.9930264841371563289, -0.4076464065212259125, 2.562902636367420772 ) ) ;
#17737=CARTESIAN_POINT ( 'NONE',  ( 1.381042549632460092, -4.059488005747549977, 6.605640880016110827 ) ) ;
#17740=CARTESIAN_POINT ( 'NONE',  ( -0.4722227023514615762, -2.122719201459649874, 2.088464165977090836 ) ) ;
#17744=CARTESIAN_POINT ( 'NONE',  ( 1.444955263746720009, -2.332313796054249710, 2.842353646881480511 ) ) ;
#17745=CARTESIAN_POINT ( 'NONE',  ( -2.350067830300900162, -0.5224576271186440746, 4.825253242917699303 ) ) ;
#17748=PRODUCT ( 'Actuator Return Helical Spring', 'Actuator Return Helical Spring', '', ( #11592 ) ) ;
#17755=CARTESIAN_POINT ( 'NONE',  ( 0.9719602541832789155, -2.844656138396589817, 6.843370931913530519 ) ) ;
#17757=CARTESIAN_POINT ( 'NONE',  ( -0.5889081234606770021, -5.462076271186440124, 6.978529000034869867 ) ) ;
#17759=CARTESIAN_POINT ( 'NONE',  ( -0.2023972492402590084, -2.146007489747939978, 2.355265251465770149 ) ) ;
#17761=CARTESIAN_POINT ( 'NONE',  ( -1.079900583135680714, -2.029566048306499670, 2.953942563037710300 ) ) ;
#17765=CARTESIAN_POINT ( 'NONE',  ( 1.569888143820300064, -0.7356046962096609576, 3.119244292431920140 ) ) ;
#17768=CARTESIAN_POINT ( 'NONE',  ( 1.728413393879709936, -4.311818300558750039, 6.297289212178290185 ) ) ;
#17774=CARTESIAN_POINT ( 'NONE',  ( 1.811729841638690219, -5.041949152542369639, 3.197954009834290012 ) ) ;
#17777=CARTESIAN_POINT ( 'NONE',  ( -2.190084968185500358, -1.567641158900710208, 3.838447030292489792 ) ) ;
#17779=CARTESIAN_POINT ( 'NONE',  ( -1.417606053559450352, -4.707719201459645397, 6.185023541745952258 ) ) ;
#17780=CARTESIAN_POINT ( 'NONE',  ( 0.3743405594629510280, -0.1423728813559329842, 7.023440622744399953 ) ) ;
#17782=CARTESIAN_POINT ( 'NONE',  ( -1.562863241354461641, -0.4913135593220345210, 6.031217337312382298 ) ) ;
#17783=CARTESIAN_POINT ( 'NONE',  ( 0.6493550500446280127, -0.01334745762711890028, 2.437955526623099889 ) ) ;
#17785=CARTESIAN_POINT ( 'NONE',  ( -1.889104232906369862, -5.555508474576269506, 3.296507079072529933 ) ) ;
#17787=CARTESIAN_POINT ( 'NONE',  ( -1.305383194095490307, -0.5672554343907051377, 3.106059597508353143 ) ) ;
#17788=CARTESIAN_POINT ( 'NONE',  ( 1.648422021521518621, -0.9155690868286361361, 6.779860219333207816 ) ) ;
#17790=CARTESIAN_POINT ( 'NONE',  ( -1.053623506755599459, -4.865515740159335856, 2.921978671571880515 ) ) ;
#17792=CARTESIAN_POINT ( 'NONE',  ( 1.854177340199709922, -3.989623140882689434, 6.149404042554680316 ) ) ;
#17793=CARTESIAN_POINT ( 'NONE',  ( -2.408279507600840308, -4.800872354612795156, 5.815035204050404971 ) ) ;
#17795=CARTESIAN_POINT ( 'NONE',  ( 0.9123513484651973870, -3.547145663405211646, 2.860838000723751051 ) ) ;
#17798=CARTESIAN_POINT ( 'NONE',  ( 2.051695471449629160, -2.266289807549351387, 4.773807418740724451 ) ) ;
#17802=CARTESIAN_POINT ( 'NONE',  ( 1.741105240696918965, -0.4774152569121725143, 2.691996915772988608 ) ) ;
#17803=CARTESIAN_POINT ( 'NONE',  ( 2.161103922260819044, -2.103271789531340641, 3.159628768708413915 ) ) ;
#17807=CARTESIAN_POINT ( 'NONE',  ( 1.641808337277750107, -5.113135593220339281, 6.386111670537619744 ) ) ;
#17814=CARTESIAN_POINT ( 'NONE',  ( -1.707817112497179934, -5.488771186440679628, 6.319218296629480314 ) ) ;
#17815=CARTESIAN_POINT ( 'NONE',  ( -2.418933091173281369, -4.501965483225034426, 5.791730916219171021 ) ) ;
#17817=CARTESIAN_POINT ( 'NONE',  ( -2.652303127816829864, -3.333710192450643373, 4.791661394135809715 ) ) ;
#17820=CARTESIAN_POINT ( 'NONE',  ( -2.145694642186069867, -4.501965483225029985, 5.666819626392589626 ) ) ;
#17823=CARTESIAN_POINT ( 'NONE',  ( 2.635341251434490495, -2.588484967225421762, 5.013193520829454464 ) ) ;
#17828=CARTESIAN_POINT ( 'NONE',  ( 1.428515267734870031, -0.3311440677966109858, 2.829745655876919841 ) ) ;
#17829=CARTESIAN_POINT ( 'NONE',  ( 1.764807890102179977, -2.378890372630820149, 3.143016121304719857 ) ) ;
#17830=CARTESIAN_POINT ( 'NONE',  ( 0.009451942938126131968, -5.000194708068004701, 2.339951117923973367 ) ) ;
#17832=CARTESIAN_POINT ( 'NONE',  ( -1.889104232906369862, -5.555508474576269506, 3.296507079072529933 ) ) ;
#17838=CARTESIAN_POINT ( 'NONE',  ( 2.100188519621589922, -4.009070552810999999, 3.637948273607370275 ) ) ;
#17846=CARTESIAN_POINT ( 'NONE',  ( -1.145304265383870090, -3.077539021279469988, 6.755972720436099088 ) ) ;
#17848=CARTESIAN_POINT ( 'NONE',  ( 1.764143222953819867, -2.425466949207401690, 3.649904513135025841 ) ) ;
#17850=CARTESIAN_POINT ( 'NONE',  ( -1.221947981261169991, -0.5741044150835520332, 2.670403636935529956 ) ) ;
#17854=CARTESIAN_POINT ( 'NONE',  ( -2.065623031241579977, -5.033755237495680213, 3.572193642975310279 ) ) ;
#17862=CARTESIAN_POINT ( 'NONE',  ( 0.7093417302541469294, -5.135381355932199909, 6.943956659919690466 ) ) ;
#17866=CARTESIAN_POINT ( 'NONE',  ( 0.2564439965879030114, -1.055298816558370101, 7.039440566481209416 ) ) ;
#17869=CARTESIAN_POINT ( 'NONE',  ( -1.381042549632419902, -1.540511994252449890, 6.605640880016140137 ) ) ;
#17870=CARTESIAN_POINT ( 'NONE',  ( -2.586172839791708533, -0.2358050847457631438, 4.104546363490954697 ) ) ;
#17876=CARTESIAN_POINT ( 'NONE',  ( -2.342931736853879787, -1.497776294035839895, 4.477701633099188783 ) ) ;
#17878=CARTESIAN_POINT ( 'NONE',  ( -1.066267773695860122, -0.5741044150835525883, 2.929718414487351374 ) ) ;
#17879=CARTESIAN_POINT ( 'NONE',  ( -1.882879255550339082, -5.103620102360555855, 2.835213315261639000 ) ) ;
#17881=CARTESIAN_POINT ( 'NONE',  ( -1.440522616026439495, -4.804713230972779137, 3.241384813161591438 ) ) ;
#17882=CARTESIAN_POINT ( 'NONE',  ( -0.2818998297622349880, -4.245794312053860153, 7.036509827384409554 ) ) ;
#17883=CARTESIAN_POINT ( 'NONE',  ( 2.248786803694151182, -4.265241723982168942, 6.109280527266637506 ) ) ;
#17887=CARTESIAN_POINT ( 'NONE',  ( -1.842787987253248883, -1.889836318576769036, 3.794994874786233652 ) ) ;
#17890=CARTESIAN_POINT ( 'NONE',  ( 2.052909741356249373, -3.826605122864674247, 4.721527574705135066 ) ) ;
#17891=ORIENTED_EDGE ( 'NONE', *, *, #13244, .F. ) ;
#17894=AXIS2_PLACEMENT_3D ( 'NONE', #7306, #5920, #12954 ) ;
#17896=CARTESIAN_POINT ( 'NONE',  ( -1.901407128523849632, -2.848497014756559143, 6.551422324754827109 ) ) ;
#17901=CARTESIAN_POINT ( 'NONE',  ( -0.1910247150515231307, -5.295550847457634269, 2.655937705488500722 ) ) ;
#17908=CARTESIAN_POINT ( 'NONE',  ( -1.978267656359410154, -5.497669491525420504, 5.974740860598790171 ) ) ;
#17909=CARTESIAN_POINT ( 'NONE',  ( 2.380466601827069262, -3.710163681423226389, 3.526759849567131955 ) ) ;
#17910=CARTESIAN_POINT ( 'NONE',  ( -1.449852972480019764, -3.589881363621813648, 2.477154964647171109 ) ) ;
#17913=CARTESIAN_POINT ( 'NONE',  ( 1.417606053559480328, -0.8922807985403484743, 6.185023541745921172 ) ) ;
#17916=CARTESIAN_POINT ( 'NONE',  ( -0.6015868932279860859, -3.007674156414608557, 7.284803068494427158 ) ) ;
#17920=CARTESIAN_POINT ( 'NONE',  ( 2.253200202764420013, -0.3889830508474579895, 5.379408587037500133 ) ) ;
#17921=CARTESIAN_POINT ( 'NONE',  ( -0.2023972492402590084, -2.146007489747939978, 2.355265251465770149 ) ) ;
#17925=CARTESIAN_POINT ( 'NONE',  ( 1.873832970144350130, -5.337500000000000355, 2.826167029855650270 ) ) ;
#17930=CARTESIAN_POINT ( 'NONE',  ( 2.332582362116870200, -5.068644067796608255, 4.387643303570811781 ) ) ;
#17932=CARTESIAN_POINT ( 'NONE',  ( -0.0009602353114164120101, -0.4652189165859030306, 2.501032900279570370 ) ) ;
#17937=CARTESIAN_POINT ( 'NONE',  ( -1.917298190932639868, -3.496728210468659892, 3.335187436117939885 ) ) ;
#17939=CARTESIAN_POINT ( 'NONE',  ( 2.023259452208809872, -2.425466949207399914, 3.497849062500220096 ) ) ;
#17941=CARTESIAN_POINT ( 'NONE',  ( -2.296954468777729463, -4.963890372630819670, 4.187412587068699565 ) ) ;
#17942=CARTESIAN_POINT ( 'NONE',  ( 0.7616804549307097938, -2.262448931189378509, 2.793499350326721142 ) ) ;
#17949=CARTESIAN_POINT ( 'NONE',  ( -2.135041058613629694, -4.800872354612799597, 5.690123914223820023 ) ) ;
#17957=CARTESIAN_POINT ( 'NONE',  ( 0.06264882350516240428, -5.148728813559320550, 7.052569299041220319 ) ) ;
#17961=CARTESIAN_POINT ( 'NONE',  ( 2.218077401483169897, -0.7758393570989060573, 5.486688202856499608 ) ) ;
#17962=AXIS2_PLACEMENT_3D ( 'NONE', #12853, #5908, #11549 ) ;
#17964=CARTESIAN_POINT ( 'NONE',  ( 2.287919158821199783, -1.051457940198389895, 5.251517552016890633 ) ) ;
#17965=CARTESIAN_POINT ( 'NONE',  ( 1.978267656359410154, -0.1023305084745769894, 5.974740860598790171 ) ) ;
#17968=CARTESIAN_POINT ( 'NONE',  ( -2.058670345754650022, -0.5491525423728820243, 3.559656372813929881 ) ) ;
#17971=CARTESIAN_POINT ( 'NONE',  ( 0.4221287159901364605, -0.1423728813559330397, 7.320050063945812369 ) ) ;
#17977=CARTESIAN_POINT ( 'NONE',  ( -1.526791597786389287, -2.825208726468270370, 6.490992212270281669 ) ) ;
#17978=CARTESIAN_POINT ( 'NONE',  ( -2.116444151961480280, -5.546610169491529518, 3.670839500609359707 ) ) ;
#17979=CARTESIAN_POINT ( 'NONE',  ( -2.622715975066178817, -4.870737219477664581, 5.105554690683034913 ) ) ;
#17981=CARTESIAN_POINT ( 'NONE',  ( -1.074005996636800075, -5.164643153926310681, 2.934052701886380010 ) ) ;
#17982=CARTESIAN_POINT ( 'NONE',  ( 2.051973656473811136, -0.6826862039457533005, 4.634380218157459375 ) ) ;
#17983=CARTESIAN_POINT ( 'NONE',  ( -2.159308672244651284, -4.754295778036219389, 6.242886823772542115 ) ) ;
#17987=CARTESIAN_POINT ( 'NONE',  ( 0.4365326870214371602, -1.330917399657850497, 6.706076034398976482 ) ) ;
#17993=CARTESIAN_POINT ( 'NONE',  ( 1.754713504580569960, -0.3489406779661023417, 3.634325740584615883 ) ) ;
#17994=CARTESIAN_POINT ( 'NONE',  ( -1.370891210199559618, -1.730659176918718956, 2.427606771969371469 ) ) ;
#17997=CARTESIAN_POINT ( 'NONE',  ( 2.000624272291700034, -5.364194915254235418, 4.239366054775996595 ) ) ;
#18005=CARTESIAN_POINT ( 'NONE',  ( 1.641808337277750107, -5.413135593220339103, 6.386111670537619744 ) ) ;
#18006=CARTESIAN_POINT ( 'NONE',  ( 0.4247583764261176897, -4.175929447188994281, 7.319674410047496416 ) ) ;
#18008=CARTESIAN_POINT ( 'NONE',  ( 1.802718065953961002, -0.5662447625043125488, 3.717600174934180046 ) ) ;
#18013=CARTESIAN_POINT ( 'NONE',  ( 1.766091042938769951, -5.222834417938730489, 2.933908957061230005 ) ) ;
#18014=CARTESIAN_POINT ( 'NONE',  ( 1.192209327851080136, -0.3222457627118649470, 2.329031440774910422 ) ) ;
#18015=CARTESIAN_POINT ( 'NONE',  ( -1.710920205120030069, -1.587088570829020107, 6.316012914303580139 ) ) ;
#18017=DIRECTION ( 'NONE',  ( 0.000000000000000000, -1.000000000000000000, 0.000000000000000000 ) ) ;
#18018=CARTESIAN_POINT ( 'NONE',  ( -0.1765068388402301069, -5.453177966101685037, 7.347961541693632803 ) ) ;
#18022=CARTESIAN_POINT ( 'NONE',  ( -1.549742865090599997, -5.184322033898308923, 6.471102547561461193 ) ) ;
#18028=CARTESIAN_POINT ( 'NONE',  ( -0.03714311608457869507, -4.521412895153340550, 7.053160869216429596 ) ) ;
#18030=CARTESIAN_POINT ( 'NONE',  ( 1.307725206348619995, -0.7471169921413569615, 2.732408283416570161 ) ) ;
#18031=CARTESIAN_POINT ( 'NONE',  ( -0.009452110982655114943, -5.299807955295455564, 2.050000000000001155 ) ) ;
#18034=CARTESIAN_POINT ( 'NONE',  ( 1.074829861819710075, -2.285737219477669946, 2.606322265575589991 ) ) ;
#18036=CARTESIAN_POINT ( 'NONE',  ( 1.404946080800569375, -2.355602084342530933, 3.202993536195909208 ) ) ;
#18039=CARTESIAN_POINT ( 'NONE',  ( -0.1926573868394080846, -0.2965485159365558454, 2.049233193116839935 ) ) ;
#18042=CARTESIAN_POINT ( 'NONE',  ( -1.722199153441400066, -5.095857339597789526, 3.099360556065549943 ) ) ;
#18047=CARTESIAN_POINT ( 'NONE',  ( 1.432215783582721613, -5.113135593220339281, 6.170863372171116801 ) ) ;
#18052=CARTESIAN_POINT ( 'NONE',  ( -1.552749016687749783, -1.563800282540730002, 6.468535037441760061 ) ) ;
#18054=CARTESIAN_POINT ( 'NONE',  ( 1.596341326794969984, -0.03559322033898330156, 2.970780074643809776 ) ) ;
#18059=CARTESIAN_POINT ( 'NONE',  ( 2.540842781840729536, -0.08898305084745804228, 5.466141598148674952 ) ) ;
#18063=CARTESIAN_POINT ( 'NONE',  ( 0.9485663501270545916, -2.545749267008809991, 6.853826262002240099 ) ) ;
#18064=CARTESIAN_POINT ( 'NONE',  ( -1.889104232906369862, -5.555508474576269506, 3.296507079072529933 ) ) ;
#18065=CARTESIAN_POINT ( 'NONE',  ( 2.501774541437309374, -0.7758393570989061683, 5.585572039315881199 ) ) ;
#18068=CARTESIAN_POINT ( 'NONE',  ( 1.668733558229380520, -0.8457042219637719294, 5.895922302771890777 ) ) ;
#18069=CARTESIAN_POINT ( 'NONE',  ( 2.437122747866759198, -0.5895330507926000996, 3.649501829874934433 ) ) ;
#18072=CARTESIAN_POINT ( 'NONE',  ( -1.353302556710470395, -1.563800282540731779, 6.243850391919187892 ) ) ;
#18078=CARTESIAN_POINT ( 'NONE',  ( -2.000624272291700034, -0.2358050847457631438, 4.239366054776020576 ) ) ;
#18080=B_SPLINE_CURVE_WITH_KNOTS ( 'NONE', 3,
 ( #9514, #805, #16175, #15173, #16269, #3572, #7841 ),
 .UNSPECIFIED., .F., .F.,
 ( 4, 1, 1, 1, 4 ),
 ( 0.000000000000000000, 0.3003308066894049833, 0.4325493167363730351, 0.5576349185191149527, 0.7853981633974479459 ),
 .UNSPECIFIED. ) ;
#18081=CARTESIAN_POINT ( 'NONE',  ( 2.295344368707611160, -2.126560077819629413, 3.367893426919545519 ) ) ;
#18082=CARTESIAN_POINT ( 'NONE',  ( -0.009452110982656913851, -5.299807955295455564, 2.050000000000001155 ) ) ;
#18083=CARTESIAN_POINT ( 'NONE',  ( -1.980638384804660257, -5.237711864406785267, 4.159858630563765480 ) ) ;
#18089=CARTESIAN_POINT ( 'NONE',  ( -2.306642602145299925, -5.515466101694909362, 5.166805192608490138 ) ) ;
#18090=CARTESIAN_POINT ( 'NONE',  ( -0.3162622016569221484, -4.245794312053864594, 7.334974746141788238 ) ) ;
#18091=CARTESIAN_POINT ( 'NONE',  ( -2.574214976178951009, -3.403575057315514130, 4.054607910322786779 ) ) ;
#18094=CARTESIAN_POINT ( 'NONE',  ( 1.458615186838411626, -0.4963798976394455664, 3.259477383973563125 ) ) ;
#18099=CARTESIAN_POINT ( 'NONE',  ( -1.925796468768790071, -0.4957627118644070130, 6.052706598917719560 ) ) ;
#18100=CARTESIAN_POINT ( 'NONE',  ( -1.948278411993560111, -3.193980462720909852, 6.020210936496040333 ) ) ;
#18103=CARTESIAN_POINT ( 'NONE',  ( 0.7998959936908462964, -5.435381355932195291, 7.230419212249866945 ) ) ;
#18110=CARTESIAN_POINT ( 'NONE',  ( 1.994983296312400123, -4.265241723982169830, 5.948514050749290405 ) ) ;
#18111=CARTESIAN_POINT ( 'NONE',  ( 0.8534102632286154622, -5.320452325212860600, 2.829778315381550780 ) ) ;
#18115=CARTESIAN_POINT ( 'NONE',  ( -2.219956784870669608, -3.426863345603790023, 3.918630970161619764 ) ) ;
#18117=CARTESIAN_POINT ( 'NONE',  ( -0.8259795455965642796, -3.054250732991181216, 6.579537079411896805 ) ) ;
#18119=CARTESIAN_POINT ( 'NONE',  ( -0.1471036068827911436, -0.2965485159365571777, 2.649244128781490737 ) ) ;
#18127=CARTESIAN_POINT ( 'NONE',  ( -1.351903350398179438, -5.184322033898315141, 6.245004350000422200 ) ) ;
#18133=CARTESIAN_POINT ( 'NONE',  ( -2.005512128484160161, -1.913124606865060029, 3.468469736471389897 ) ) ;
#18134=CARTESIAN_POINT ( 'NONE',  ( 0.07299321914061039640, -0.001483050847457899942, 2.350000000000000089 ) ) ;
#18136=CARTESIAN_POINT ( 'NONE',  ( 2.345900685764729765, -0.3711864406779670222, 4.512231114381330066 ) ) ;
#18137=CARTESIAN_POINT ( 'NONE',  ( 2.306642602145299925, -0.3845338983050849979, 5.166805192608480368 ) ) ;
#18139=CARTESIAN_POINT ( 'NONE',  ( 1.246151616534670215, -0.03114406779661053892, 3.068501529594759081 ) ) ;
#18143=CARTESIAN_POINT ( 'NONE',  ( -1.832842064134659665, -2.871785303044850579, 6.176291182464519913 ) ) ;
#18145=CARTESIAN_POINT ( 'NONE',  ( -1.747582379783008788, -5.484322033898315851, 6.697200745122486865 ) ) ;
#18148=CARTESIAN_POINT ( 'NONE',  ( -2.091095264232510242, -1.656953435693890198, 5.779845490516250628 ) ) ;
#18150=CARTESIAN_POINT ( 'NONE',  ( -1.134881315981510541, -0.4779661016949154906, 6.410767520434657918 ) ) ;
#18155=CARTESIAN_POINT ( 'NONE',  ( 1.688800633088581860, -0.8418633456037974971, 3.532586505616389871 ) ) ;
#18160=CARTESIAN_POINT ( 'NONE',  ( 1.921786527979010062, -0.3578389830508479363, 3.977907449687776431 ) ) ;
#18161=CARTESIAN_POINT ( 'NONE',  ( 1.132648842710480830, -4.106064582324130185, 7.100045893750476900 ) ) ;
#18162=CARTESIAN_POINT ( 'NONE',  ( -1.053623506755599459, -4.865515740159335856, 2.921978671571880515 ) ) ;
#18163=CARTESIAN_POINT ( 'NONE',  ( 1.494593880360790550, -5.338983050847455836, 3.295456077495951153 ) ) ;
#18166=CARTESIAN_POINT ( 'NONE',  ( 1.438959988998139914E-16, 0.000000000000000000, 2.350000000000000089 ) ) ;
#18168=CARTESIAN_POINT ( 'NONE',  ( -1.377628188826471423, -0.5741044150835525883, 2.411088859383701433 ) ) ;
#18171=CARTESIAN_POINT ( 'NONE',  ( -2.340070819011249803, -5.519915254237290014, 4.950151441910549899 ) ) ;
#18173=CARTESIAN_POINT ( 'NONE',  ( 2.235075160050071119, -3.966334852594401994, 6.130927224539736820 ) ) ;
#18176=CARTESIAN_POINT ( 'NONE',  ( -1.835037444103819970, -1.358046564306109261, 5.620619042473610882 ) ) ;
#18181=CARTESIAN_POINT ( 'NONE',  ( 1.851073041990159984, -0.4067796610169499560, 6.153284478378259870 ) ) ;
#18182=CARTESIAN_POINT ( 'NONE',  ( 1.353103843060669886, -2.798079561820010053, 6.625579309552930063 ) ) ;
#18185=CARTESIAN_POINT ( 'NONE',  ( 2.578017356471871135, -5.086440677966105994, 5.329826563567761077 ) ) ;
#18195=CARTESIAN_POINT ( 'NONE',  ( -2.334032080503389839, -3.310421904162350160, 5.001728246382240783 ) ) ;
#18197=CARTESIAN_POINT ( 'NONE',  ( 0.9788656693287738353, -5.320452325212859712, 2.556357798777459944 ) ) ;
#18200=CARTESIAN_POINT ( 'NONE',  ( 1.026235786675480099, -4.404971453711899798, 6.817920158464540137 ) ) ;
#18203=CARTESIAN_POINT ( 'NONE',  ( 0.2993653819235879698, -2.914521003261450360, 6.731079075450741911 ) ) ;
#18209=CARTESIAN_POINT ( 'NONE',  ( -0.009452110982655708218, -0.5998079552954630467, 2.350000000000000089 ) ) ;
#18219=CARTESIAN_POINT ( 'NONE',  ( -1.246151616534680651, -5.268855932203385883, 3.068501529594771071 ) ) ;
#18220=CARTESIAN_POINT ( 'NONE',  ( -2.470260739716218179, -1.567641158900710430, 3.729986819255259878 ) ) ;
#18228=CARTESIAN_POINT ( 'NONE',  ( 1.902324933209389890, -2.402178660919109809, 3.314393441133530072 ) ) ;
#18232=CARTESIAN_POINT ( 'NONE',  ( -2.048006021857541548, -3.058091609351150986, 4.556566471620694614 ) ) ;
#18234=CARTESIAN_POINT ( 'NONE',  ( -1.925796468768790071, -0.1957627118644069963, 6.052706598917719560 ) ) ;
#18239=CARTESIAN_POINT ( 'NONE',  ( -0.7093417302541390468, -0.1646186440677969987, 6.943956659919700236 ) ) ;
#18245=CARTESIAN_POINT ( 'NONE',  ( -2.190084968185499914, -1.567641158900710208, 3.838447030292489348 ) ) ;
#18246=CARTESIAN_POINT ( 'NONE',  ( -3.408368997776849933E-15, -5.599999999999999645, 2.350000000000000089 ) ) ;
#18250=CARTESIAN_POINT ( 'NONE',  ( 2.287919158821199783, -1.051457940198389895, 5.251517552016890633 ) ) ;
#18251=CARTESIAN_POINT ( 'NONE',  ( -1.562863241354461641, -0.4913135593220345210, 6.031217337312382298 ) ) ;
#18259=CARTESIAN_POINT ( 'NONE',  ( -1.485933537025771356, -4.796950468210009255, 3.286232459959995911 ) ) ;
#18266=CARTESIAN_POINT ( 'NONE',  ( -1.580445181003969912, -0.2580508474576271305, 3.389704561770339630 ) ) ;
#18267=CARTESIAN_POINT ( 'NONE',  ( 0.6672256841321406728, -4.152641158900696183, 7.268642361138727637 ) ) ;
#18270=CARTESIAN_POINT ( 'NONE',  ( -0.5230055860628765041, -5.251463457376924104, 2.087624054227240844 ) ) ;
#18271=CARTESIAN_POINT ( 'NONE',  ( -1.614765845140348821, -5.193220338983044471, 5.967758800287426446 ) ) ;
#18276=CARTESIAN_POINT ( 'NONE',  ( -0.1869574461324000070, -0.5962015548080630278, 2.350675676344399889 ) ) ;
#18281=CARTESIAN_POINT ( 'NONE',  ( -0.3949552299395130417, -1.823812330071880039, 2.379923265530350385 ) ) ;
#18284=CARTESIAN_POINT ( 'NONE',  ( -2.016543577558690625, -1.521064582324129777, 4.314702916654059806 ) ) ;
ENDSEC;
END-ISO-10303-21;
